ISO-10303-21;
HEADER;
/* Generated by software containing ST-Developer
 * from STEP Tools, Inc. (www.steptools.com) 
 */

FILE_DESCRIPTION(
/* description */ (''),
/* implementation_level */ '2;1');

FILE_NAME(
/* name */ '15_Offset_Adjusting_Screw_ISO_4017_M12x40.step',
/* time_stamp */ '2026-10-26T03:50:32-07:00',
/* author */ (''),
/* organization */ (''),
/* preprocessor_version */ 'ST-DEVELOPER v20.2',
/* originating_system */ 'Autodesk Translation Framework v15.15.0.0',
/* authorisation */ '');

FILE_SCHEMA (('AUTOMOTIVE_DESIGN { 1 0 10303 214 3 1 1 }'));
ENDSEC;

DATA;
#10=MECHANICAL_DESIGN_GEOMETRIC_PRESENTATION_REPRESENTATION('',(#1056),#76660);
#130=(
BOUNDED_CURVE()
B_SPLINE_CURVE(2,(#68996,#68997,#68998),.UNSPECIFIED.,.F.,.F.)
B_SPLINE_CURVE_WITH_KNOTS((3,3),(0.0817872044632405,1.1645820942826),
 .UNSPECIFIED.)
CURVE()
GEOMETRIC_REPRESENTATION_ITEM()
RATIONAL_B_SPLINE_CURVE((1.02578342306321,1.1844726708716,1.02578342306321))
REPRESENTATION_ITEM('')
);
#131=(
BOUNDED_CURVE()
B_SPLINE_CURVE(2,(#69000,#69001,#69002),.UNSPECIFIED.,.F.,.F.)
B_SPLINE_CURVE_WITH_KNOTS((3,3),(0.0817872044632409,1.1645820942826),
 .UNSPECIFIED.)
CURVE()
GEOMETRIC_REPRESENTATION_ITEM()
RATIONAL_B_SPLINE_CURVE((1.02578342306321,1.1844726708716,1.02578342306321))
REPRESENTATION_ITEM('')
);
#132=(
BOUNDED_CURVE()
B_SPLINE_CURVE(2,(#69004,#69005,#69006),.UNSPECIFIED.,.F.,.F.)
B_SPLINE_CURVE_WITH_KNOTS((3,3),(0.0817872044632405,1.1645820942826),
 .UNSPECIFIED.)
CURVE()
GEOMETRIC_REPRESENTATION_ITEM()
RATIONAL_B_SPLINE_CURVE((1.02578342306321,1.1844726708716,1.02578342306321))
REPRESENTATION_ITEM('')
);
#133=(
BOUNDED_CURVE()
B_SPLINE_CURVE(2,(#69008,#69009,#69010),.UNSPECIFIED.,.F.,.F.)
B_SPLINE_CURVE_WITH_KNOTS((3,3),(0.0817872044632409,1.1645820942826),
 .UNSPECIFIED.)
CURVE()
GEOMETRIC_REPRESENTATION_ITEM()
RATIONAL_B_SPLINE_CURVE((1.02578342306321,1.1844726708716,1.02578342306321))
REPRESENTATION_ITEM('')
);
#134=(
BOUNDED_CURVE()
B_SPLINE_CURVE(2,(#69012,#69013,#69014),.UNSPECIFIED.,.F.,.F.)
B_SPLINE_CURVE_WITH_KNOTS((3,3),(0.623184649372919,1.1645820942826),
 .UNSPECIFIED.)
CURVE()
GEOMETRIC_REPRESENTATION_ITEM()
RATIONAL_B_SPLINE_CURVE((1.1051280469674,1.1051280469674,1.02578342306321))
REPRESENTATION_ITEM('')
);
#135=(
BOUNDED_CURVE()
B_SPLINE_CURVE(2,(#69019,#69020,#69021),.UNSPECIFIED.,.F.,.F.)
B_SPLINE_CURVE_WITH_KNOTS((3,3),(0.081787204463241,0.623184649372919),
 .UNSPECIFIED.)
CURVE()
GEOMETRIC_REPRESENTATION_ITEM()
RATIONAL_B_SPLINE_CURVE((1.02578342306321,1.1051280469674,1.1051280469674))
REPRESENTATION_ITEM('')
);
#136=(
BOUNDED_CURVE()
B_SPLINE_CURVE(2,(#69022,#69023,#69024),.UNSPECIFIED.,.F.,.F.)
B_SPLINE_CURVE_WITH_KNOTS((3,3),(0.0817872044632407,1.1645820942826),
 .UNSPECIFIED.)
CURVE()
GEOMETRIC_REPRESENTATION_ITEM()
RATIONAL_B_SPLINE_CURVE((1.02578342306321,1.1844726708716,1.02578342306321))
REPRESENTATION_ITEM('')
);
#168=B_SPLINE_SURFACE_WITH_KNOTS('',3,3,((#66314,#66315,#66316,#66317,#66318,
#66319,#66320,#66321,#66322,#66323,#66324,#66325,#66326,#66327,#66328,#66329,
#66330,#66331,#66332,#66333,#66334,#66335,#66336,#66337,#66338,#66339,#66340,
#66341,#66342,#66343,#66344,#66345,#66346,#66347,#66348,#66349,#66350,#66351,
#66352,#66353,#66354,#66355,#66356,#66357,#66358,#66359,#66360,#66361,#66362,
#66363,#66364,#66365,#66366,#66367,#66368,#66369,#66370,#66371,#66372,#66373,
#66374,#66375,#66376,#66377,#66378,#66379,#66380,#66381,#66382,#66383,#66384,
#66385,#66386,#66387,#66388,#66389,#66390,#66391,#66392,#66393,#66394,#66395,
#66396,#66397,#66398,#66399,#66400,#66401,#66402,#66403,#66404,#66405,#66406,
#66407,#66408,#66409,#66410,#66411,#66412,#66413,#66414,#66415,#66416,#66417,
#66418,#66419,#66420,#66421,#66422,#66423,#66424,#66425,#66426,#66427,#66428,
#66429,#66430,#66431,#66432,#66433,#66434,#66435,#66436,#66437,#66438,#66439,
#66440,#66441,#66442,#66443,#66444,#66445,#66446,#66447,#66448,#66449,#66450,
#66451,#66452,#66453,#66454,#66455,#66456,#66457,#66458,#66459,#66460,#66461,
#66462,#66463,#66464,#66465,#66466,#66467,#66468,#66469,#66470,#66471,#66472,
#66473,#66474,#66475,#66476,#66477,#66478,#66479,#66480,#66481,#66482,#66483,
#66484,#66485,#66486,#66487,#66488,#66489,#66490,#66491,#66492,#66493,#66494,
#66495,#66496,#66497,#66498,#66499,#66500,#66501,#66502,#66503,#66504,#66505,
#66506,#66507,#66508,#66509,#66510,#66511,#66512,#66513,#66514,#66515,#66516,
#66517,#66518,#66519,#66520,#66521,#66522,#66523,#66524,#66525,#66526,#66527,
#66528,#66529,#66530,#66531,#66532,#66533,#66534,#66535,#66536,#66537,#66538,
#66539,#66540,#66541,#66542,#66543,#66544,#66545,#66546,#66547,#66548,#66549,
#66550,#66551,#66552,#66553,#66554,#66555,#66556,#66557,#66558,#66559,#66560,
#66561,#66562,#66563,#66564,#66565,#66566,#66567,#66568,#66569,#66570,#66571,
#66572,#66573,#66574,#66575,#66576,#66577,#66578,#66579,#66580,#66581,#66582,
#66583,#66584,#66585,#66586,#66587,#66588,#66589,#66590,#66591,#66592,#66593,
#66594,#66595,#66596,#66597,#66598,#66599,#66600,#66601,#66602,#66603,#66604),
(#66605,#66606,#66607,#66608,#66609,#66610,#66611,#66612,#66613,#66614,
#66615,#66616,#66617,#66618,#66619,#66620,#66621,#66622,#66623,#66624,#66625,
#66626,#66627,#66628,#66629,#66630,#66631,#66632,#66633,#66634,#66635,#66636,
#66637,#66638,#66639,#66640,#66641,#66642,#66643,#66644,#66645,#66646,#66647,
#66648,#66649,#66650,#66651,#66652,#66653,#66654,#66655,#66656,#66657,#66658,
#66659,#66660,#66661,#66662,#66663,#66664,#66665,#66666,#66667,#66668,#66669,
#66670,#66671,#66672,#66673,#66674,#66675,#66676,#66677,#66678,#66679,#66680,
#66681,#66682,#66683,#66684,#66685,#66686,#66687,#66688,#66689,#66690,#66691,
#66692,#66693,#66694,#66695,#66696,#66697,#66698,#66699,#66700,#66701,#66702,
#66703,#66704,#66705,#66706,#66707,#66708,#66709,#66710,#66711,#66712,#66713,
#66714,#66715,#66716,#66717,#66718,#66719,#66720,#66721,#66722,#66723,#66724,
#66725,#66726,#66727,#66728,#66729,#66730,#66731,#66732,#66733,#66734,#66735,
#66736,#66737,#66738,#66739,#66740,#66741,#66742,#66743,#66744,#66745,#66746,
#66747,#66748,#66749,#66750,#66751,#66752,#66753,#66754,#66755,#66756,#66757,
#66758,#66759,#66760,#66761,#66762,#66763,#66764,#66765,#66766,#66767,#66768,
#66769,#66770,#66771,#66772,#66773,#66774,#66775,#66776,#66777,#66778,#66779,
#66780,#66781,#66782,#66783,#66784,#66785,#66786,#66787,#66788,#66789,#66790,
#66791,#66792,#66793,#66794,#66795,#66796,#66797,#66798,#66799,#66800,#66801,
#66802,#66803,#66804,#66805,#66806,#66807,#66808,#66809,#66810,#66811,#66812,
#66813,#66814,#66815,#66816,#66817,#66818,#66819,#66820,#66821,#66822,#66823,
#66824,#66825,#66826,#66827,#66828,#66829,#66830,#66831,#66832,#66833,#66834,
#66835,#66836,#66837,#66838,#66839,#66840,#66841,#66842,#66843,#66844,#66845,
#66846,#66847,#66848,#66849,#66850,#66851,#66852,#66853,#66854,#66855,#66856,
#66857,#66858,#66859,#66860,#66861,#66862,#66863,#66864,#66865,#66866,#66867,
#66868,#66869,#66870,#66871,#66872,#66873,#66874,#66875,#66876,#66877,#66878,
#66879,#66880,#66881,#66882,#66883,#66884,#66885,#66886,#66887,#66888,#66889,
#66890,#66891,#66892,#66893,#66894,#66895),(#66896,#66897,#66898,#66899,
#66900,#66901,#66902,#66903,#66904,#66905,#66906,#66907,#66908,#66909,#66910,
#66911,#66912,#66913,#66914,#66915,#66916,#66917,#66918,#66919,#66920,#66921,
#66922,#66923,#66924,#66925,#66926,#66927,#66928,#66929,#66930,#66931,#66932,
#66933,#66934,#66935,#66936,#66937,#66938,#66939,#66940,#66941,#66942,#66943,
#66944,#66945,#66946,#66947,#66948,#66949,#66950,#66951,#66952,#66953,#66954,
#66955,#66956,#66957,#66958,#66959,#66960,#66961,#66962,#66963,#66964,#66965,
#66966,#66967,#66968,#66969,#66970,#66971,#66972,#66973,#66974,#66975,#66976,
#66977,#66978,#66979,#66980,#66981,#66982,#66983,#66984,#66985,#66986,#66987,
#66988,#66989,#66990,#66991,#66992,#66993,#66994,#66995,#66996,#66997,#66998,
#66999,#67000,#67001,#67002,#67003,#67004,#67005,#67006,#67007,#67008,#67009,
#67010,#67011,#67012,#67013,#67014,#67015,#67016,#67017,#67018,#67019,#67020,
#67021,#67022,#67023,#67024,#67025,#67026,#67027,#67028,#67029,#67030,#67031,
#67032,#67033,#67034,#67035,#67036,#67037,#67038,#67039,#67040,#67041,#67042,
#67043,#67044,#67045,#67046,#67047,#67048,#67049,#67050,#67051,#67052,#67053,
#67054,#67055,#67056,#67057,#67058,#67059,#67060,#67061,#67062,#67063,#67064,
#67065,#67066,#67067,#67068,#67069,#67070,#67071,#67072,#67073,#67074,#67075,
#67076,#67077,#67078,#67079,#67080,#67081,#67082,#67083,#67084,#67085,#67086,
#67087,#67088,#67089,#67090,#67091,#67092,#67093,#67094,#67095,#67096,#67097,
#67098,#67099,#67100,#67101,#67102,#67103,#67104,#67105,#67106,#67107,#67108,
#67109,#67110,#67111,#67112,#67113,#67114,#67115,#67116,#67117,#67118,#67119,
#67120,#67121,#67122,#67123,#67124,#67125,#67126,#67127,#67128,#67129,#67130,
#67131,#67132,#67133,#67134,#67135,#67136,#67137,#67138,#67139,#67140,#67141,
#67142,#67143,#67144,#67145,#67146,#67147,#67148,#67149,#67150,#67151,#67152,
#67153,#67154,#67155,#67156,#67157,#67158,#67159,#67160,#67161,#67162,#67163,
#67164,#67165,#67166,#67167,#67168,#67169,#67170,#67171,#67172,#67173,#67174,
#67175,#67176,#67177,#67178,#67179,#67180,#67181,#67182,#67183,#67184,#67185,
#67186),(#67187,#67188,#67189,#67190,#67191,#67192,#67193,#67194,#67195,
#67196,#67197,#67198,#67199,#67200,#67201,#67202,#67203,#67204,#67205,#67206,
#67207,#67208,#67209,#67210,#67211,#67212,#67213,#67214,#67215,#67216,#67217,
#67218,#67219,#67220,#67221,#67222,#67223,#67224,#67225,#67226,#67227,#67228,
#67229,#67230,#67231,#67232,#67233,#67234,#67235,#67236,#67237,#67238,#67239,
#67240,#67241,#67242,#67243,#67244,#67245,#67246,#67247,#67248,#67249,#67250,
#67251,#67252,#67253,#67254,#67255,#67256,#67257,#67258,#67259,#67260,#67261,
#67262,#67263,#67264,#67265,#67266,#67267,#67268,#67269,#67270,#67271,#67272,
#67273,#67274,#67275,#67276,#67277,#67278,#67279,#67280,#67281,#67282,#67283,
#67284,#67285,#67286,#67287,#67288,#67289,#67290,#67291,#67292,#67293,#67294,
#67295,#67296,#67297,#67298,#67299,#67300,#67301,#67302,#67303,#67304,#67305,
#67306,#67307,#67308,#67309,#67310,#67311,#67312,#67313,#67314,#67315,#67316,
#67317,#67318,#67319,#67320,#67321,#67322,#67323,#67324,#67325,#67326,#67327,
#67328,#67329,#67330,#67331,#67332,#67333,#67334,#67335,#67336,#67337,#67338,
#67339,#67340,#67341,#67342,#67343,#67344,#67345,#67346,#67347,#67348,#67349,
#67350,#67351,#67352,#67353,#67354,#67355,#67356,#67357,#67358,#67359,#67360,
#67361,#67362,#67363,#67364,#67365,#67366,#67367,#67368,#67369,#67370,#67371,
#67372,#67373,#67374,#67375,#67376,#67377,#67378,#67379,#67380,#67381,#67382,
#67383,#67384,#67385,#67386,#67387,#67388,#67389,#67390,#67391,#67392,#67393,
#67394,#67395,#67396,#67397,#67398,#67399,#67400,#67401,#67402,#67403,#67404,
#67405,#67406,#67407,#67408,#67409,#67410,#67411,#67412,#67413,#67414,#67415,
#67416,#67417,#67418,#67419,#67420,#67421,#67422,#67423,#67424,#67425,#67426,
#67427,#67428,#67429,#67430,#67431,#67432,#67433,#67434,#67435,#67436,#67437,
#67438,#67439,#67440,#67441,#67442,#67443,#67444,#67445,#67446,#67447,#67448,
#67449,#67450,#67451,#67452,#67453,#67454,#67455,#67456,#67457,#67458,#67459,
#67460,#67461,#67462,#67463,#67464,#67465,#67466,#67467,#67468,#67469,#67470,
#67471,#67472,#67473,#67474,#67475,#67476,#67477)),.UNSPECIFIED.,.F.,.F.,
 .F.,(4,4),(4,1,1,1,1,1,1,1,1,1,1,1,1,1,1,1,1,1,1,1,1,1,1,1,1,1,1,1,1,1,
1,1,1,1,1,1,1,1,1,1,1,1,1,1,1,1,1,1,1,1,1,1,1,1,1,1,1,1,1,1,1,1,1,1,1,1,
1,1,1,1,1,1,1,1,1,1,1,1,1,1,1,1,1,1,1,1,1,1,1,1,1,1,1,1,1,1,1,1,1,1,1,1,
1,1,1,1,1,1,1,1,1,1,1,1,1,1,1,1,1,1,1,1,1,1,1,1,1,1,1,1,1,1,1,1,1,1,1,1,
1,1,1,1,1,1,1,1,1,1,1,1,1,1,1,1,1,1,1,1,1,1,1,1,1,1,1,1,1,1,1,1,1,1,1,1,
1,1,1,1,1,1,1,1,1,1,1,1,1,1,1,1,1,1,1,1,1,1,1,1,1,1,1,1,1,1,1,1,1,1,1,1,
1,1,1,1,1,1,1,1,1,1,1,1,1,1,1,1,1,1,1,1,1,1,1,1,1,1,1,1,1,1,1,1,1,1,1,1,
1,1,1,1,1,1,1,1,1,1,1,1,1,1,1,1,1,1,1,1,1,1,1,1,1,1,1,1,1,1,1,1,1,1,1,1,
1,1,1,1,1,1,4),(0.,0.115296848757168),(8.30592286723176,8.80533305296603,
9.30474323870031,9.80415342443458,10.3035636101689,10.8029737959031,11.3023839816374,
11.8017941673717,12.301204353106,12.8006145388402,13.3000247245745,13.7994349103088,
14.298845096043,14.7982552817773,15.2976654675116,15.7970756532459,16.2964858389801,
16.7958960247144,17.2953062104487,17.794716396183,18.2941265819172,18.7935367676515,
19.2929469533858,19.7923571391201,20.2917673248543,20.7911775105886,21.2905876963229,
21.7899978820572,22.2894080677914,22.7888182535257,23.28822843926,23.7876386249943,
24.2870488107285,24.7864589964628,25.2858691821971,25.7852793679313,26.2846895536656,
26.7840997393999,27.2835099251342,27.7829201108684,28.2823302966027,28.781740482337,
29.2811506680713,29.7805608538055,30.2799710395398,30.7793812252741,31.2787914110084,
31.7782015967426,32.2776117824769,32.7770219682112,33.2764321539455,33.7758423396797,
34.275252525414,34.7746627111483,35.2740728968826,35.7734830826168,36.2728932683511,
36.7723034540854,37.2717136398197,37.7711238255539,38.2705340112882,38.7699441970225,
39.2693543827567,39.768764568491,40.2681747542253,40.7675849399596,41.2669951256938,
41.7664053114281,42.2658154971624,42.7652256828967,43.2646358686309,43.7640460543652,
44.2634562400995,44.7628664258338,45.262276611568,45.7616867973023,46.2610969830366,
46.7605071687709,47.2599173545051,47.7593275402394,48.2587377259737,48.758147911708,
49.2575580974422,49.7569682831765,50.2563784689108,50.755788654645,51.2551988403793,
51.7546090261136,52.2540192118479,52.7534293975821,53.2528395833164,53.7522497690507,
54.251659954785,54.7510701405192,55.2504803262535,55.7498905119878,56.2493006977221,
56.7487108834563,57.2481210691906,57.7475312549249,58.2469414406592,58.7463516263934,
59.2457618121277,59.745171997862,60.2445821835963,60.7439923693305,61.2434025550648,
61.7428127407991,62.2422229265333,62.7416331122676,63.2410432980019,63.7404534837362,
64.2398636694704,64.7392738552047,65.238684040939,65.7380942266733,66.2375044124075,
66.7369145981418,67.2363247838761,67.7357349696103,68.2351451553446,68.7345553410789,
69.2339655268132,69.7333757125475,70.2327858982817,70.732196084016,71.2316062697503,
71.7310164554845,72.2304266412188,72.7298368269531,73.2292470126874,73.7286571984216,
74.2280673841559,74.7274775698902,75.2268877556245,75.7262979413587,76.225708127093,
76.7251183128273,77.2245284985616,77.7239386842958,78.2233488700301,78.7227590557644,
79.2221692414986,79.7215794272329,80.2209896129672,80.7203997987015,81.2198099844358,
81.71922017017,82.2186303559043,82.7180405416386,83.2174507273728,83.7168609131071,
84.2162710988414,84.7156812845757,85.2150914703099,85.7145016560442,86.2139118417785,
86.7133220275128,87.212732213247,87.7121423989813,88.2115525847156,88.7109627704499,
89.2103729561841,89.7097831419184,90.2091933276527,90.7086035133869,91.2080136991212,
91.7074238848555,92.2068340705898,92.7062442563241,93.2056544420583,93.7050646277926,
94.2044748135269,94.7038849992611,95.2032951849954,95.7027053707297,96.202115556464,
96.7015257421982,97.2009359279325,97.7003461136668,98.1997562994011,98.6991664851353,
99.1985766708696,99.6979868566039,100.197397042338,100.696807228072,101.196217413807,
101.695627599541,102.195037785275,102.69444797101,103.193858156744,103.693268342478,
104.192678528212,104.692088713947,105.191498899681,105.690909085415,106.190319271149,
106.689729456884,107.189139642618,107.688549828352,108.187960014087,108.687370199821,
109.186780385555,109.686190571289,110.185600757024,110.685010942758,111.184421128492,
111.683831314226,112.183241499961,112.682651685695,113.182061871429,113.681472057164,
114.180882242898,114.680292428632,115.179702614366,115.679112800101,116.178522985835,
116.677933171569,117.177343357303,117.676753543038,118.176163728772,118.675573914506,
119.174984100241,119.674394285975,120.173804471709,120.673214657443,121.172624843178,
121.672035028912,122.171445214646,122.67085540038,123.170265586115,123.669675771849,
124.169085957583,124.668496143318,125.167906329052,125.667316514786,126.16672670052,
126.666136886255,127.165547071989,127.664957257723,128.164367443458,128.663777629192,
129.163187814926,129.66259800066,130.162008186395,130.661418372129,131.160828557863,
131.660238743597,132.159648929332,132.659059115066,133.1584693008,133.657879486535,
134.157289672269,134.656699858003,135.156110043737,135.655520229472,136.154930415206,
136.65434060094,137.153750786674,137.653160972409,138.152571158143,138.651981343877,
139.151391529612,139.650801715346,140.15021190108,140.649622086814,141.149032272549,
141.648442458283,142.147852644017,142.647262829751,143.146673015486,143.64608320122,
144.145493386954,144.644903572689,145.144313758423,145.643723944157,146.143134129891,
146.642544315626,147.14195450136,147.641364687094,148.140774872828,148.640185058563,
149.139595244297,149.639005430031,150.138415615766,150.6378258015,151.137235987234,
151.636646172968,152.136056358703),.UNSPECIFIED.);
#169=B_SPLINE_SURFACE_WITH_KNOTS('',3,3,((#67742,#67743,#67744,#67745,#67746,
#67747,#67748,#67749,#67750,#67751,#67752,#67753,#67754,#67755,#67756,#67757,
#67758,#67759,#67760,#67761,#67762,#67763,#67764,#67765,#67766,#67767,#67768,
#67769,#67770,#67771,#67772,#67773,#67774,#67775,#67776,#67777,#67778,#67779,
#67780,#67781,#67782,#67783,#67784,#67785,#67786,#67787,#67788,#67789,#67790,
#67791,#67792,#67793,#67794,#67795,#67796,#67797,#67798,#67799,#67800,#67801,
#67802,#67803,#67804,#67805,#67806,#67807,#67808,#67809,#67810,#67811,#67812,
#67813,#67814,#67815,#67816,#67817,#67818,#67819,#67820,#67821,#67822,#67823,
#67824,#67825,#67826,#67827,#67828,#67829,#67830,#67831,#67832,#67833,#67834,
#67835,#67836,#67837,#67838,#67839,#67840,#67841,#67842,#67843,#67844,#67845,
#67846,#67847,#67848,#67849,#67850,#67851,#67852,#67853,#67854,#67855,#67856,
#67857,#67858,#67859,#67860,#67861,#67862,#67863,#67864,#67865,#67866,#67867,
#67868,#67869,#67870,#67871,#67872,#67873,#67874,#67875,#67876,#67877,#67878,
#67879,#67880,#67881,#67882,#67883,#67884,#67885,#67886,#67887,#67888,#67889,
#67890,#67891,#67892,#67893,#67894,#67895,#67896,#67897,#67898,#67899,#67900,
#67901,#67902,#67903,#67904,#67905,#67906,#67907,#67908,#67909,#67910,#67911,
#67912,#67913,#67914,#67915,#67916,#67917,#67918,#67919,#67920,#67921,#67922,
#67923,#67924,#67925,#67926,#67927,#67928,#67929,#67930,#67931,#67932,#67933,
#67934,#67935,#67936,#67937,#67938,#67939,#67940,#67941,#67942,#67943,#67944,
#67945,#67946,#67947,#67948,#67949,#67950,#67951,#67952,#67953,#67954,#67955,
#67956,#67957,#67958,#67959,#67960,#67961,#67962,#67963,#67964,#67965,#67966,
#67967,#67968,#67969,#67970,#67971,#67972,#67973,#67974,#67975,#67976,#67977,
#67978,#67979,#67980,#67981,#67982,#67983,#67984,#67985,#67986,#67987,#67988,
#67989,#67990,#67991,#67992,#67993,#67994,#67995,#67996,#67997,#67998,#67999,
#68000,#68001,#68002,#68003,#68004,#68005,#68006,#68007,#68008,#68009,#68010,
#68011,#68012,#68013,#68014,#68015,#68016,#68017,#68018,#68019,#68020,#68021,
#68022,#68023,#68024,#68025,#68026,#68027,#68028,#68029,#68030,#68031,#68032),
(#68033,#68034,#68035,#68036,#68037,#68038,#68039,#68040,#68041,#68042,
#68043,#68044,#68045,#68046,#68047,#68048,#68049,#68050,#68051,#68052,#68053,
#68054,#68055,#68056,#68057,#68058,#68059,#68060,#68061,#68062,#68063,#68064,
#68065,#68066,#68067,#68068,#68069,#68070,#68071,#68072,#68073,#68074,#68075,
#68076,#68077,#68078,#68079,#68080,#68081,#68082,#68083,#68084,#68085,#68086,
#68087,#68088,#68089,#68090,#68091,#68092,#68093,#68094,#68095,#68096,#68097,
#68098,#68099,#68100,#68101,#68102,#68103,#68104,#68105,#68106,#68107,#68108,
#68109,#68110,#68111,#68112,#68113,#68114,#68115,#68116,#68117,#68118,#68119,
#68120,#68121,#68122,#68123,#68124,#68125,#68126,#68127,#68128,#68129,#68130,
#68131,#68132,#68133,#68134,#68135,#68136,#68137,#68138,#68139,#68140,#68141,
#68142,#68143,#68144,#68145,#68146,#68147,#68148,#68149,#68150,#68151,#68152,
#68153,#68154,#68155,#68156,#68157,#68158,#68159,#68160,#68161,#68162,#68163,
#68164,#68165,#68166,#68167,#68168,#68169,#68170,#68171,#68172,#68173,#68174,
#68175,#68176,#68177,#68178,#68179,#68180,#68181,#68182,#68183,#68184,#68185,
#68186,#68187,#68188,#68189,#68190,#68191,#68192,#68193,#68194,#68195,#68196,
#68197,#68198,#68199,#68200,#68201,#68202,#68203,#68204,#68205,#68206,#68207,
#68208,#68209,#68210,#68211,#68212,#68213,#68214,#68215,#68216,#68217,#68218,
#68219,#68220,#68221,#68222,#68223,#68224,#68225,#68226,#68227,#68228,#68229,
#68230,#68231,#68232,#68233,#68234,#68235,#68236,#68237,#68238,#68239,#68240,
#68241,#68242,#68243,#68244,#68245,#68246,#68247,#68248,#68249,#68250,#68251,
#68252,#68253,#68254,#68255,#68256,#68257,#68258,#68259,#68260,#68261,#68262,
#68263,#68264,#68265,#68266,#68267,#68268,#68269,#68270,#68271,#68272,#68273,
#68274,#68275,#68276,#68277,#68278,#68279,#68280,#68281,#68282,#68283,#68284,
#68285,#68286,#68287,#68288,#68289,#68290,#68291,#68292,#68293,#68294,#68295,
#68296,#68297,#68298,#68299,#68300,#68301,#68302,#68303,#68304,#68305,#68306,
#68307,#68308,#68309,#68310,#68311,#68312,#68313,#68314,#68315,#68316,#68317,
#68318,#68319,#68320,#68321,#68322,#68323),(#68324,#68325,#68326,#68327,
#68328,#68329,#68330,#68331,#68332,#68333,#68334,#68335,#68336,#68337,#68338,
#68339,#68340,#68341,#68342,#68343,#68344,#68345,#68346,#68347,#68348,#68349,
#68350,#68351,#68352,#68353,#68354,#68355,#68356,#68357,#68358,#68359,#68360,
#68361,#68362,#68363,#68364,#68365,#68366,#68367,#68368,#68369,#68370,#68371,
#68372,#68373,#68374,#68375,#68376,#68377,#68378,#68379,#68380,#68381,#68382,
#68383,#68384,#68385,#68386,#68387,#68388,#68389,#68390,#68391,#68392,#68393,
#68394,#68395,#68396,#68397,#68398,#68399,#68400,#68401,#68402,#68403,#68404,
#68405,#68406,#68407,#68408,#68409,#68410,#68411,#68412,#68413,#68414,#68415,
#68416,#68417,#68418,#68419,#68420,#68421,#68422,#68423,#68424,#68425,#68426,
#68427,#68428,#68429,#68430,#68431,#68432,#68433,#68434,#68435,#68436,#68437,
#68438,#68439,#68440,#68441,#68442,#68443,#68444,#68445,#68446,#68447,#68448,
#68449,#68450,#68451,#68452,#68453,#68454,#68455,#68456,#68457,#68458,#68459,
#68460,#68461,#68462,#68463,#68464,#68465,#68466,#68467,#68468,#68469,#68470,
#68471,#68472,#68473,#68474,#68475,#68476,#68477,#68478,#68479,#68480,#68481,
#68482,#68483,#68484,#68485,#68486,#68487,#68488,#68489,#68490,#68491,#68492,
#68493,#68494,#68495,#68496,#68497,#68498,#68499,#68500,#68501,#68502,#68503,
#68504,#68505,#68506,#68507,#68508,#68509,#68510,#68511,#68512,#68513,#68514,
#68515,#68516,#68517,#68518,#68519,#68520,#68521,#68522,#68523,#68524,#68525,
#68526,#68527,#68528,#68529,#68530,#68531,#68532,#68533,#68534,#68535,#68536,
#68537,#68538,#68539,#68540,#68541,#68542,#68543,#68544,#68545,#68546,#68547,
#68548,#68549,#68550,#68551,#68552,#68553,#68554,#68555,#68556,#68557,#68558,
#68559,#68560,#68561,#68562,#68563,#68564,#68565,#68566,#68567,#68568,#68569,
#68570,#68571,#68572,#68573,#68574,#68575,#68576,#68577,#68578,#68579,#68580,
#68581,#68582,#68583,#68584,#68585,#68586,#68587,#68588,#68589,#68590,#68591,
#68592,#68593,#68594,#68595,#68596,#68597,#68598,#68599,#68600,#68601,#68602,
#68603,#68604,#68605,#68606,#68607,#68608,#68609,#68610,#68611,#68612,#68613,
#68614),(#68615,#68616,#68617,#68618,#68619,#68620,#68621,#68622,#68623,
#68624,#68625,#68626,#68627,#68628,#68629,#68630,#68631,#68632,#68633,#68634,
#68635,#68636,#68637,#68638,#68639,#68640,#68641,#68642,#68643,#68644,#68645,
#68646,#68647,#68648,#68649,#68650,#68651,#68652,#68653,#68654,#68655,#68656,
#68657,#68658,#68659,#68660,#68661,#68662,#68663,#68664,#68665,#68666,#68667,
#68668,#68669,#68670,#68671,#68672,#68673,#68674,#68675,#68676,#68677,#68678,
#68679,#68680,#68681,#68682,#68683,#68684,#68685,#68686,#68687,#68688,#68689,
#68690,#68691,#68692,#68693,#68694,#68695,#68696,#68697,#68698,#68699,#68700,
#68701,#68702,#68703,#68704,#68705,#68706,#68707,#68708,#68709,#68710,#68711,
#68712,#68713,#68714,#68715,#68716,#68717,#68718,#68719,#68720,#68721,#68722,
#68723,#68724,#68725,#68726,#68727,#68728,#68729,#68730,#68731,#68732,#68733,
#68734,#68735,#68736,#68737,#68738,#68739,#68740,#68741,#68742,#68743,#68744,
#68745,#68746,#68747,#68748,#68749,#68750,#68751,#68752,#68753,#68754,#68755,
#68756,#68757,#68758,#68759,#68760,#68761,#68762,#68763,#68764,#68765,#68766,
#68767,#68768,#68769,#68770,#68771,#68772,#68773,#68774,#68775,#68776,#68777,
#68778,#68779,#68780,#68781,#68782,#68783,#68784,#68785,#68786,#68787,#68788,
#68789,#68790,#68791,#68792,#68793,#68794,#68795,#68796,#68797,#68798,#68799,
#68800,#68801,#68802,#68803,#68804,#68805,#68806,#68807,#68808,#68809,#68810,
#68811,#68812,#68813,#68814,#68815,#68816,#68817,#68818,#68819,#68820,#68821,
#68822,#68823,#68824,#68825,#68826,#68827,#68828,#68829,#68830,#68831,#68832,
#68833,#68834,#68835,#68836,#68837,#68838,#68839,#68840,#68841,#68842,#68843,
#68844,#68845,#68846,#68847,#68848,#68849,#68850,#68851,#68852,#68853,#68854,
#68855,#68856,#68857,#68858,#68859,#68860,#68861,#68862,#68863,#68864,#68865,
#68866,#68867,#68868,#68869,#68870,#68871,#68872,#68873,#68874,#68875,#68876,
#68877,#68878,#68879,#68880,#68881,#68882,#68883,#68884,#68885,#68886,#68887,
#68888,#68889,#68890,#68891,#68892,#68893,#68894,#68895,#68896,#68897,#68898,
#68899,#68900,#68901,#68902,#68903,#68904,#68905)),.UNSPECIFIED.,.F.,.F.,
 .F.,(4,4),(4,1,1,1,1,1,1,1,1,1,1,1,1,1,1,1,1,1,1,1,1,1,1,1,1,1,1,1,1,1,
1,1,1,1,1,1,1,1,1,1,1,1,1,1,1,1,1,1,1,1,1,1,1,1,1,1,1,1,1,1,1,1,1,1,1,1,
1,1,1,1,1,1,1,1,1,1,1,1,1,1,1,1,1,1,1,1,1,1,1,1,1,1,1,1,1,1,1,1,1,1,1,1,
1,1,1,1,1,1,1,1,1,1,1,1,1,1,1,1,1,1,1,1,1,1,1,1,1,1,1,1,1,1,1,1,1,1,1,1,
1,1,1,1,1,1,1,1,1,1,1,1,1,1,1,1,1,1,1,1,1,1,1,1,1,1,1,1,1,1,1,1,1,1,1,1,
1,1,1,1,1,1,1,1,1,1,1,1,1,1,1,1,1,1,1,1,1,1,1,1,1,1,1,1,1,1,1,1,1,1,1,1,
1,1,1,1,1,1,1,1,1,1,1,1,1,1,1,1,1,1,1,1,1,1,1,1,1,1,1,1,1,1,1,1,1,1,1,1,
1,1,1,1,1,1,1,1,1,1,1,1,1,1,1,1,1,1,1,1,1,1,1,1,1,1,1,1,1,1,1,1,1,1,1,1,
1,1,1,1,1,1,4),(0.,0.115296848757168),(11.6154215191107,12.1148317048449,
12.6142418905792,13.1136520763135,13.6130622620478,14.112472447782,14.6118826335163,
15.1112928192506,15.6107030049849,16.1101131907191,16.6095233764534,17.1089335621877,
17.608343747922,18.1077539336562,18.6071641193905,19.1065743051248,19.6059844908591,
20.1053946765933,20.6048048623276,21.1042150480619,21.6036252337962,22.1030354195304,
22.6024456052647,23.101855790999,23.6012659767333,24.1006761624675,24.6000863482018,
25.0994965339361,25.5989067196703,26.0983169054046,26.5977270911389,27.0971372768732,
27.5965474626074,28.0959576483417,28.595367834076,29.0947780198103,29.5941882055445,
30.0935983912788,30.5930085770131,31.0924187627474,31.5918289484816,32.0912391342159,
32.5906493199502,33.0900595056845,33.5894696914187,34.088879877153,34.5882900628873,
35.0877002486216,35.5871104343558,36.0865206200901,36.5859308058244,37.0853409915587,
37.5847511772929,38.0841613630272,38.5835715487615,39.0829817344957,39.58239192023,
40.0818021059643,40.5812122916986,41.0806224774328,41.5800326631671,42.0794428489014,
42.5788530346357,43.0782632203699,43.5776734061042,44.0770835918385,44.5764937775728,
45.075903963307,45.5753141490413,46.0747243347756,46.5741345205099,47.0735447062441,
47.5729548919784,48.0723650777127,48.571775263447,49.0711854491812,49.5705956349155,
50.0700058206498,50.5694160063841,51.0688261921183,51.5682363778526,52.0676465635869,
52.5670567493211,53.0664669350554,53.5658771207897,54.065287306524,54.5646974922582,
55.0641076779925,55.5635178637268,56.0629280494611,56.5623382351953,57.0617484209296,
57.5611586066639,58.0605687923982,58.5599789781324,59.0593891638667,59.558799349601,
60.0582095353353,60.5576197210695,61.0570299068038,61.5564400925381,62.0558502782724,
62.5552604640066,63.0546706497409,63.5540808354752,64.0534910212095,64.5529012069437,
65.052311392678,65.5517215784123,66.0511317641465,66.5505419498808,67.0499521356151,
67.5493623213494,68.0487725070836,68.5481826928179,69.0475928785522,69.5470030642865,
70.0464132500207,70.545823435755,71.0452336214893,71.5446438072236,72.0440539929578,
72.5434641786921,73.0428743644264,73.5422845501607,74.0416947358949,74.5411049216292,
75.0405151073635,75.5399252930978,76.039335478832,76.5387456645663,77.0381558503006,
77.5375660360349,78.0369762217691,78.5363864075034,79.0357965932377,79.5352067789719,
80.0346169647062,80.5340271504405,81.0334373361748,81.532847521909,82.0322577076433,
82.5316678933776,83.0310780791119,83.5304882648461,84.0298984505804,84.5293086363147,
85.028718822049,85.5281290077832,86.0275391935175,86.5269493792518,87.0263595649861,
87.5257697507203,88.0251799364546,88.5245901221889,89.0240003079231,89.5234104936574,
90.0228206793917,90.522230865126,91.0216410508603,91.5210512365945,92.0204614223288,
92.5198716080631,93.0192817937973,93.5186919795316,94.0181021652659,94.5175123510002,
95.0169225367344,95.5163327224687,96.015742908203,96.5151530939373,97.0145632796715,
97.5139734654058,98.0133836511401,98.5127938368744,99.0122040226086,99.5116142083429,
100.011024394077,100.510434579811,101.009844765546,101.50925495128,102.008665137014,
102.508075322749,103.007485508483,103.506895694217,104.006305879951,104.505716065686,
105.00512625142,105.504536437154,106.003946622888,106.503356808623,107.002766994357,
107.502177180091,108.001587365826,108.50099755156,109.000407737294,109.499817923028,
109.999228108763,110.498638294497,110.998048480231,111.497458665965,111.9968688517,
112.496279037434,112.995689223168,113.495099408903,113.994509594637,114.493919780371,
114.993329966105,115.49274015184,115.992150337574,116.491560523308,116.990970709043,
117.490380894777,117.989791080511,118.489201266245,118.98861145198,119.488021637714,
119.987431823448,120.486842009182,120.986252194917,121.485662380651,121.985072566385,
122.48448275212,122.983892937854,123.483303123588,123.982713309322,124.482123495057,
124.981533680791,125.480943866525,125.980354052259,126.479764237994,126.979174423728,
127.478584609462,127.977994795197,128.477404980931,128.976815166665,129.476225352399,
129.975635538134,130.475045723868,130.974455909602,131.473866095336,131.973276281071,
132.472686466805,132.972096652539,133.471506838274,133.970917024008,134.470327209742,
134.969737395476,135.469147581211,135.968557766945,136.467967952679,136.967378138413,
137.466788324148,137.966198509882,138.465608695616,138.965018881351,139.464429067085,
139.963839252819,140.463249438553,140.962659624288,141.462069810022,141.961479995756,
142.46089018149,142.960300367225,143.459710552959,143.959120738693,144.458530924428,
144.957941110162,145.457351295896,145.95676148163,146.456171667365,146.955581853099,
147.454992038833,147.954402224568,148.453812410302,148.953222596036,149.45263278177,
149.952042967505,150.451453153239,150.950863338973,151.450273524707,151.949683710442,
152.449093896176,152.94850408191,153.447914267645,153.947324453379,154.446734639113,
154.946144824847,155.445555010582),.UNSPECIFIED.);
#716=B_SPLINE_CURVE_WITH_KNOTS('',3,(#63548,#63549,#63550,#63551,#63552,
#63553,#63554,#63555,#63556,#63557,#63558,#63559,#63560,#63561,#63562,#63563),
 .UNSPECIFIED.,.F.,.F.,(4,3,3,3,3,4),(-4.09254174883827,-3.99528148587419,
-3.49587130013992,-2.99646111440564,-2.49705092867137,-2.06980418878615),
 .UNSPECIFIED.);
#717=B_SPLINE_CURVE_WITH_KNOTS('',3,(#63566,#63567,#63568,#63569,#63570,
#63571,#63572,#63573,#63574,#63575),.UNSPECIFIED.,.F.,.F.,(4,3,3,4),(0.,
0.499410185734265,0.998820371468536,1.11885509353751),.UNSPECIFIED.);
#718=B_SPLINE_CURVE_WITH_KNOTS('',3,(#63580,#63581,#63582,#63583,#63584,
#63585,#63586,#63587,#63588,#63589,#63590,#63591,#63592,#63593,#63594,#63595,
#63596,#63597,#63598,#63599,#63600,#63601,#63602,#63603,#63604,#63605,#63606,
#63607,#63608,#63609,#63610,#63611,#63612,#63613,#63614,#63615,#63616,#63617,
#63618,#63619),.UNSPECIFIED.,.F.,.F.,(4,3,3,3,3,3,3,3,3,3,3,3,3,4),(-10.3757270560179,
-9.98820371468548,-9.48879352895121,-8.98938334321694,-8.48997315748266,
-7.99056297174839,-7.49115278601411,-6.99174260027984,-6.49233241454556,
-5.99292222881129,-5.49351204307701,-4.99410185734274,-4.49469167160847,
-4.09254174883827),.UNSPECIFIED.);
#719=B_SPLINE_CURVE_WITH_KNOTS('',3,(#63620,#63621,#63622,#63623,#63624,
#63625,#63626,#63627,#63628,#63629,#63630,#63631,#63632,#63633,#63634,#63635,
#63636,#63637,#63638,#63639,#63640,#63641,#63642,#63643,#63644,#63645,#63646,
#63647,#63648,#63649,#63650,#63651,#63652,#63653,#63654,#63655,#63656,#63657,
#63658,#63659),.UNSPECIFIED.,.F.,.F.,(4,3,3,3,3,3,3,3,3,3,3,3,3,4),(1.11885509353751,
1.49823055720281,1.99764074293709,2.49705092867136,2.99646111440564,3.49587130013992,
3.99528148587419,4.49469167160847,4.99410185734275,5.49351204307702,5.9929222288113,
6.49233241454557,6.99174260027985,7.40204040071709),.UNSPECIFIED.);
#720=B_SPLINE_CURVE_WITH_KNOTS('',3,(#63664,#63665,#63666,#63667,#63668,
#63669,#63670,#63671,#63672,#63673,#63674,#63675,#63676,#63677,#63678,#63679,
#63680,#63681,#63682,#63683,#63684,#63685,#63686,#63687,#63688,#63689,#63690,
#63691,#63692,#63693,#63694,#63695,#63696,#63697,#63698,#63699,#63700,#63701,
#63702,#63703,#63704,#63705,#63706),.UNSPECIFIED.,.F.,.F.,(4,3,3,3,3,3,
3,3,3,3,3,3,3,3,4),(-16.6589123631974,-16.480536129231,-15.9811259434968,
-15.4817157577625,-14.9823055720282,-14.4828953862939,-13.9834852005597,
-13.4840750148254,-12.9846648290911,-12.4852546433568,-11.9858444576226,
-11.4864342718883,-10.987024086154,-10.4876139004198,-10.3757270560179),
 .UNSPECIFIED.);
#721=B_SPLINE_CURVE_WITH_KNOTS('',3,(#63707,#63708,#63709,#63710,#63711,
#63712,#63713,#63714,#63715,#63716,#63717,#63718,#63719,#63720,#63721,#63722,
#63723,#63724,#63725,#63726,#63727,#63728,#63729,#63730,#63731,#63732,#63733,
#63734,#63735,#63736,#63737,#63738,#63739,#63740,#63741,#63742,#63743,#63744,
#63745,#63746,#63747,#63748,#63749),.UNSPECIFIED.,.F.,.F.,(4,3,3,3,3,3,
3,3,3,3,3,3,3,3,4),(7.40204040071709,7.49115278601413,7.9905629717484,8.48997315748267,
8.98938334321695,9.48879352895122,9.98820371468549,10.4876139004198,10.987024086154,
11.4864342718883,11.9858444576226,12.4852546433569,12.9846648290911,13.4840750148254,
13.6852257078967),.UNSPECIFIED.);
#722=B_SPLINE_CURVE_WITH_KNOTS('',3,(#63754,#63755,#63756,#63757,#63758,
#63759,#63760,#63761,#63762,#63763,#63764,#63765,#63766,#63767,#63768,#63769,
#63770,#63771,#63772,#63773,#63774,#63775,#63776,#63777,#63778,#63779,#63780,
#63781,#63782,#63783,#63784,#63785,#63786,#63787,#63788,#63789,#63790,#63791,
#63792,#63793),.UNSPECIFIED.,.F.,.F.,(4,3,3,3,3,3,3,3,3,3,3,3,3,4),(-22.942097670377,
-22.4734583580423,-21.9740481723081,-21.4746379865738,-20.9752278008395,
-20.4758176151052,-19.976407429371,-19.4769972436367,-18.9775870579024,
-18.4781768721681,-17.9787666864339,-17.4793565006996,-16.9799463149653,
-16.6589123631974),.UNSPECIFIED.);
#723=B_SPLINE_CURVE_WITH_KNOTS('',3,(#63794,#63795,#63796,#63797,#63798,
#63799,#63800,#63801,#63802,#63803,#63804,#63805,#63806,#63807,#63808,#63809,
#63810,#63811,#63812,#63813,#63814,#63815,#63816,#63817,#63818,#63819,#63820,
#63821,#63822,#63823,#63824,#63825,#63826,#63827,#63828,#63829,#63830,#63831,
#63832,#63833),.UNSPECIFIED.,.F.,.F.,(4,3,3,3,3,3,3,3,3,3,3,3,3,4),(13.6852257078967,
13.9834852005597,14.482895386294,14.9823055720282,15.4817157577625,15.9811259434968,
16.480536129231,16.9799463149653,17.4793565006996,17.9787666864339,18.4781768721681,
18.9775870579024,19.4769972436367,19.9684110150763),.UNSPECIFIED.);
#724=B_SPLINE_CURVE_WITH_KNOTS('',3,(#63838,#63839,#63840,#63841,#63842,
#63843,#63844,#63845,#63846,#63847,#63848,#63849,#63850,#63851,#63852,#63853,
#63854,#63855,#63856,#63857,#63858,#63859,#63860,#63861,#63862,#63863,#63864,
#63865,#63866,#63867,#63868,#63869,#63870,#63871,#63872,#63873,#63874,#63875,
#63876,#63877,#63878,#63879,#63880),.UNSPECIFIED.,.F.,.F.,(4,3,3,3,3,3,
3,3,3,3,3,3,3,3,4),(-29.2252829775566,-28.9657907725879,-28.4663805868536,
-27.9669704011194,-27.4675602153851,-26.9681500296508,-26.4687398439165,
-25.9693296581823,-25.469919472448,-24.9705092867137,-24.4710991009794,
-23.9716889152452,-23.4722787295109,-22.9728685437766,-22.942097670377),
 .UNSPECIFIED.);
#725=B_SPLINE_CURVE_WITH_KNOTS('',3,(#63881,#63882,#63883,#63884,#63885,
#63886,#63887,#63888,#63889,#63890,#63891,#63892,#63893,#63894,#63895,#63896,
#63897,#63898,#63899,#63900,#63901,#63902,#63903,#63904,#63905,#63906,#63907,
#63908,#63909,#63910,#63911,#63912,#63913,#63914,#63915,#63916,#63917,#63918,
#63919,#63920,#63921,#63922,#63923),.UNSPECIFIED.,.F.,.F.,(4,3,3,3,3,3,
3,3,3,3,3,3,3,3,4),(19.9684110150763,19.9764074293709,20.4758176151052,
20.9752278008395,21.4746379865738,21.974048172308,22.4734583580423,22.9728685437766,
23.4722787295109,23.9716889152451,24.4710991009794,24.9705092867137,25.469919472448,
25.9693296581822,26.2515963222559),.UNSPECIFIED.);
#726=B_SPLINE_CURVE_WITH_KNOTS('',3,(#63928,#63929,#63930,#63931,#63932,
#63933,#63934,#63935,#63936,#63937,#63938,#63939,#63940,#63941,#63942,#63943,
#63944,#63945,#63946,#63947,#63948,#63949,#63950,#63951,#63952,#63953,#63954,
#63955,#63956,#63957,#63958,#63959,#63960,#63961,#63962,#63963,#63964,#63965,
#63966,#63967,#63968,#63969,#63970),.UNSPECIFIED.,.F.,.F.,(4,3,3,3,3,3,
3,3,3,3,3,3,3,3,4),(-35.5084682847362,-35.4581231871335,-34.9587130013992,
-34.4593028156649,-33.9598926299306,-33.4604824441964,-32.9610722584621,
-32.4616620727278,-31.9622518869935,-31.4628417012593,-30.963431515525,
-30.4640213297907,-29.9646111440564,-29.4652009583222,-29.2252829775566),
 .UNSPECIFIED.);
#727=B_SPLINE_CURVE_WITH_KNOTS('',3,(#63971,#63972,#63973,#63974,#63975,
#63976,#63977,#63978,#63979,#63980,#63981,#63982,#63983,#63984,#63985,#63986,
#63987,#63988,#63989,#63990,#63991,#63992,#63993,#63994,#63995,#63996,#63997,
#63998,#63999,#64000,#64001,#64002,#64003,#64004,#64005,#64006,#64007,#64008,
#64009,#64010,#64011,#64012,#64013),.UNSPECIFIED.,.F.,.F.,(4,3,3,3,3,3,
3,3,3,3,3,3,3,3,4),(26.2515963222559,26.4687398439165,26.9681500296508,
27.4675602153851,27.9669704011193,28.4663805868536,28.9657907725879,29.4652009583222,
29.9646111440564,30.4640213297907,30.963431515525,31.4628417012593,31.9622518869935,
32.4616620727278,32.5347816294354),.UNSPECIFIED.);
#728=B_SPLINE_CURVE_WITH_KNOTS('',3,(#64018,#64019,#64020,#64021,#64022,
#64023,#64024,#64025,#64026,#64027,#64028,#64029,#64030,#64031,#64032,#64033,
#64034,#64035,#64036,#64037,#64038,#64039,#64040,#64041,#64042,#64043,#64044,
#64045,#64046,#64047,#64048,#64049,#64050,#64051,#64052,#64053,#64054,#64055,
#64056,#64057),.UNSPECIFIED.,.F.,.F.,(4,3,3,3,3,3,3,3,3,3,3,3,3,4),(-41.7916535919158,
-41.4510454159447,-40.9516352302105,-40.4522250444762,-39.9528148587419,
-39.4534046730076,-38.9539944872734,-38.4545843015391,-37.9551741158048,
-37.4557639300706,-36.9563537443363,-36.456943558602,-35.9575333728677,
-35.5084682847362),.UNSPECIFIED.);
#729=B_SPLINE_CURVE_WITH_KNOTS('',3,(#64058,#64059,#64060,#64061,#64062,
#64063,#64064,#64065,#64066,#64067,#64068,#64069,#64070,#64071,#64072,#64073,
#64074,#64075,#64076,#64077,#64078,#64079,#64080,#64081,#64082,#64083,#64084,
#64085,#64086,#64087,#64088,#64089,#64090,#64091,#64092,#64093,#64094,#64095,
#64096,#64097),.UNSPECIFIED.,.F.,.F.,(4,3,3,3,3,3,3,3,3,3,3,3,3,4),(32.5347816294354,
32.9610722584621,33.4604824441964,33.9598926299306,34.4593028156649,34.9587130013992,
35.4581231871335,35.9575333728677,36.456943558602,36.9563537443363,37.4557639300705,
37.9551741158048,38.4545843015391,38.817966936615),.UNSPECIFIED.);
#730=B_SPLINE_CURVE_WITH_KNOTS('',3,(#64102,#64103,#64104,#64105,#64106,
#64107,#64108,#64109,#64110,#64111,#64112,#64113,#64114,#64115,#64116,#64117,
#64118,#64119,#64120,#64121,#64122,#64123,#64124,#64125,#64126,#64127,#64128,
#64129,#64130,#64131,#64132,#64133,#64134,#64135,#64136,#64137,#64138,#64139,
#64140,#64141,#64142,#64143,#64144),.UNSPECIFIED.,.F.,.F.,(4,3,3,3,3,3,
3,3,3,3,3,3,3,3,4),(-48.0748388990954,-47.9433778304903,-47.443967644756,
-46.9445574590218,-46.4451472732875,-45.9457370875532,-45.4463269018189,
-44.9469167160847,-44.4475065303504,-43.9480963446161,-43.4486861588818,
-42.9492759731476,-42.4498657874133,-41.950455601679,-41.7916535919158),
 .UNSPECIFIED.);
#731=B_SPLINE_CURVE_WITH_KNOTS('',3,(#64145,#64146,#64147,#64148,#64149,
#64150,#64151,#64152,#64153,#64154,#64155,#64156,#64157,#64158,#64159,#64160,
#64161,#64162,#64163,#64164,#64165,#64166,#64167,#64168,#64169,#64170,#64171,
#64172,#64173,#64174,#64175,#64176,#64177,#64178,#64179,#64180,#64181,#64182,
#64183,#64184,#64185,#64186,#64187),.UNSPECIFIED.,.F.,.F.,(4,3,3,3,3,3,
3,3,3,3,3,3,3,3,4),(38.817966936615,38.9539944872734,39.4534046730076,39.9528148587419,
40.4522250444762,40.9516352302105,41.4510454159447,41.950455601679,42.4498657874133,
42.9492759731476,43.4486861588818,43.9480963446161,44.4475065303504,44.9469167160847,
45.1011522437946),.UNSPECIFIED.);
#732=B_SPLINE_CURVE_WITH_KNOTS('',3,(#64192,#64193,#64194,#64195,#64196,
#64197,#64198,#64199,#64200,#64201,#64202,#64203,#64204,#64205,#64206,#64207,
#64208,#64209,#64210,#64211,#64212,#64213,#64214,#64215,#64216,#64217,#64218,
#64219,#64220,#64221,#64222,#64223,#64224,#64225,#64226,#64227,#64228,#64229,
#64230,#64231),.UNSPECIFIED.,.F.,.F.,(4,3,3,3,3,3,3,3,3,3,3,3,3,4),(-54.358024206275,
-53.9363000593016,-53.4368898735673,-52.937479687833,-52.4380695020988,
-51.9386593163645,-51.4392491306302,-50.939838944896,-50.4404287591617,
-49.9410185734274,-49.4416083876931,-48.9421982019589,-48.4427880162246,
-48.0748388990954),.UNSPECIFIED.);
#733=B_SPLINE_CURVE_WITH_KNOTS('',3,(#64232,#64233,#64234,#64235,#64236,
#64237,#64238,#64239,#64240,#64241,#64242,#64243,#64244,#64245,#64246,#64247,
#64248,#64249,#64250,#64251,#64252,#64253,#64254,#64255,#64256,#64257,#64258,
#64259,#64260,#64261,#64262,#64263,#64264,#64265,#64266,#64267,#64268,#64269,
#64270,#64271),.UNSPECIFIED.,.F.,.F.,(4,3,3,3,3,3,3,3,3,3,3,3,3,4),(45.1011522437946,
45.4463269018189,45.9457370875532,46.4451472732875,46.9445574590218,47.443967644756,
47.9433778304903,48.4427880162246,48.9421982019588,49.4416083876931,49.9410185734274,
50.4404287591617,50.9398389448959,51.3843375509742),.UNSPECIFIED.);
#734=B_SPLINE_CURVE_WITH_KNOTS('',3,(#64276,#64277,#64278,#64279,#64280,
#64281,#64282,#64283,#64284,#64285,#64286,#64287,#64288,#64289,#64290,#64291,
#64292,#64293,#64294,#64295,#64296,#64297,#64298,#64299,#64300,#64301,#64302,
#64303,#64304,#64305,#64306,#64307,#64308,#64309,#64310,#64311,#64312,#64313,
#64314,#64315,#64316,#64317,#64318),.UNSPECIFIED.,.F.,.F.,(4,3,3,3,3,3,
3,3,3,3,3,3,3,3,4),(-60.6412095134546,-60.4286324738472,-59.9292222881129,
-59.4298121023786,-58.9304019166443,-58.4309917309101,-57.9315815451758,
-57.4321713594415,-56.9327611737072,-56.433350987973,-55.9339408022387,
-55.4345306165044,-54.9351204307702,-54.4357102450359,-54.358024206275),
 .UNSPECIFIED.);
#735=B_SPLINE_CURVE_WITH_KNOTS('',3,(#64319,#64320,#64321,#64322,#64323,
#64324,#64325,#64326,#64327,#64328,#64329,#64330,#64331,#64332,#64333,#64334,
#64335,#64336,#64337,#64338,#64339,#64340,#64341,#64342,#64343,#64344,#64345,
#64346,#64347,#64348,#64349,#64350,#64351,#64352,#64353,#64354,#64355,#64356,
#64357,#64358,#64359,#64360,#64361),.UNSPECIFIED.,.F.,.F.,(4,3,3,3,3,3,
3,3,3,3,3,3,3,3,4),(51.3843375509742,51.4392491306302,51.9386593163645,
52.4380695020988,52.937479687833,53.4368898735673,53.9363000593016,54.4357102450359,
54.9351204307701,55.4345306165044,55.9339408022387,56.433350987973,56.9327611737072,
57.4321713594415,57.6675228581538),.UNSPECIFIED.);
#736=B_SPLINE_CURVE_WITH_KNOTS('',3,(#64366,#64367,#64368,#64369,#64370,
#64371,#64372,#64373,#64374,#64375,#64376,#64377,#64378,#64379,#64380,#64381,
#64382,#64383,#64384,#64385,#64386,#64387,#64388,#64389,#64390,#64391,#64392,
#64393,#64394,#64395,#64396,#64397,#64398,#64399,#64400,#64401,#64402,#64403,
#64404,#64405,#64406,#64407,#64408),.UNSPECIFIED.,.F.,.F.,(4,3,3,3,3,3,
3,3,3,3,3,3,3,3,4),(-66.9243948206342,-66.9209648883927,-66.4215547026584,
-65.9221445169242,-65.4227343311899,-64.9233241454556,-64.4239139597213,
-63.9245037739871,-63.4250935882528,-62.9256834025185,-62.4262732167843,
-61.92686303105,-61.4274528453157,-60.9280426595814,-60.6412095134546),
 .UNSPECIFIED.);
#737=B_SPLINE_CURVE_WITH_KNOTS('',3,(#64409,#64410,#64411,#64412,#64413,
#64414,#64415,#64416,#64417,#64418,#64419,#64420,#64421,#64422,#64423,#64424,
#64425,#64426,#64427,#64428,#64429,#64430,#64431,#64432,#64433,#64434,#64435,
#64436,#64437,#64438,#64439,#64440,#64441,#64442,#64443,#64444,#64445,#64446,
#64447,#64448,#64449,#64450,#64451),.UNSPECIFIED.,.F.,.F.,(4,3,3,3,3,3,
3,3,3,3,3,3,3,3,4),(57.6675228581538,57.9315815451758,58.4309917309101,
58.9304019166443,59.4298121023786,59.9292222881129,60.4286324738472,60.9280426595814,
61.4274528453157,61.92686303105,62.4262732167843,62.9256834025185,63.4250935882528,
63.9245037739871,63.9507081653334),.UNSPECIFIED.);
#738=B_SPLINE_CURVE_WITH_KNOTS('',3,(#64456,#64457,#64458,#64459,#64460,
#64461,#64462,#64463,#64464,#64465,#64466,#64467,#64468,#64469,#64470,#64471,
#64472,#64473,#64474,#64475,#64476,#64477,#64478,#64479,#64480,#64481,#64482,
#64483,#64484,#64485,#64486,#64487,#64488,#64489,#64490,#64491,#64492,#64493,
#64494,#64495),.UNSPECIFIED.,.F.,.F.,(4,3,3,3,3,3,3,3,3,3,3,3,3,4),(-73.2075801278138,
-72.913887117204,-72.4144769314697,-71.9150667457355,-71.4156565600012,
-70.9162463742669,-70.4168361885326,-69.9174260027984,-69.4180158170641,
-68.9186056313298,-68.4191954455955,-67.9197852598613,-67.420375074127,
-66.9243948206342),.UNSPECIFIED.);
#739=B_SPLINE_CURVE_WITH_KNOTS('',3,(#64496,#64497,#64498,#64499,#64500,
#64501,#64502,#64503,#64504,#64505,#64506,#64507,#64508,#64509,#64510,#64511,
#64512,#64513,#64514,#64515,#64516,#64517,#64518,#64519,#64520,#64521,#64522,
#64523,#64524,#64525,#64526,#64527,#64528,#64529,#64530,#64531,#64532,#64533,
#64534,#64535),.UNSPECIFIED.,.F.,.F.,(4,3,3,3,3,3,3,3,3,3,3,3,3,4),(63.9507081653334,
64.4239139597213,64.9233241454556,65.4227343311899,65.9221445169242,66.4215547026584,
66.9209648883927,67.420375074127,67.9197852598613,68.4191954455955,68.9186056313298,
69.4180158170641,69.9174260027984,70.233893472513),.UNSPECIFIED.);
#740=B_SPLINE_CURVE_WITH_KNOTS('',3,(#64540,#64541,#64542,#64543,#64544,
#64545,#64546,#64547,#64548,#64549,#64550,#64551,#64552,#64553,#64554,#64555,
#64556,#64557,#64558,#64559,#64560,#64561,#64562,#64563,#64564,#64565,#64566,
#64567,#64568,#64569,#64570,#64571,#64572,#64573,#64574,#64575,#64576,#64577,
#64578,#64579,#64580,#64581,#64582),.UNSPECIFIED.,.F.,.F.,(4,3,3,3,3,3,
3,3,3,3,3,3,3,3,4),(-79.4907654349934,-79.4062195317496,-78.9068093460153,
-78.407399160281,-77.9079889745468,-77.4085787888125,-76.9091686030782,
-76.4097584173439,-75.9103482316097,-75.4109380458754,-74.9115278601411,
-74.4121176744069,-73.9127074886726,-73.4132973029383,-73.2075801278138),
 .UNSPECIFIED.);
#741=B_SPLINE_CURVE_WITH_KNOTS('',3,(#64583,#64584,#64585,#64586,#64587,
#64588,#64589,#64590,#64591,#64592,#64593,#64594,#64595,#64596,#64597,#64598,
#64599,#64600,#64601,#64602,#64603,#64604,#64605,#64606,#64607,#64608,#64609,
#64610,#64611,#64612,#64613,#64614,#64615,#64616,#64617,#64618,#64619,#64620,
#64621,#64622,#64623,#64624,#64625),.UNSPECIFIED.,.F.,.F.,(4,3,3,3,3,3,
3,3,3,3,3,3,3,3,4),(70.233893472513,70.4168361885326,70.9162463742669,71.4156565600012,
71.9150667457354,72.4144769314697,72.913887117204,73.4132973029382,73.9127074886725,
74.4121176744068,74.9115278601411,75.4109380458754,75.9103482316096,76.4097584173439,
76.5170787796926),.UNSPECIFIED.);
#742=B_SPLINE_CURVE_WITH_KNOTS('',3,(#64630,#64631,#64632,#64633,#64634,
#64635,#64636,#64637,#64638,#64639,#64640,#64641,#64642,#64643,#64644,#64645,
#64646,#64647,#64648,#64649,#64650,#64651,#64652,#64653,#64654,#64655,#64656,
#64657,#64658,#64659,#64660,#64661,#64662,#64663,#64664,#64665,#64666,#64667,
#64668,#64669),.UNSPECIFIED.,.F.,.F.,(4,3,3,3,3,3,3,3,3,3,3,3,3,4),(-85.773950742173,
-85.3991417605609,-84.8997315748266,-84.4003213890923,-83.900911203358,
-83.4015010176238,-82.9020908318895,-82.4026806461552,-81.9032704604209,
-81.4038602746867,-80.9044500889524,-80.4050399032181,-79.9056297174838,
-79.4907654349934),.UNSPECIFIED.);
#743=B_SPLINE_CURVE_WITH_KNOTS('',3,(#64670,#64671,#64672,#64673,#64674,
#64675,#64676,#64677,#64678,#64679,#64680,#64681,#64682,#64683,#64684,#64685,
#64686,#64687,#64688,#64689,#64690,#64691,#64692,#64693,#64694,#64695,#64696,
#64697,#64698,#64699,#64700,#64701,#64702,#64703,#64704,#64705,#64706,#64707,
#64708,#64709),.UNSPECIFIED.,.F.,.F.,(4,3,3,3,3,3,3,3,3,3,3,3,3,4),(76.5170787796926,
76.9091686030782,77.4085787888124,77.9079889745467,78.407399160281,78.9068093460153,
79.4062195317496,79.9056297174838,80.4050399032181,80.9044500889524,81.4038602746867,
81.9032704604209,82.4026806461552,82.8002640868722),.UNSPECIFIED.);
#744=B_SPLINE_CURVE_WITH_KNOTS('',3,(#64714,#64715,#64716,#64717,#64718,
#64719,#64720,#64721,#64722,#64723,#64724,#64725,#64726,#64727,#64728,#64729,
#64730,#64731,#64732,#64733,#64734,#64735,#64736,#64737,#64738,#64739,#64740,
#64741,#64742,#64743,#64744,#64745,#64746,#64747,#64748,#64749,#64750,#64751,
#64752,#64753,#64754,#64755,#64756),.UNSPECIFIED.,.F.,.F.,(4,3,3,3,3,3,
3,3,3,3,3,3,3,3,4),(-92.0571360493526,-91.8914741751064,-91.3920639893721,
-90.8926538036379,-90.3932436179036,-89.8938334321693,-89.3944232464351,
-88.8950130607008,-88.3956028749665,-87.8961926892322,-87.396782503498,
-86.8973723177637,-86.3979621320294,-85.8985519462951,-85.773950742173),
 .UNSPECIFIED.);
#745=B_SPLINE_CURVE_WITH_KNOTS('',3,(#64757,#64758,#64759,#64760,#64761,
#64762,#64763,#64764,#64765,#64766,#64767,#64768,#64769,#64770,#64771,#64772,
#64773,#64774,#64775,#64776,#64777,#64778,#64779,#64780,#64781,#64782,#64783,
#64784,#64785,#64786,#64787,#64788,#64789,#64790,#64791,#64792,#64793,#64794,
#64795,#64796,#64797,#64798,#64799),.UNSPECIFIED.,.F.,.F.,(4,3,3,3,3,3,
3,3,3,3,3,3,3,3,4),(82.8002640868722,82.9020908318895,83.4015010176238,
83.900911203358,84.4003213890923,84.8997315748266,85.3991417605608,85.8985519462951,
86.3979621320294,86.8973723177637,87.3967825034979,87.8961926892322,88.3956028749665,
88.8950130607008,89.0834493940518),.UNSPECIFIED.);
#746=B_SPLINE_CURVE_WITH_KNOTS('',3,(#64804,#64805,#64806,#64807,#64808,
#64809,#64810,#64811,#64812,#64813,#64814,#64815,#64816,#64817,#64818,#64819,
#64820,#64821,#64822,#64823,#64824,#64825,#64826,#64827,#64828,#64829,#64830,
#64831,#64832,#64833,#64834,#64835,#64836,#64837,#64838,#64839,#64840,#64841,
#64842,#64843),.UNSPECIFIED.,.F.,.F.,(4,3,3,3,3,3,3,3,3,3,3,3,3,4),(-98.3403213565321,
-97.8843964039177,-97.3849862181834,-96.8855760324492,-96.3861658467149,
-95.8867556609806,-95.3873454752463,-94.8879352895121,-94.3885251037778,
-93.8891149180435,-93.3897047323093,-92.890294546575,-92.3908843608407,
-92.0571360493526),.UNSPECIFIED.);
#747=B_SPLINE_CURVE_WITH_KNOTS('',3,(#64844,#64845,#64846,#64847,#64848,
#64849,#64850,#64851,#64852,#64853,#64854,#64855,#64856,#64857,#64858,#64859,
#64860,#64861,#64862,#64863,#64864,#64865,#64866,#64867,#64868,#64869,#64870,
#64871,#64872,#64873,#64874,#64875,#64876,#64877,#64878,#64879,#64880,#64881,
#64882,#64883),.UNSPECIFIED.,.F.,.F.,(4,3,3,3,3,3,3,3,3,3,3,3,3,4),(89.0834493940518,
89.394423246435,89.8938334321693,90.3932436179036,90.8926538036378,91.3920639893721,
91.8914741751064,92.3908843608407,92.8902945465749,93.3897047323092,93.8891149180435,
94.3885251037778,94.887935289512,95.3666347012314),.UNSPECIFIED.);
#748=B_SPLINE_CURVE_WITH_KNOTS('',3,(#64888,#64889,#64890,#64891,#64892,
#64893,#64894,#64895,#64896,#64897,#64898,#64899,#64900,#64901,#64902,#64903,
#64904,#64905,#64906,#64907,#64908,#64909,#64910,#64911,#64912,#64913,#64914,
#64915,#64916,#64917,#64918,#64919,#64920,#64921,#64922,#64923,#64924,#64925,
#64926,#64927,#64928,#64929,#64930),.UNSPECIFIED.,.F.,.F.,(4,3,3,3,3,3,
3,3,3,3,3,3,3,3,4),(-104.623506663712,-104.376728818463,-103.877318632729,
-103.377908446995,-102.87849826126,-102.379088075526,-101.879677889792,
-101.380267704058,-100.880857518323,-100.381447332589,-99.8820371468548,
-99.3826269611206,-98.8832167753863,-98.383806589652,-98.3403213565321),
 .UNSPECIFIED.);
#749=B_SPLINE_CURVE_WITH_KNOTS('',3,(#64931,#64932,#64933,#64934,#64935,
#64936,#64937,#64938,#64939,#64940,#64941,#64942,#64943,#64944,#64945,#64946,
#64947,#64948,#64949,#64950,#64951,#64952,#64953,#64954,#64955,#64956,#64957,
#64958,#64959,#64960,#64961,#64962,#64963,#64964,#64965,#64966,#64967,#64968,
#64969,#64970,#64971,#64972,#64973),.UNSPECIFIED.,.F.,.F.,(4,3,3,3,3,3,
3,3,3,3,3,3,3,3,4),(95.3666347012314,95.3873454752463,95.8867556609806,
96.3861658467149,96.8855760324491,97.3849862181834,97.8843964039177,98.383806589652,
98.8832167753862,99.3826269611205,99.8820371468548,100.381447332589,100.880857518323,
101.380267704058,101.649820008411),.UNSPECIFIED.);
#750=B_SPLINE_CURVE_WITH_KNOTS('',3,(#64978,#64979,#64980,#64981,#64982,
#64983,#64984,#64985,#64986,#64987,#64988,#64989,#64990,#64991,#64992,#64993,
#64994,#64995,#64996,#64997,#64998,#64999,#65000,#65001,#65002,#65003,#65004,
#65005,#65006,#65007,#65008,#65009,#65010,#65011,#65012,#65013,#65014,#65015,
#65016,#65017,#65018,#65019,#65020),.UNSPECIFIED.,.F.,.F.,(4,3,3,3,3,3,
3,3,3,3,3,3,3,3,4),(-110.906691970891,-110.869061233009,-110.369651047275,
-109.87024086154,-109.370830675806,-108.871420490072,-108.372010304337,
-107.872600118603,-107.373189932869,-106.873779747135,-106.3743695614,-105.874959375666,
-105.375549189932,-104.876139004198,-104.623506663712),.UNSPECIFIED.);
#751=B_SPLINE_CURVE_WITH_KNOTS('',3,(#65021,#65022,#65023,#65024,#65025,
#65026,#65027,#65028,#65029,#65030,#65031,#65032,#65033,#65034,#65035,#65036,
#65037,#65038,#65039,#65040,#65041,#65042,#65043,#65044,#65045,#65046,#65047,
#65048,#65049,#65050,#65051,#65052,#65053,#65054,#65055,#65056,#65057,#65058,
#65059,#65060,#65061,#65062,#65063),.UNSPECIFIED.,.F.,.F.,(4,3,3,3,3,3,
3,3,3,3,3,3,3,3,4),(101.649820008411,101.879677889792,102.379088075526,
102.87849826126,103.377908446995,103.877318632729,104.376728818463,104.876139004198,
105.375549189932,105.874959375666,106.3743695614,106.873779747135,107.373189932869,
107.872600118603,107.933005315591),.UNSPECIFIED.);
#752=B_SPLINE_CURVE_WITH_KNOTS('',3,(#65068,#65069,#65070,#65071,#65072,
#65073,#65074,#65075,#65076,#65077,#65078,#65079,#65080,#65081,#65082,#65083,
#65084,#65085,#65086,#65087,#65088,#65089,#65090,#65091,#65092,#65093,#65094,
#65095,#65096,#65097,#65098,#65099,#65100,#65101,#65102,#65103,#65104,#65105,
#65106,#65107),.UNSPECIFIED.,.F.,.F.,(4,3,3,3,3,3,3,3,3,3,3,3,3,4),(-117.189877278071,
-116.86198346182,-116.362573276086,-115.863163090352,-115.363752904617,
-114.864342718883,-114.364932533149,-113.865522347414,-113.36611216168,
-112.866701975946,-112.367291790212,-111.867881604477,-111.368471418743,
-110.906691970891),.UNSPECIFIED.);
#753=B_SPLINE_CURVE_WITH_KNOTS('',3,(#65108,#65109,#65110,#65111,#65112,
#65113,#65114,#65115,#65116,#65117,#65118,#65119,#65120,#65121,#65122,#65123,
#65124,#65125,#65126,#65127,#65128,#65129,#65130,#65131,#65132,#65133,#65134,
#65135,#65136,#65137,#65138,#65139,#65140,#65141,#65142,#65143,#65144,#65145,
#65146,#65147),.UNSPECIFIED.,.F.,.F.,(4,3,3,3,3,3,3,3,3,3,3,3,3,4),(107.933005315591,
108.372010304337,108.871420490072,109.370830675806,109.87024086154,110.369651047275,
110.869061233009,111.368471418743,111.867881604477,112.367291790212,112.866701975946,
113.36611216168,113.865522347414,114.21619062277),.UNSPECIFIED.);
#754=B_SPLINE_CURVE_WITH_KNOTS('',3,(#65152,#65153,#65154,#65155,#65156,
#65157,#65158,#65159,#65160,#65161,#65162,#65163,#65164,#65165,#65166,#65167,
#65168,#65169,#65170,#65171,#65172,#65173,#65174,#65175,#65176,#65177,#65178,
#65179,#65180,#65181,#65182,#65183,#65184,#65185,#65186,#65187,#65188,#65189,
#65190,#65191,#65192,#65193,#65194),.UNSPECIFIED.,.F.,.F.,(4,3,3,3,3,3,
3,3,3,3,3,3,3,3,4),(-123.473062585251,-123.354315876366,-122.854905690631,
-122.355495504897,-121.856085319163,-121.356675133429,-120.857264947694,
-120.35785476196,-119.858444576226,-119.359034390492,-118.859624204757,
-118.360214019023,-117.860803833289,-117.361393647554,-117.189877278071),
 .UNSPECIFIED.);
#755=B_SPLINE_CURVE_WITH_KNOTS('',3,(#65195,#65196,#65197,#65198,#65199,
#65200,#65201,#65202,#65203,#65204,#65205,#65206,#65207,#65208,#65209,#65210,
#65211,#65212,#65213,#65214,#65215,#65216,#65217,#65218,#65219,#65220,#65221,
#65222,#65223,#65224,#65225,#65226,#65227,#65228,#65229,#65230,#65231,#65232,
#65233,#65234,#65235,#65236,#65237),.UNSPECIFIED.,.F.,.F.,(4,3,3,3,3,3,
3,3,3,3,3,3,3,3,4),(114.21619062277,114.364932533149,114.864342718883,115.363752904617,
115.863163090352,116.362573276086,116.86198346182,117.361393647554,117.860803833289,
118.360214019023,118.859624204757,119.359034390491,119.858444576226,120.35785476196,
120.49937592995),.UNSPECIFIED.);
#756=B_SPLINE_CURVE_WITH_KNOTS('',3,(#65242,#65243,#65244,#65245,#65246,
#65247,#65248,#65249,#65250,#65251,#65252,#65253,#65254,#65255,#65256,#65257,
#65258,#65259,#65260,#65261,#65262,#65263,#65264,#65265,#65266,#65267,#65268,
#65269,#65270,#65271,#65272,#65273,#65274,#65275,#65276,#65277,#65278,#65279,
#65280,#65281),.UNSPECIFIED.,.F.,.F.,(4,3,3,3,3,3,3,3,3,3,3,3,3,4),(-129.75624789243,
-129.347238105177,-128.847827919443,-128.348417733708,-127.849007547974,
-127.34959736224,-126.850187176506,-126.350776990771,-125.851366805037,
-125.351956619303,-124.852546433569,-124.353136247834,-123.8537260621,-123.473062585251),
 .UNSPECIFIED.);
#757=B_SPLINE_CURVE_WITH_KNOTS('',3,(#65282,#65283,#65284,#65285,#65286,
#65287,#65288,#65289,#65290,#65291,#65292,#65293,#65294,#65295,#65296,#65297,
#65298,#65299,#65300,#65301,#65302,#65303,#65304,#65305,#65306,#65307,#65308,
#65309,#65310,#65311,#65312,#65313,#65314,#65315,#65316,#65317,#65318,#65319,
#65320,#65321),.UNSPECIFIED.,.F.,.F.,(4,3,3,3,3,3,3,3,3,3,3,3,3,4),(120.49937592995,
120.857264947694,121.356675133429,121.856085319163,122.355495504897,122.854905690631,
123.354315876366,123.8537260621,124.353136247834,124.852546433568,125.351956619303,
125.851366805037,126.350776990771,126.782561237129),.UNSPECIFIED.);
#758=B_SPLINE_CURVE_WITH_KNOTS('',3,(#65326,#65327,#65328,#65329,#65330,
#65331,#65332,#65333,#65334,#65335,#65336,#65337,#65338,#65339,#65340,#65341,
#65342,#65343,#65344,#65345,#65346,#65347,#65348,#65349,#65350,#65351,#65352,
#65353,#65354,#65355,#65356,#65357,#65358,#65359,#65360,#65361,#65362,#65363,
#65364,#65365,#65366,#65367,#65368),.UNSPECIFIED.,.F.,.F.,(4,3,3,3,3,3,
3,3,3,3,3,3,3,3,4),(-136.03943319961,-135.839570519723,-135.340160333988,
-134.840750148254,-134.34133996252,-133.841929776785,-133.342519591051,
-132.843109405317,-132.343699219583,-131.844289033848,-131.344878848114,
-130.84546866238,-130.346058476646,-129.846648290911,-129.75624789243),
 .UNSPECIFIED.);
#759=B_SPLINE_CURVE_WITH_KNOTS('',3,(#65369,#65370,#65371,#65372,#65373,
#65374,#65375,#65376,#65377,#65378,#65379,#65380,#65381,#65382,#65383,#65384,
#65385,#65386,#65387,#65388,#65389,#65390,#65391,#65392,#65393,#65394,#65395,
#65396,#65397,#65398,#65399,#65400,#65401,#65402,#65403,#65404,#65405,#65406,
#65407,#65408,#65409,#65410,#65411),.UNSPECIFIED.,.F.,.F.,(4,3,3,3,3,3,
3,3,3,3,3,3,3,3,4),(126.782561237129,126.850187176506,127.34959736224,127.849007547974,
128.348417733708,128.847827919443,129.347238105177,129.846648290911,130.346058476646,
130.84546866238,131.344878848114,131.844289033848,132.343699219583,132.843109405317,
133.065746544309),.UNSPECIFIED.);
#760=B_SPLINE_CURVE_WITH_KNOTS('',3,(#65416,#65417,#65418,#65419,#65420,
#65421,#65422,#65423,#65424,#65425,#65426,#65427,#65428,#65429,#65430,#65431,
#65432,#65433,#65434,#65435,#65436,#65437,#65438,#65439,#65440,#65441,#65442,
#65443,#65444,#65445,#65446,#65447,#65448,#65449,#65450,#65451,#65452,#65453,
#65454,#65455),.UNSPECIFIED.,.F.,.F.,(4,3,3,3,3,3,3,3,3,3,3,3,3,4),(-142.322618506789,
-141.832492748534,-141.3330825628,-140.833672377065,-140.334262191331,-139.834852005597,
-139.335441819862,-138.836031634128,-138.336621448394,-137.83721126266,
-137.337801076925,-136.838390891191,-136.338980705457,-136.03943319961),
 .UNSPECIFIED.);
#761=B_SPLINE_CURVE_WITH_KNOTS('',3,(#65456,#65457,#65458,#65459,#65460,
#65461,#65462,#65463,#65464,#65465,#65466,#65467,#65468,#65469,#65470,#65471,
#65472,#65473,#65474,#65475,#65476,#65477,#65478,#65479,#65480,#65481,#65482,
#65483,#65484,#65485,#65486,#65487,#65488,#65489,#65490,#65491,#65492,#65493,
#65494,#65495,#65496,#65497,#65498),.UNSPECIFIED.,.F.,.F.,(4,3,3,3,3,3,
3,3,3,3,3,3,3,3,4),(133.065746544309,133.342519591051,133.841929776785,
134.34133996252,134.840750148254,135.340160333988,135.839570519723,136.338980705457,
136.838390891191,137.337801076925,137.83721126266,138.336621448394,138.836031634128,
139.335441819862,139.348931851488),.UNSPECIFIED.);
#762=B_SPLINE_CURVE_WITH_KNOTS('',3,(#65504,#65505,#65506,#65507,#65508,
#65509,#65510,#65511,#65512,#65513,#65514,#65515,#65516,#65517,#65518),
 .UNSPECIFIED.,.F.,.F.,(4,1,1,1,1,1,1,1,1,1,1,1,4),(147.65485471872,147.954402224568,
148.453812410302,148.953222596036,149.45263278177,149.952042967505,150.451453153239,
150.950863338973,151.450273524707,151.949683710442,152.449093896176,152.94850408191,
153.375750821795),.UNSPECIFIED.);
#763=B_SPLINE_CURVE_WITH_KNOTS('',3,(#65521,#65522,#65523,#65524,#65525,
#65526,#65527,#65528,#65529,#65530,#65531,#65532),.UNSPECIFIED.,.F.,.F.,
(4,1,1,1,1,1,1,1,1,4),(147.65485471872,148.140774872828,148.640185058563,
149.139595244297,149.639005430031,150.138415615766,150.6378258015,151.137235987234,
151.636646172968,152.136056358703),.UNSPECIFIED.);
#764=B_SPLINE_CURVE_WITH_KNOTS('',3,(#65537,#65538,#65539,#65540,#65541,
#65542,#65543,#65544,#65545,#65546,#65547,#65548,#65549,#65550,#65551,#65552,
#65553),.UNSPECIFIED.,.F.,.F.,(4,1,1,1,1,1,1,1,1,1,1,1,1,1,4),(141.371669411541,
141.462069810022,141.961479995756,142.46089018149,142.960300367225,143.459710552959,
143.959120738693,144.458530924428,144.957941110162,145.457351295896,145.95676148163,
146.456171667365,146.955581853099,147.454992038833,147.65485471872),
 .UNSPECIFIED.);
#765=B_SPLINE_CURVE_WITH_KNOTS('',3,(#65554,#65555,#65556,#65557,#65558,
#65559,#65560,#65561,#65562,#65563,#65564,#65565,#65566,#65567,#65568,#65569,
#65570),.UNSPECIFIED.,.F.,.F.,(4,1,1,1,1,1,1,1,1,1,1,1,1,1,4),(141.371669411541,
141.648442458283,142.147852644017,142.647262829751,143.146673015486,143.64608320122,
144.145493386954,144.644903572689,145.144313758423,145.643723944157,146.143134129891,
146.642544315626,147.14195450136,147.641364687094,147.65485471872),
 .UNSPECIFIED.);
#766=B_SPLINE_CURVE_WITH_KNOTS('',3,(#65575,#65576,#65577,#65578,#65579,
#65580,#65581,#65582,#65583,#65584,#65585,#65586,#65587,#65588,#65589,#65590),
 .UNSPECIFIED.,.F.,.F.,(4,1,1,1,1,1,1,1,1,1,1,1,1,4),(135.088484104361,
135.469147581211,135.968557766945,136.467967952679,136.967378138413,137.466788324148,
137.966198509882,138.465608695616,138.965018881351,139.464429067085,139.963839252819,
140.463249438553,140.962659624288,141.371669411541),.UNSPECIFIED.);
#767=B_SPLINE_CURVE_WITH_KNOTS('',3,(#65591,#65592,#65593,#65594,#65595,
#65596,#65597,#65598,#65599,#65600,#65601,#65602,#65603,#65604,#65605,#65606,
#65607),.UNSPECIFIED.,.F.,.F.,(4,1,1,1,1,1,1,1,1,1,1,1,1,1,4),(135.088484104361,
135.156110043737,135.655520229472,136.154930415206,136.65434060094,137.153750786674,
137.653160972409,138.152571158143,138.651981343877,139.151391529612,139.650801715346,
140.15021190108,140.649622086814,141.149032272549,141.371669411541),
 .UNSPECIFIED.);
#768=B_SPLINE_CURVE_WITH_KNOTS('',3,(#65612,#65613,#65614,#65615,#65616,
#65617,#65618,#65619,#65620,#65621,#65622,#65623,#65624,#65625,#65626,#65627,
#65628),.UNSPECIFIED.,.F.,.F.,(4,1,1,1,1,1,1,1,1,1,1,1,1,1,4),(128.805298797182,
128.976815166665,129.476225352399,129.975635538134,130.475045723868,130.974455909602,
131.473866095336,131.973276281071,132.472686466805,132.972096652539,133.471506838274,
133.970917024008,134.470327209742,134.969737395476,135.088484104361),
 .UNSPECIFIED.);
#769=B_SPLINE_CURVE_WITH_KNOTS('',3,(#65629,#65630,#65631,#65632,#65633,
#65634,#65635,#65636,#65637,#65638,#65639,#65640,#65641,#65642,#65643,#65644),
 .UNSPECIFIED.,.F.,.F.,(4,1,1,1,1,1,1,1,1,1,1,1,1,4),(128.805298797182,
129.163187814926,129.66259800066,130.162008186395,130.661418372129,131.160828557863,
131.660238743597,132.159648929332,132.659059115066,133.1584693008,133.657879486535,
134.157289672269,134.656699858003,135.088484104361),.UNSPECIFIED.);
#770=B_SPLINE_CURVE_WITH_KNOTS('',3,(#65649,#65650,#65651,#65652,#65653,
#65654,#65655,#65656,#65657,#65658,#65659,#65660,#65661,#65662,#65663,#65664),
 .UNSPECIFIED.,.F.,.F.,(4,1,1,1,1,1,1,1,1,1,1,1,1,4),(122.522113490002,
122.983892937854,123.483303123588,123.982713309322,124.482123495057,124.981533680791,
125.480943866525,125.980354052259,126.479764237994,126.979174423728,127.478584609462,
127.977994795197,128.477404980931,128.805298797182),.UNSPECIFIED.);
#771=B_SPLINE_CURVE_WITH_KNOTS('',3,(#65665,#65666,#65667,#65668,#65669,
#65670,#65671,#65672,#65673,#65674,#65675,#65676,#65677,#65678,#65679,#65680,
#65681),.UNSPECIFIED.,.F.,.F.,(4,1,1,1,1,1,1,1,1,1,1,1,1,1,4),(122.522113490002,
122.67085540038,123.170265586115,123.669675771849,124.169085957583,124.668496143318,
125.167906329052,125.667316514786,126.16672670052,126.666136886255,127.165547071989,
127.664957257723,128.164367443458,128.663777629192,128.805298797182),
 .UNSPECIFIED.);
#772=B_SPLINE_CURVE_WITH_KNOTS('',3,(#65686,#65687,#65688,#65689,#65690,
#65691,#65692,#65693,#65694,#65695,#65696,#65697,#65698,#65699,#65700,#65701,
#65702),.UNSPECIFIED.,.F.,.F.,(4,1,1,1,1,1,1,1,1,1,1,1,1,1,4),(116.238928182822,
116.491560523308,116.990970709043,117.490380894777,117.989791080511,118.489201266245,
118.98861145198,119.488021637714,119.987431823448,120.486842009182,120.986252194917,
121.485662380651,121.985072566385,122.48448275212,122.522113490002),
 .UNSPECIFIED.);
#773=B_SPLINE_CURVE_WITH_KNOTS('',3,(#65703,#65704,#65705,#65706,#65707,
#65708,#65709,#65710,#65711,#65712,#65713,#65714,#65715,#65716,#65717,#65718),
 .UNSPECIFIED.,.F.,.F.,(4,1,1,1,1,1,1,1,1,1,1,1,1,4),(116.238928182822,
116.677933171569,117.177343357303,117.676753543038,118.176163728772,118.675573914506,
119.174984100241,119.674394285975,120.173804471709,120.673214657443,121.172624843178,
121.672035028912,122.171445214646,122.522113490002),.UNSPECIFIED.);
#774=B_SPLINE_CURVE_WITH_KNOTS('',3,(#65723,#65724,#65725,#65726,#65727,
#65728,#65729,#65730,#65731,#65732,#65733,#65734,#65735,#65736,#65737,#65738,
#65739),.UNSPECIFIED.,.F.,.F.,(4,1,1,1,1,1,1,1,1,1,1,1,1,1,4),(109.955742875643,
109.999228108763,110.498638294497,110.998048480231,111.497458665965,111.9968688517,
112.496279037434,112.995689223168,113.495099408903,113.994509594637,114.493919780371,
114.993329966105,115.49274015184,115.992150337574,116.238928182822),
 .UNSPECIFIED.);
#775=B_SPLINE_CURVE_WITH_KNOTS('',3,(#65740,#65741,#65742,#65743,#65744,
#65745,#65746,#65747,#65748,#65749,#65750,#65751,#65752,#65753,#65754,#65755,
#65756),.UNSPECIFIED.,.F.,.F.,(4,1,1,1,1,1,1,1,1,1,1,1,1,1,4),(109.955742875643,
110.185600757024,110.685010942758,111.184421128492,111.683831314226,112.183241499961,
112.682651685695,113.182061871429,113.681472057164,114.180882242898,114.680292428632,
115.179702614366,115.679112800101,116.178522985835,116.238928182822),
 .UNSPECIFIED.);
#776=B_SPLINE_CURVE_WITH_KNOTS('',3,(#65761,#65762,#65763,#65764,#65765,
#65766,#65767,#65768,#65769,#65770,#65771,#65772,#65773,#65774,#65775,#65776),
 .UNSPECIFIED.,.F.,.F.,(4,1,1,1,1,1,1,1,1,1,1,1,1,4),(103.672557568463,
104.006305879951,104.505716065686,105.00512625142,105.504536437154,106.003946622888,
106.503356808623,107.002766994357,107.502177180091,108.001587365826,108.50099755156,
109.000407737294,109.499817923028,109.955742875643),.UNSPECIFIED.);
#777=B_SPLINE_CURVE_WITH_KNOTS('',3,(#65777,#65778,#65779,#65780,#65781,
#65782,#65783,#65784,#65785,#65786,#65787,#65788,#65789,#65790,#65791,#65792,
#65793),.UNSPECIFIED.,.F.,.F.,(4,1,1,1,1,1,1,1,1,1,1,1,1,1,4),(103.672557568463,
103.693268342478,104.192678528212,104.692088713947,105.191498899681,105.690909085415,
106.190319271149,106.689729456884,107.189139642618,107.688549828352,108.187960014087,
108.687370199821,109.186780385555,109.686190571289,109.955742875643),
 .UNSPECIFIED.);
#778=B_SPLINE_CURVE_WITH_KNOTS('',3,(#65798,#65799,#65800,#65801,#65802,
#65803,#65804,#65805,#65806,#65807,#65808,#65809,#65810,#65811,#65812,#65813,
#65814),.UNSPECIFIED.,.F.,.F.,(4,1,1,1,1,1,1,1,1,1,1,1,1,1,4),(97.3893722612836,
97.5139734654058,98.0133836511401,98.5127938368744,99.0122040226086,99.5116142083429,
100.011024394077,100.510434579811,101.009844765546,101.50925495128,102.008665137014,
102.508075322749,103.007485508483,103.506895694217,103.672557568463),
 .UNSPECIFIED.);
#779=B_SPLINE_CURVE_WITH_KNOTS('',3,(#65815,#65816,#65817,#65818,#65819,
#65820,#65821,#65822,#65823,#65824,#65825,#65826,#65827,#65828,#65829,#65830),
 .UNSPECIFIED.,.F.,.F.,(4,1,1,1,1,1,1,1,1,1,1,1,1,4),(97.3893722612836,
97.7003461136668,98.1997562994011,98.6991664851353,99.1985766708696,99.6979868566039,
100.197397042338,100.696807228072,101.196217413807,101.695627599541,102.195037785275,
102.69444797101,103.193858156744,103.672557568463),.UNSPECIFIED.);
#780=B_SPLINE_CURVE_WITH_KNOTS('',3,(#65835,#65836,#65837,#65838,#65839,
#65840,#65841,#65842,#65843,#65844,#65845,#65846,#65847,#65848,#65849,#65850),
 .UNSPECIFIED.,.F.,.F.,(4,1,1,1,1,1,1,1,1,1,1,1,1,4),(91.106186954104,91.5210512365945,
92.0204614223288,92.5198716080631,93.0192817937973,93.5186919795316,94.0181021652659,
94.5175123510002,95.0169225367344,95.5163327224687,96.015742908203,96.5151530939373,
97.0145632796715,97.3893722612836),.UNSPECIFIED.);
#781=B_SPLINE_CURVE_WITH_KNOTS('',3,(#65851,#65852,#65853,#65854,#65855,
#65856,#65857,#65858,#65859,#65860,#65861,#65862,#65863,#65864,#65865,#65866,
#65867),.UNSPECIFIED.,.F.,.F.,(4,1,1,1,1,1,1,1,1,1,1,1,1,1,4),(91.106186954104,
91.2080136991212,91.7074238848555,92.2068340705898,92.7062442563241,93.2056544420583,
93.7050646277926,94.2044748135269,94.7038849992611,95.2032951849954,95.7027053707297,
96.202115556464,96.7015257421982,97.2009359279325,97.3893722612836),
 .UNSPECIFIED.);
#782=B_SPLINE_CURVE_WITH_KNOTS('',3,(#65872,#65873,#65874,#65875,#65876,
#65877,#65878,#65879,#65880,#65881,#65882,#65883,#65884,#65885,#65886,#65887,
#65888),.UNSPECIFIED.,.F.,.F.,(4,1,1,1,1,1,1,1,1,1,1,1,1,1,4),(84.8230016469244,
85.028718822049,85.5281290077832,86.0275391935175,86.5269493792518,87.0263595649861,
87.5257697507203,88.0251799364546,88.5245901221889,89.0240003079231,89.5234104936574,
90.0228206793917,90.522230865126,91.0216410508603,91.106186954104),
 .UNSPECIFIED.);
#783=B_SPLINE_CURVE_WITH_KNOTS('',3,(#65889,#65890,#65891,#65892,#65893,
#65894,#65895,#65896,#65897,#65898,#65899,#65900,#65901,#65902,#65903,#65904),
 .UNSPECIFIED.,.F.,.F.,(4,1,1,1,1,1,1,1,1,1,1,1,1,4),(84.8230016469244,
85.2150914703099,85.7145016560442,86.2139118417785,86.7133220275128,87.212732213247,
87.7121423989813,88.2115525847156,88.7109627704499,89.2103729561841,89.7097831419184,
90.2091933276527,90.7086035133869,91.106186954104),.UNSPECIFIED.);
#784=B_SPLINE_CURVE_WITH_KNOTS('',3,(#65909,#65910,#65911,#65912,#65913,
#65914,#65915,#65916,#65917,#65918,#65919,#65920,#65921,#65922,#65923,#65924),
 .UNSPECIFIED.,.F.,.F.,(4,1,1,1,1,1,1,1,1,1,1,1,1,4),(78.5398163397448,
79.0357965932377,79.5352067789719,80.0346169647062,80.5340271504405,81.0334373361748,
81.532847521909,82.0322577076433,82.5316678933776,83.0310780791119,83.5304882648461,
84.0298984505804,84.5293086363147,84.8230016469244),.UNSPECIFIED.);
#785=B_SPLINE_CURVE_WITH_KNOTS('',3,(#65925,#65926,#65927,#65928,#65929,
#65930,#65931,#65932,#65933,#65934,#65935,#65936,#65937,#65938,#65939,#65940,
#65941),.UNSPECIFIED.,.F.,.F.,(4,1,1,1,1,1,1,1,1,1,1,1,1,1,4),(78.5398163397448,
78.7227590557644,79.2221692414986,79.7215794272329,80.2209896129672,80.7203997987015,
81.2198099844358,81.71922017017,82.2186303559043,82.7180405416386,83.2174507273728,
83.7168609131071,84.2162710988414,84.7156812845757,84.8230016469244),
 .UNSPECIFIED.);
#786=B_SPLINE_CURVE_WITH_KNOTS('',3,(#65946,#65947,#65948,#65949,#65950,
#65951,#65952,#65953,#65954,#65955,#65956,#65957,#65958,#65959,#65960,#65961,
#65962),.UNSPECIFIED.,.F.,.F.,(4,1,1,1,1,1,1,1,1,1,1,1,1,1,4),(72.2566310325653,
72.5434641786921,73.0428743644264,73.5422845501607,74.0416947358949,74.5411049216292,
75.0405151073635,75.5399252930978,76.039335478832,76.5387456645663,77.0381558503006,
77.5375660360349,78.0369762217691,78.5363864075034,78.5398163397448),
 .UNSPECIFIED.);
#787=B_SPLINE_CURVE_WITH_KNOTS('',3,(#65963,#65964,#65965,#65966,#65967,
#65968,#65969,#65970,#65971,#65972,#65973,#65974,#65975,#65976,#65977,#65978),
 .UNSPECIFIED.,.F.,.F.,(4,1,1,1,1,1,1,1,1,1,1,1,1,4),(72.2566310325653,
72.7298368269531,73.2292470126874,73.7286571984216,74.2280673841559,74.7274775698902,
75.2268877556245,75.7262979413587,76.225708127093,76.7251183128273,77.2245284985616,
77.7239386842958,78.2233488700301,78.5398163397448),.UNSPECIFIED.);
#788=B_SPLINE_CURVE_WITH_KNOTS('',3,(#65983,#65984,#65985,#65986,#65987,
#65988,#65989,#65990,#65991,#65992,#65993,#65994,#65995,#65996,#65997,#65998,
#65999),.UNSPECIFIED.,.F.,.F.,(4,1,1,1,1,1,1,1,1,1,1,1,1,1,4),(65.9734457253856,
66.0511317641465,66.5505419498808,67.0499521356151,67.5493623213494,68.0487725070836,
68.5481826928179,69.0475928785522,69.5470030642865,70.0464132500207,70.545823435755,
71.0452336214893,71.5446438072236,72.0440539929578,72.2566310325653),
 .UNSPECIFIED.);
#789=B_SPLINE_CURVE_WITH_KNOTS('',3,(#66000,#66001,#66002,#66003,#66004,
#66005,#66006,#66007,#66008,#66009,#66010,#66011,#66012,#66013,#66014,#66015,
#66016),.UNSPECIFIED.,.F.,.F.,(4,1,1,1,1,1,1,1,1,1,1,1,1,1,4),(65.9734457253856,
66.2375044124075,66.7369145981418,67.2363247838761,67.7357349696103,68.2351451553446,
68.7345553410789,69.2339655268132,69.7333757125475,70.2327858982817,70.732196084016,
71.2316062697503,71.7310164554845,72.2304266412188,72.2566310325653),
 .UNSPECIFIED.);
#790=B_SPLINE_CURVE_WITH_KNOTS('',3,(#66021,#66022,#66023,#66024,#66025,
#66026,#66027,#66028,#66029,#66030,#66031,#66032,#66033,#66034,#66035,#66036),
 .UNSPECIFIED.,.F.,.F.,(4,1,1,1,1,1,1,1,1,1,1,1,1,4),(59.6902604182061,
60.0582095353353,60.5576197210695,61.0570299068038,61.5564400925381,62.0558502782724,
62.5552604640066,63.0546706497409,63.5540808354752,64.0534910212095,64.5529012069437,
65.052311392678,65.5517215784123,65.9734457253856),.UNSPECIFIED.);
#791=B_SPLINE_CURVE_WITH_KNOTS('',3,(#66037,#66038,#66039,#66040,#66041,
#66042,#66043,#66044,#66045,#66046,#66047,#66048,#66049,#66050,#66051,#66052,
#66053),.UNSPECIFIED.,.F.,.F.,(4,1,1,1,1,1,1,1,1,1,1,1,1,1,4),(59.6902604182061,
59.745171997862,60.2445821835963,60.7439923693305,61.2434025550648,61.7428127407991,
62.2422229265333,62.7416331122676,63.2410432980019,63.7404534837362,64.2398636694704,
64.7392738552047,65.238684040939,65.7380942266733,65.9734457253856),
 .UNSPECIFIED.);
#792=B_SPLINE_CURVE_WITH_KNOTS('',3,(#66058,#66059,#66060,#66061,#66062,
#66063,#66064,#66065,#66066,#66067,#66068,#66069,#66070,#66071,#66072,#66073,
#66074),.UNSPECIFIED.,.F.,.F.,(4,1,1,1,1,1,1,1,1,1,1,1,1,1,4),(53.4070751110265,
53.5658771207897,54.065287306524,54.5646974922582,55.0641076779925,55.5635178637268,
56.0629280494611,56.5623382351953,57.0617484209296,57.5611586066639,58.0605687923982,
58.5599789781324,59.0593891638667,59.558799349601,59.6902604182061),
 .UNSPECIFIED.);
#793=B_SPLINE_CURVE_WITH_KNOTS('',3,(#66075,#66076,#66077,#66078,#66079,
#66080,#66081,#66082,#66083,#66084,#66085,#66086,#66087,#66088,#66089,#66090),
 .UNSPECIFIED.,.F.,.F.,(4,1,1,1,1,1,1,1,1,1,1,1,1,4),(53.4070751110265,
53.7522497690507,54.251659954785,54.7510701405192,55.2504803262535,55.7498905119878,
56.2493006977221,56.7487108834563,57.2481210691906,57.7475312549249,58.2469414406592,
58.7463516263934,59.2457618121277,59.6902604182061),.UNSPECIFIED.);
#794=B_SPLINE_CURVE_WITH_KNOTS('',3,(#66095,#66096,#66097,#66098,#66099,
#66100,#66101,#66102,#66103,#66104,#66105,#66106,#66107,#66108,#66109,#66110),
 .UNSPECIFIED.,.F.,.F.,(4,1,1,1,1,1,1,1,1,1,1,1,1,4),(47.1238898038469,
47.5729548919784,48.0723650777127,48.571775263447,49.0711854491812,49.5705956349155,
50.0700058206498,50.5694160063841,51.0688261921183,51.5682363778526,52.0676465635869,
52.5670567493211,53.0664669350554,53.4070751110265),.UNSPECIFIED.);
#795=B_SPLINE_CURVE_WITH_KNOTS('',3,(#66111,#66112,#66113,#66114,#66115,
#66116,#66117,#66118,#66119,#66120,#66121,#66122,#66123,#66124,#66125,#66126,
#66127),.UNSPECIFIED.,.F.,.F.,(4,1,1,1,1,1,1,1,1,1,1,1,1,1,4),(47.1238898038469,
47.2599173545051,47.7593275402394,48.2587377259737,48.758147911708,49.2575580974422,
49.7569682831765,50.2563784689108,50.755788654645,51.2551988403793,51.7546090261136,
52.2540192118479,52.7534293975821,53.2528395833164,53.4070751110265),
 .UNSPECIFIED.);
#796=B_SPLINE_CURVE_WITH_KNOTS('',3,(#66132,#66133,#66134,#66135,#66136,
#66137,#66138,#66139,#66140,#66141,#66142,#66143,#66144,#66145,#66146,#66147,
#66148),.UNSPECIFIED.,.F.,.F.,(4,1,1,1,1,1,1,1,1,1,1,1,1,1,4),(40.8407044966673,
41.0806224774328,41.5800326631671,42.0794428489014,42.5788530346357,43.0782632203699,
43.5776734061042,44.0770835918385,44.5764937775728,45.075903963307,45.5753141490413,
46.0747243347756,46.5741345205099,47.0735447062441,47.1238898038469),
 .UNSPECIFIED.);
#797=B_SPLINE_CURVE_WITH_KNOTS('',3,(#66149,#66150,#66151,#66152,#66153,
#66154,#66155,#66156,#66157,#66158,#66159,#66160,#66161,#66162,#66163,#66164),
 .UNSPECIFIED.,.F.,.F.,(4,1,1,1,1,1,1,1,1,1,1,1,1,4),(40.8407044966673,
41.2669951256938,41.7664053114281,42.2658154971624,42.7652256828967,43.2646358686309,
43.7640460543652,44.2634562400995,44.7628664258338,45.262276611568,45.7616867973023,
46.2610969830366,46.7605071687709,47.1238898038469),.UNSPECIFIED.);
#798=B_SPLINE_CURVE_WITH_KNOTS('',3,(#66169,#66170,#66171,#66172,#66173,
#66174,#66175,#66176,#66177,#66178,#66179,#66180,#66181,#66182,#66183,#66184,
#66185),.UNSPECIFIED.,.F.,.F.,(4,1,1,1,1,1,1,1,1,1,1,1,1,1,4),(34.5575191894877,
34.5882900628873,35.0877002486216,35.5871104343558,36.0865206200901,36.5859308058244,
37.0853409915587,37.5847511772929,38.0841613630272,38.5835715487615,39.0829817344957,
39.58239192023,40.0818021059643,40.5812122916986,40.8407044966673),
 .UNSPECIFIED.);
#799=B_SPLINE_CURVE_WITH_KNOTS('',3,(#66186,#66187,#66188,#66189,#66190,
#66191,#66192,#66193,#66194,#66195,#66196,#66197,#66198,#66199,#66200,#66201,
#66202),.UNSPECIFIED.,.F.,.F.,(4,1,1,1,1,1,1,1,1,1,1,1,1,1,4),(34.5575191894877,
34.7746627111483,35.2740728968826,35.7734830826168,36.2728932683511,36.7723034540854,
37.2717136398197,37.7711238255539,38.2705340112882,38.7699441970225,39.2693543827567,
39.768764568491,40.2681747542253,40.7675849399596,40.8407044966673),
 .UNSPECIFIED.);
#800=B_SPLINE_CURVE_WITH_KNOTS('',3,(#66207,#66208,#66209,#66210,#66211,
#66212,#66213,#66214,#66215,#66216,#66217,#66218,#66219,#66220,#66221,#66222),
 .UNSPECIFIED.,.F.,.F.,(4,1,1,1,1,1,1,1,1,1,1,1,1,4),(28.2743338823081,
28.595367834076,29.0947780198103,29.5941882055445,30.0935983912788,30.5930085770131,
31.0924187627474,31.5918289484816,32.0912391342159,32.5906493199502,33.0900595056845,
33.5894696914187,34.088879877153,34.5575191894877),.UNSPECIFIED.);
#801=B_SPLINE_CURVE_WITH_KNOTS('',3,(#66223,#66224,#66225,#66226,#66227,
#66228,#66229,#66230,#66231,#66232,#66233,#66234,#66235,#66236,#66237,#66238,
#66239),.UNSPECIFIED.,.F.,.F.,(4,1,1,1,1,1,1,1,1,1,1,1,1,1,4),(28.2743338823081,
28.2823302966027,28.781740482337,29.2811506680713,29.7805608538055,30.2799710395398,
30.7793812252741,31.2787914110084,31.7782015967426,32.2776117824769,32.7770219682112,
33.2764321539455,33.7758423396797,34.275252525414,34.5575191894877),
 .UNSPECIFIED.);
#802=B_SPLINE_CURVE_WITH_KNOTS('',3,(#66244,#66245,#66246,#66247,#66248,
#66249,#66250,#66251,#66252,#66253,#66254,#66255,#66256,#66257,#66258,#66259,
#66260),.UNSPECIFIED.,.F.,.F.,(4,1,1,1,1,1,1,1,1,1,1,1,1,1,4),(21.9911485751285,
22.1030354195304,22.6024456052647,23.101855790999,23.6012659767333,24.1006761624675,
24.6000863482018,25.0994965339361,25.5989067196703,26.0983169054046,26.5977270911389,
27.0971372768732,27.5965474626074,28.0959576483417,28.2743338823081),
 .UNSPECIFIED.);
#803=B_SPLINE_CURVE_WITH_KNOTS('',3,(#66261,#66262,#66263,#66264,#66265,
#66266,#66267,#66268,#66269,#66270,#66271,#66272,#66273,#66274,#66275,#66276),
 .UNSPECIFIED.,.F.,.F.,(4,1,1,1,1,1,1,1,1,1,1,1,1,4),(21.9911485751285,
22.2894080677914,22.7888182535257,23.28822843926,23.7876386249943,24.2870488107285,
24.7864589964628,25.2858691821971,25.7852793679313,26.2846895536656,26.7840997393999,
27.2835099251342,27.7829201108684,28.2743338823081),.UNSPECIFIED.);
#804=B_SPLINE_CURVE_WITH_KNOTS('',3,(#66281,#66282,#66283,#66284,#66285,
#66286,#66287,#66288,#66289,#66290,#66291,#66292,#66293,#66294,#66295,#66296),
 .UNSPECIFIED.,.F.,.F.,(4,1,1,1,1,1,1,1,1,1,1,1,1,4),(15.7079632679489,
16.1101131907191,16.6095233764534,17.1089335621877,17.608343747922,18.1077539336562,
18.6071641193905,19.1065743051248,19.6059844908591,20.1053946765933,20.6048048623276,
21.1042150480619,21.6036252337962,21.9911485751285),.UNSPECIFIED.);
#805=B_SPLINE_CURVE_WITH_KNOTS('',3,(#66297,#66298,#66299,#66300,#66301,
#66302,#66303,#66304,#66305,#66306,#66307,#66308,#66309,#66310,#66311,#66312,
#66313),.UNSPECIFIED.,.F.,.F.,(4,1,1,1,1,1,1,1,1,1,1,1,1,1,4),(15.7079632679489,
15.7970756532459,16.2964858389801,16.7958960247144,17.2953062104487,17.794716396183,
18.2941265819172,18.7935367676515,19.2929469533858,19.7923571391201,20.2917673248543,
20.7911775105886,21.2905876963229,21.7899978820572,21.9911485751285),
 .UNSPECIFIED.);
#806=B_SPLINE_CURVE_WITH_KNOTS('',3,(#67479,#67480,#67481,#67482,#67483,
#67484,#67485,#67486,#67487,#67488,#67489,#67490,#67491,#67492,#67493,#67494,
#67495,#67496,#67497,#67498,#67499,#67500,#67501,#67502,#67503,#67504,#67505,
#67506,#67507,#67508,#67509,#67510,#67511,#67512,#67513,#67514,#67515,#67516,
#67517,#67518,#67519,#67520,#67521,#67522,#67523,#67524,#67525,#67526,#67527,
#67528,#67529,#67530,#67531,#67532,#67533,#67534,#67535,#67536,#67537,#67538,
#67539,#67540,#67541,#67542,#67543,#67544,#67545,#67546,#67547,#67548),
 .UNSPECIFIED.,.F.,.F.,(4,3,3,3,3,3,3,3,3,3,3,3,3,3,3,3,3,3,3,3,3,3,3,4),
(-1.12653966532777,-1.08393007696725,-1.01186793859792,-0.979479106883256,
-0.956116981122905,-0.875899252306419,-0.82547163350704,-0.8061866417097,
-0.795681523489932,-0.710458657553849,-0.62620775347041,-0.607006915743544,
-0.586923413382426,-0.518700915770662,-0.451188877692257,-0.412581476881461,
-0.394181574045281,-0.313650449653669,-0.253407622478392,-0.210833150163061,
-0.193782661020163,-0.115040611558608,-0.0378484817361047,0.),
 .UNSPECIFIED.);
#807=B_SPLINE_CURVE_WITH_KNOTS('',3,(#67549,#67550,#67551,#67552,#67553,
#67554,#67555,#67556,#67557,#67558,#67559,#67560,#67561,#67562,#67563,#67564),
 .UNSPECIFIED.,.F.,.F.,(4,3,3,3,3,4),(139.348931851488,139.834852005597,
140.334262191331,140.833672377065,141.3330825628,141.760329302685),
 .UNSPECIFIED.);
#808=B_SPLINE_CURVE_WITH_KNOTS('',3,(#67566,#67567,#67568,#67569,#67570,
#67571,#67572,#67573,#67574,#67575,#67576,#67577,#67578,#67579,#67580,#67581,
#67582,#67583,#67584,#67585,#67586,#67587,#67588,#67589,#67590,#67591,#67592,
#67593,#67594,#67595,#67596,#67597,#67598,#67599,#67600,#67601,#67602,#67603,
#67604,#67605,#67606,#67607,#67608,#67609,#67610,#67611,#67612,#67613,#67614,
#67615,#67616,#67617,#67618,#67619,#67620,#67621,#67622,#67623,#67624,#67625,
#67626,#67627,#67628,#67629,#67630,#67631,#67632,#67633,#67634,#67635,#67636,
#67637,#67638),.UNSPECIFIED.,.F.,.F.,(4,3,3,3,3,3,3,3,3,3,3,3,3,3,3,3,3,
3,3,3,3,3,3,3,4),(-1.13094109509784,-1.09499881239214,-1.03107752332609,
-1.00370431748061,-0.983750389109266,-0.911532022618602,-0.881102070346245,
-0.860943270171285,-0.839313656127939,-0.758239088642718,-0.705009903366053,
-0.662463525867964,-0.643629991304747,-0.571319967865515,-0.50135866204052,
-0.457365025783336,-0.433111592060782,-0.34693419716568,-0.291474744565535,
-0.247356571073232,-0.228207082344636,-0.208365914759508,-0.120835935788132,
-0.0326428575257076,0.),.UNSPECIFIED.);
#809=B_SPLINE_CURVE_WITH_KNOTS('',3,(#67639,#67640,#67641,#67642,#67643,
#67644,#67645,#67646,#67647,#67648,#67649,#67650,#67651,#67652),
 .UNSPECIFIED.,.F.,.F.,(4,1,1,1,1,1,1,1,1,1,1,4),(10.3757270560179,10.8029737959031,
11.3023839816374,11.8017941673717,12.301204353106,12.8006145388402,13.3000247245745,
13.7994349103088,14.298845096043,14.7982552817773,15.2976654675116,15.7079632679489),
 .UNSPECIFIED.);
#810=B_SPLINE_CURVE_WITH_KNOTS('',3,(#67658,#67659,#67660,#67661,#67662,
#67663,#67664,#67665,#67666,#67667,#67668,#67669,#67670,#67671,#67672,#67673,
#67674,#67675,#67676,#67677,#67678,#67679,#67680,#67681,#67682,#67683,#67684,
#67685,#67686,#67687,#67688,#67689,#67690,#67691,#67692,#67693,#67694,#67695,
#67696,#67697,#67698,#67699,#67700,#67701,#67702,#67703,#67704,#67705,#67706,
#67707,#67708,#67709,#67710,#67711,#67712,#67713,#67714,#67715,#67716,#67717,
#67718,#67719,#67720,#67721,#67722,#67723,#67724,#67725,#67726,#67727),
 .UNSPECIFIED.,.F.,.F.,(4,3,3,3,3,3,3,3,3,3,3,3,3,3,3,3,3,3,3,3,3,3,3,4),
(-1.12653966532772,-1.08393007696717,-1.01186793859786,-0.979479105150202,
-0.956116979414424,-0.875899251452182,-0.825471633444292,-0.806186641683957,
-0.795681523489941,-0.710458660083624,-0.626207772623579,-0.607006965671262,
-0.586923425467474,-0.51870091577066,-0.45118883434751,-0.412581370547731,
-0.394181524461002,-0.313650379586371,-0.253407622478375,-0.210833136397955,
-0.193782655965201,-0.11504060523123,-0.0378485150221377,0.),
 .UNSPECIFIED.);
#811=B_SPLINE_CURVE_WITH_KNOTS('',3,(#67730,#67731,#67732,#67733,#67734,
#67735,#67736,#67737,#67738,#67739,#67740,#67741),.UNSPECIFIED.,.F.,.F.,
(4,1,1,1,1,1,1,1,1,4),(11.6154215191107,12.1148317048449,12.6142418905792,
13.1136520763135,13.6130622620478,14.112472447782,14.6118826335163,15.1112928192506,
15.6107030049849,15.7079632679489),.UNSPECIFIED.);
#812=B_SPLINE_CURVE_WITH_KNOTS('',3,(#68907,#68908,#68909,#68910,#68911,
#68912,#68913,#68914,#68915,#68916,#68917,#68918,#68919,#68920,#68921,#68922,
#68923,#68924,#68925,#68926,#68927,#68928,#68929,#68930,#68931,#68932,#68933,
#68934,#68935,#68936,#68937,#68938,#68939,#68940,#68941,#68942,#68943,#68944,
#68945,#68946,#68947,#68948,#68949,#68950,#68951,#68952,#68953,#68954,#68955,
#68956,#68957,#68958,#68959,#68960,#68961,#68962,#68963,#68964,#68965,#68966,
#68967,#68968,#68969,#68970,#68971,#68972,#68973,#68974,#68975,#68976,#68977,
#68978,#68979),.UNSPECIFIED.,.F.,.F.,(4,3,3,3,3,3,3,3,3,3,3,3,3,3,3,3,3,
3,3,3,3,3,3,3,4),(-1.13094109509794,-1.09499881239224,-1.03107752332618,
-1.00370431382378,-0.983750382690077,-0.911532019409036,-0.881102067268382,
-0.860943264422037,-0.839313656127995,-0.758239093290739,-0.705009897535087,
-0.662463517590346,-0.643629976777734,-0.571319967865571,-0.501358662040571,
-0.457365024033757,-0.43311159034779,-0.346934199158609,-0.291474744565571,
-0.247356575879909,-0.228207098197964,-0.208365917531837,-0.120835914342496,
-0.032642851524005,0.),.UNSPECIFIED.);
#813=B_SPLINE_CURVE_WITH_KNOTS('',3,(#68980,#68981,#68982,#68983,#68984,
#68985,#68986,#68987,#68988,#68989,#68990,#68991,#68992),.UNSPECIFIED.,
 .F.,.F.,(4,3,3,3,4),(-143.830133491471,-143.330723305737,-142.831313120002,
-142.331902934268,-142.322618506789),.UNSPECIFIED.);
#1016=SHAPE_REPRESENTATION_RELATIONSHIP('SRR','None',#76753,#1036);
#1036=ADVANCED_BREP_SHAPE_REPRESENTATION('',(#1076),#76657);
#1056=STYLED_ITEM('',(#76913),#1076);
#1076=MANIFOLD_SOLID_BREP('Hex screw',#26681);
#1414=CYLINDRICAL_SURFACE('',#28561,0.591675);
#1415=CYLINDRICAL_SURFACE('',#28563,0.591675);
#1416=CYLINDRICAL_SURFACE('',#28564,0.591675);
#1417=CYLINDRICAL_SURFACE('',#28565,0.591675);
#1418=CYLINDRICAL_SURFACE('',#28566,0.591675);
#1419=CYLINDRICAL_SURFACE('',#28567,0.591675);
#1420=CYLINDRICAL_SURFACE('',#28568,0.591675);
#1421=CYLINDRICAL_SURFACE('',#28569,0.591675);
#1422=CYLINDRICAL_SURFACE('',#28570,0.591675);
#1423=CYLINDRICAL_SURFACE('',#28571,0.591675);
#1424=CYLINDRICAL_SURFACE('',#28572,0.591675);
#1425=CYLINDRICAL_SURFACE('',#28573,0.591675);
#1426=CYLINDRICAL_SURFACE('',#28574,0.591675);
#1427=CYLINDRICAL_SURFACE('',#28575,0.591675);
#1428=CYLINDRICAL_SURFACE('',#28576,0.591675);
#1429=CYLINDRICAL_SURFACE('',#28577,0.591675);
#1430=CYLINDRICAL_SURFACE('',#28578,0.591675);
#1431=CYLINDRICAL_SURFACE('',#28579,0.591675);
#1432=CYLINDRICAL_SURFACE('',#28580,0.591675);
#1433=CYLINDRICAL_SURFACE('',#28581,0.591675);
#1434=CYLINDRICAL_SURFACE('',#28582,0.591675);
#1435=CYLINDRICAL_SURFACE('',#28583,0.591675);
#1436=CYLINDRICAL_SURFACE('',#28584,0.591675);
#1437=CYLINDRICAL_SURFACE('',#28585,0.491825);
#1438=CYLINDRICAL_SURFACE('',#28587,0.491825);
#1439=CYLINDRICAL_SURFACE('',#28588,0.491825);
#1440=CYLINDRICAL_SURFACE('',#28589,0.491825);
#1441=CYLINDRICAL_SURFACE('',#28590,0.491825);
#1442=CYLINDRICAL_SURFACE('',#28591,0.491825);
#1443=CYLINDRICAL_SURFACE('',#28592,0.491825);
#1444=CYLINDRICAL_SURFACE('',#28593,0.491825);
#1445=CYLINDRICAL_SURFACE('',#28594,0.491825);
#1446=CYLINDRICAL_SURFACE('',#28595,0.491825);
#1447=CYLINDRICAL_SURFACE('',#28596,0.491825);
#1448=CYLINDRICAL_SURFACE('',#28597,0.491825);
#1449=CYLINDRICAL_SURFACE('',#28598,0.491825);
#1450=CYLINDRICAL_SURFACE('',#28599,0.491825);
#1451=CYLINDRICAL_SURFACE('',#28600,0.491825);
#1452=CYLINDRICAL_SURFACE('',#28601,0.491825);
#1453=CYLINDRICAL_SURFACE('',#28602,0.491825);
#1454=CYLINDRICAL_SURFACE('',#28603,0.491825);
#1455=CYLINDRICAL_SURFACE('',#28604,0.491825);
#1456=CYLINDRICAL_SURFACE('',#28605,0.491825);
#1457=CYLINDRICAL_SURFACE('',#28606,0.491825);
#1458=CYLINDRICAL_SURFACE('',#28607,0.491825);
#1459=CYLINDRICAL_SURFACE('',#28612,0.491825);
#1460=CYLINDRICAL_SURFACE('',#28627,0.591675);
#1461=CYLINDRICAL_SURFACE('',#28631,0.83);
#1650=FACE_BOUND('',#5289,.T.);
#1651=FACE_BOUND('',#5298,.T.);
#2191=PLANE('',#28608);
#2192=PLANE('',#28615);
#2193=PLANE('',#28616);
#2194=PLANE('',#28617);
#2195=PLANE('',#28618);
#2196=PLANE('',#28620);
#2197=PLANE('',#28621);
#2198=PLANE('',#28622);
#2199=PLANE('',#28623);
#2200=PLANE('',#28624);
#2201=PLANE('',#28629);
#3586=FACE_OUTER_BOUND('',#5235,.T.);
#3587=FACE_OUTER_BOUND('',#5236,.T.);
#3588=FACE_OUTER_BOUND('',#5237,.T.);
#3589=FACE_OUTER_BOUND('',#5238,.T.);
#3590=FACE_OUTER_BOUND('',#5239,.T.);
#3591=FACE_OUTER_BOUND('',#5240,.T.);
#3592=FACE_OUTER_BOUND('',#5241,.T.);
#3593=FACE_OUTER_BOUND('',#5242,.T.);
#3594=FACE_OUTER_BOUND('',#5243,.T.);
#3595=FACE_OUTER_BOUND('',#5244,.T.);
#3596=FACE_OUTER_BOUND('',#5245,.T.);
#3597=FACE_OUTER_BOUND('',#5246,.T.);
#3598=FACE_OUTER_BOUND('',#5247,.T.);
#3599=FACE_OUTER_BOUND('',#5248,.T.);
#3600=FACE_OUTER_BOUND('',#5249,.T.);
#3601=FACE_OUTER_BOUND('',#5250,.T.);
#3602=FACE_OUTER_BOUND('',#5251,.T.);
#3603=FACE_OUTER_BOUND('',#5252,.T.);
#3604=FACE_OUTER_BOUND('',#5253,.T.);
#3605=FACE_OUTER_BOUND('',#5254,.T.);
#3606=FACE_OUTER_BOUND('',#5255,.T.);
#3607=FACE_OUTER_BOUND('',#5256,.T.);
#3608=FACE_OUTER_BOUND('',#5257,.T.);
#3609=FACE_OUTER_BOUND('',#5258,.T.);
#3610=FACE_OUTER_BOUND('',#5259,.T.);
#3611=FACE_OUTER_BOUND('',#5260,.T.);
#3612=FACE_OUTER_BOUND('',#5261,.T.);
#3613=FACE_OUTER_BOUND('',#5262,.T.);
#3614=FACE_OUTER_BOUND('',#5263,.T.);
#3615=FACE_OUTER_BOUND('',#5264,.T.);
#3616=FACE_OUTER_BOUND('',#5265,.T.);
#3617=FACE_OUTER_BOUND('',#5266,.T.);
#3618=FACE_OUTER_BOUND('',#5267,.T.);
#3619=FACE_OUTER_BOUND('',#5268,.T.);
#3620=FACE_OUTER_BOUND('',#5269,.T.);
#3621=FACE_OUTER_BOUND('',#5270,.T.);
#3622=FACE_OUTER_BOUND('',#5271,.T.);
#3623=FACE_OUTER_BOUND('',#5272,.T.);
#3624=FACE_OUTER_BOUND('',#5273,.T.);
#3625=FACE_OUTER_BOUND('',#5274,.T.);
#3626=FACE_OUTER_BOUND('',#5275,.T.);
#3627=FACE_OUTER_BOUND('',#5276,.T.);
#3628=FACE_OUTER_BOUND('',#5277,.T.);
#3629=FACE_OUTER_BOUND('',#5278,.T.);
#3630=FACE_OUTER_BOUND('',#5279,.T.);
#3631=FACE_OUTER_BOUND('',#5280,.T.);
#3632=FACE_OUTER_BOUND('',#5281,.T.);
#3633=FACE_OUTER_BOUND('',#5282,.T.);
#3634=FACE_OUTER_BOUND('',#5283,.T.);
#3635=FACE_OUTER_BOUND('',#5284,.T.);
#3636=FACE_OUTER_BOUND('',#5285,.T.);
#3637=FACE_OUTER_BOUND('',#5286,.T.);
#3638=FACE_OUTER_BOUND('',#5287,.T.);
#3639=FACE_OUTER_BOUND('',#5288,.T.);
#3640=FACE_OUTER_BOUND('',#5290,.T.);
#3641=FACE_OUTER_BOUND('',#5291,.T.);
#3642=FACE_OUTER_BOUND('',#5292,.T.);
#3643=FACE_OUTER_BOUND('',#5293,.T.);
#3644=FACE_OUTER_BOUND('',#5294,.T.);
#3645=FACE_OUTER_BOUND('',#5295,.T.);
#3646=FACE_OUTER_BOUND('',#5296,.T.);
#3647=FACE_OUTER_BOUND('',#5297,.T.);
#3648=FACE_OUTER_BOUND('',#5299,.T.);
#5235=EDGE_LOOP('',(#22415,#22416,#22417,#22418));
#5236=EDGE_LOOP('',(#22419,#22420,#22421,#22422));
#5237=EDGE_LOOP('',(#22423,#22424,#22425,#22426));
#5238=EDGE_LOOP('',(#22427,#22428,#22429,#22430));
#5239=EDGE_LOOP('',(#22431,#22432,#22433,#22434));
#5240=EDGE_LOOP('',(#22435,#22436,#22437,#22438));
#5241=EDGE_LOOP('',(#22439,#22440,#22441,#22442));
#5242=EDGE_LOOP('',(#22443,#22444,#22445,#22446));
#5243=EDGE_LOOP('',(#22447,#22448,#22449,#22450));
#5244=EDGE_LOOP('',(#22451,#22452,#22453,#22454));
#5245=EDGE_LOOP('',(#22455,#22456,#22457,#22458));
#5246=EDGE_LOOP('',(#22459,#22460,#22461,#22462));
#5247=EDGE_LOOP('',(#22463,#22464,#22465,#22466));
#5248=EDGE_LOOP('',(#22467,#22468,#22469,#22470));
#5249=EDGE_LOOP('',(#22471,#22472,#22473,#22474));
#5250=EDGE_LOOP('',(#22475,#22476,#22477,#22478));
#5251=EDGE_LOOP('',(#22479,#22480,#22481,#22482));
#5252=EDGE_LOOP('',(#22483,#22484,#22485,#22486));
#5253=EDGE_LOOP('',(#22487,#22488,#22489,#22490));
#5254=EDGE_LOOP('',(#22491,#22492,#22493,#22494));
#5255=EDGE_LOOP('',(#22495,#22496,#22497,#22498));
#5256=EDGE_LOOP('',(#22499,#22500,#22501,#22502));
#5257=EDGE_LOOP('',(#22503,#22504,#22505,#22506));
#5258=EDGE_LOOP('',(#22507,#22508,#22509,#22510));
#5259=EDGE_LOOP('',(#22511,#22512,#22513,#22514));
#5260=EDGE_LOOP('',(#22515,#22516,#22517,#22518));
#5261=EDGE_LOOP('',(#22519,#22520,#22521,#22522));
#5262=EDGE_LOOP('',(#22523,#22524,#22525,#22526));
#5263=EDGE_LOOP('',(#22527,#22528,#22529,#22530));
#5264=EDGE_LOOP('',(#22531,#22532,#22533,#22534));
#5265=EDGE_LOOP('',(#22535,#22536,#22537,#22538));
#5266=EDGE_LOOP('',(#22539,#22540,#22541,#22542));
#5267=EDGE_LOOP('',(#22543,#22544,#22545,#22546));
#5268=EDGE_LOOP('',(#22547,#22548,#22549,#22550));
#5269=EDGE_LOOP('',(#22551,#22552,#22553,#22554));
#5270=EDGE_LOOP('',(#22555,#22556,#22557,#22558));
#5271=EDGE_LOOP('',(#22559,#22560,#22561,#22562));
#5272=EDGE_LOOP('',(#22563,#22564,#22565,#22566));
#5273=EDGE_LOOP('',(#22567,#22568,#22569,#22570));
#5274=EDGE_LOOP('',(#22571,#22572,#22573,#22574));
#5275=EDGE_LOOP('',(#22575,#22576,#22577,#22578));
#5276=EDGE_LOOP('',(#22579,#22580,#22581,#22582));
#5277=EDGE_LOOP('',(#22583,#22584,#22585,#22586));
#5278=EDGE_LOOP('',(#22587,#22588,#22589,#22590));
#5279=EDGE_LOOP('',(#22591,#22592,#22593,#22594));
#5280=EDGE_LOOP('',(#22595,#22596,#22597,#22598,#22599,#22600,#22601,#22602,
#22603,#22604,#22605,#22606,#22607,#22608,#22609,#22610,#22611,#22612,#22613,
#22614,#22615,#22616,#22617,#22618,#22619,#22620,#22621,#22622,#22623,#22624,
#22625,#22626,#22627,#22628,#22629,#22630,#22631,#22632,#22633,#22634,#22635,
#22636,#22637,#22638,#22639,#22640,#22641,#22642,#22643));
#5281=EDGE_LOOP('',(#22644,#22645,#22646,#22647,#22648));
#5282=EDGE_LOOP('',(#22649,#22650,#22651,#22652));
#5283=EDGE_LOOP('',(#22653,#22654,#22655,#22656,#22657,#22658,#22659,#22660,
#22661,#22662,#22663,#22664,#22665,#22666,#22667,#22668,#22669,#22670,#22671,
#22672,#22673,#22674,#22675,#22676,#22677,#22678,#22679,#22680,#22681,#22682,
#22683,#22684,#22685,#22686,#22687,#22688,#22689,#22690,#22691,#22692,#22693,
#22694,#22695,#22696,#22697,#22698,#22699,#22700,#22701));
#5284=EDGE_LOOP('',(#22702,#22703,#22704,#22705,#22706,#22707,#22708,#22709,
#22710,#22711));
#5285=EDGE_LOOP('',(#22712,#22713,#22714,#22715));
#5286=EDGE_LOOP('',(#22716,#22717,#22718,#22719));
#5287=EDGE_LOOP('',(#22720,#22721,#22722,#22723));
#5288=EDGE_LOOP('',(#22724,#22725,#22726,#22727,#22728,#22729));
#5289=EDGE_LOOP('',(#22730));
#5290=EDGE_LOOP('',(#22731,#22732,#22733,#22734));
#5291=EDGE_LOOP('',(#22735,#22736,#22737,#22738));
#5292=EDGE_LOOP('',(#22739,#22740,#22741,#22742,#22743));
#5293=EDGE_LOOP('',(#22744));
#5294=EDGE_LOOP('',(#22745));
#5295=EDGE_LOOP('',(#22746,#22747,#22748,#22749,#22750,#22751));
#5296=EDGE_LOOP('',(#22752,#22753,#22754,#22755));
#5297=EDGE_LOOP('',(#22756));
#5298=EDGE_LOOP('',(#22757,#22758,#22759,#22760));
#5299=EDGE_LOOP('',(#22761,#22762,#22763,#22764));
#6322=CIRCLE('',#28562,0.591675);
#6323=CIRCLE('',#28586,0.491825);
#6324=CIRCLE('',#28609,0.591675);
#6325=CIRCLE('',#28610,0.591675);
#6326=CIRCLE('',#28611,0.491825);
#6327=CIRCLE('',#28614,0.855);
#6328=CIRCLE('',#28619,0.83);
#6329=CIRCLE('',#28625,0.54);
#6330=CIRCLE('',#28628,0.591675);
#6331=CIRCLE('',#28630,0.83);
#8053=LINE('',#63546,#10209);
#8054=LINE('',#63579,#10210);
#8055=LINE('',#63663,#10211);
#8056=LINE('',#63753,#10212);
#8057=LINE('',#63837,#10213);
#8058=LINE('',#63927,#10214);
#8059=LINE('',#64017,#10215);
#8060=LINE('',#64101,#10216);
#8061=LINE('',#64191,#10217);
#8062=LINE('',#64275,#10218);
#8063=LINE('',#64365,#10219);
#8064=LINE('',#64455,#10220);
#8065=LINE('',#64539,#10221);
#8066=LINE('',#64629,#10222);
#8067=LINE('',#64713,#10223);
#8068=LINE('',#64803,#10224);
#8069=LINE('',#64887,#10225);
#8070=LINE('',#64977,#10226);
#8071=LINE('',#65067,#10227);
#8072=LINE('',#65151,#10228);
#8073=LINE('',#65241,#10229);
#8074=LINE('',#65325,#10230);
#8075=LINE('',#65415,#10231);
#8076=LINE('',#65502,#10232);
#8077=LINE('',#65536,#10233);
#8078=LINE('',#65574,#10234);
#8079=LINE('',#65611,#10235);
#8080=LINE('',#65648,#10236);
#8081=LINE('',#65685,#10237);
#8082=LINE('',#65722,#10238);
#8083=LINE('',#65760,#10239);
#8084=LINE('',#65797,#10240);
#8085=LINE('',#65834,#10241);
#8086=LINE('',#65871,#10242);
#8087=LINE('',#65908,#10243);
#8088=LINE('',#65945,#10244);
#8089=LINE('',#65982,#10245);
#8090=LINE('',#66020,#10246);
#8091=LINE('',#66057,#10247);
#8092=LINE('',#66094,#10248);
#8093=LINE('',#66131,#10249);
#8094=LINE('',#66168,#10250);
#8095=LINE('',#66206,#10251);
#8096=LINE('',#66243,#10252);
#8097=LINE('',#66280,#10253);
#8098=LINE('',#69016,#10254);
#8099=LINE('',#69027,#10255);
#8100=LINE('',#69029,#10256);
#8101=LINE('',#69030,#10257);
#8102=LINE('',#69033,#10258);
#8103=LINE('',#69034,#10259);
#8104=LINE('',#69037,#10260);
#8105=LINE('',#69038,#10261);
#8106=LINE('',#69041,#10262);
#8107=LINE('',#69043,#10263);
#8108=LINE('',#69044,#10264);
#8109=LINE('',#69048,#10265);
#8110=LINE('',#69050,#10266);
#8111=LINE('',#69057,#10267);
#8112=LINE('',#69064,#10268);
#10209=VECTOR('',#34120,0.6);
#10210=VECTOR('',#34125,0.6);
#10211=VECTOR('',#34128,0.6);
#10212=VECTOR('',#34131,0.6);
#10213=VECTOR('',#34134,0.6);
#10214=VECTOR('',#34137,0.6);
#10215=VECTOR('',#34140,0.6);
#10216=VECTOR('',#34143,0.6);
#10217=VECTOR('',#34146,0.6);
#10218=VECTOR('',#34149,0.6);
#10219=VECTOR('',#34152,0.6);
#10220=VECTOR('',#34155,0.6);
#10221=VECTOR('',#34158,0.6);
#10222=VECTOR('',#34161,0.6);
#10223=VECTOR('',#34164,0.6);
#10224=VECTOR('',#34167,0.6);
#10225=VECTOR('',#34170,0.6);
#10226=VECTOR('',#34173,0.6);
#10227=VECTOR('',#34176,0.6);
#10228=VECTOR('',#34179,0.6);
#10229=VECTOR('',#34182,0.6);
#10230=VECTOR('',#34185,0.6);
#10231=VECTOR('',#34188,0.6);
#10232=VECTOR('',#34191,0.491825);
#10233=VECTOR('',#34196,0.491825);
#10234=VECTOR('',#34199,0.491825);
#10235=VECTOR('',#34202,0.491825);
#10236=VECTOR('',#34205,0.491825);
#10237=VECTOR('',#34208,0.491825);
#10238=VECTOR('',#34211,0.491825);
#10239=VECTOR('',#34214,0.491825);
#10240=VECTOR('',#34217,0.491825);
#10241=VECTOR('',#34220,0.491825);
#10242=VECTOR('',#34223,0.491825);
#10243=VECTOR('',#34226,0.491825);
#10244=VECTOR('',#34229,0.491825);
#10245=VECTOR('',#34232,0.491825);
#10246=VECTOR('',#34235,0.491825);
#10247=VECTOR('',#34238,0.491825);
#10248=VECTOR('',#34241,0.491825);
#10249=VECTOR('',#34244,0.491825);
#10250=VECTOR('',#34247,0.491825);
#10251=VECTOR('',#34250,0.491825);
#10252=VECTOR('',#34253,0.491825);
#10253=VECTOR('',#34256,0.491825);
#10254=VECTOR('',#34269,0.972115242270663);
#10255=VECTOR('',#34274,1.);
#10256=VECTOR('',#34275,1.);
#10257=VECTOR('',#34276,1.);
#10258=VECTOR('',#34279,1.);
#10259=VECTOR('',#34280,1.);
#10260=VECTOR('',#34283,1.);
#10261=VECTOR('',#34284,1.);
#10262=VECTOR('',#34287,1.);
#10263=VECTOR('',#34288,1.);
#10264=VECTOR('',#34289,1.);
#10265=VECTOR('',#34294,1.);
#10266=VECTOR('',#34297,1.);
#10267=VECTOR('',#34308,0.57);
#10268=VECTOR('',#34319,0.83);
#12538=VERTEX_POINT('',#63544);
#12539=VERTEX_POINT('',#63545);
#12540=VERTEX_POINT('',#63547);
#12541=VERTEX_POINT('',#63564);
#12542=VERTEX_POINT('',#63577);
#12543=VERTEX_POINT('',#63578);
#12544=VERTEX_POINT('',#63661);
#12545=VERTEX_POINT('',#63662);
#12546=VERTEX_POINT('',#63751);
#12547=VERTEX_POINT('',#63752);
#12548=VERTEX_POINT('',#63835);
#12549=VERTEX_POINT('',#63836);
#12550=VERTEX_POINT('',#63925);
#12551=VERTEX_POINT('',#63926);
#12552=VERTEX_POINT('',#64015);
#12553=VERTEX_POINT('',#64016);
#12554=VERTEX_POINT('',#64099);
#12555=VERTEX_POINT('',#64100);
#12556=VERTEX_POINT('',#64189);
#12557=VERTEX_POINT('',#64190);
#12558=VERTEX_POINT('',#64273);
#12559=VERTEX_POINT('',#64274);
#12560=VERTEX_POINT('',#64363);
#12561=VERTEX_POINT('',#64364);
#12562=VERTEX_POINT('',#64453);
#12563=VERTEX_POINT('',#64454);
#12564=VERTEX_POINT('',#64537);
#12565=VERTEX_POINT('',#64538);
#12566=VERTEX_POINT('',#64627);
#12567=VERTEX_POINT('',#64628);
#12568=VERTEX_POINT('',#64711);
#12569=VERTEX_POINT('',#64712);
#12570=VERTEX_POINT('',#64801);
#12571=VERTEX_POINT('',#64802);
#12572=VERTEX_POINT('',#64885);
#12573=VERTEX_POINT('',#64886);
#12574=VERTEX_POINT('',#64975);
#12575=VERTEX_POINT('',#64976);
#12576=VERTEX_POINT('',#65065);
#12577=VERTEX_POINT('',#65066);
#12578=VERTEX_POINT('',#65149);
#12579=VERTEX_POINT('',#65150);
#12580=VERTEX_POINT('',#65239);
#12581=VERTEX_POINT('',#65240);
#12582=VERTEX_POINT('',#65323);
#12583=VERTEX_POINT('',#65324);
#12584=VERTEX_POINT('',#65413);
#12585=VERTEX_POINT('',#65414);
#12586=VERTEX_POINT('',#65500);
#12587=VERTEX_POINT('',#65501);
#12588=VERTEX_POINT('',#65503);
#12589=VERTEX_POINT('',#65519);
#12590=VERTEX_POINT('',#65534);
#12591=VERTEX_POINT('',#65535);
#12592=VERTEX_POINT('',#65572);
#12593=VERTEX_POINT('',#65573);
#12594=VERTEX_POINT('',#65609);
#12595=VERTEX_POINT('',#65610);
#12596=VERTEX_POINT('',#65646);
#12597=VERTEX_POINT('',#65647);
#12598=VERTEX_POINT('',#65683);
#12599=VERTEX_POINT('',#65684);
#12600=VERTEX_POINT('',#65720);
#12601=VERTEX_POINT('',#65721);
#12602=VERTEX_POINT('',#65758);
#12603=VERTEX_POINT('',#65759);
#12604=VERTEX_POINT('',#65795);
#12605=VERTEX_POINT('',#65796);
#12606=VERTEX_POINT('',#65832);
#12607=VERTEX_POINT('',#65833);
#12608=VERTEX_POINT('',#65869);
#12609=VERTEX_POINT('',#65870);
#12610=VERTEX_POINT('',#65906);
#12611=VERTEX_POINT('',#65907);
#12612=VERTEX_POINT('',#65943);
#12613=VERTEX_POINT('',#65944);
#12614=VERTEX_POINT('',#65980);
#12615=VERTEX_POINT('',#65981);
#12616=VERTEX_POINT('',#66018);
#12617=VERTEX_POINT('',#66019);
#12618=VERTEX_POINT('',#66055);
#12619=VERTEX_POINT('',#66056);
#12620=VERTEX_POINT('',#66092);
#12621=VERTEX_POINT('',#66093);
#12622=VERTEX_POINT('',#66129);
#12623=VERTEX_POINT('',#66130);
#12624=VERTEX_POINT('',#66166);
#12625=VERTEX_POINT('',#66167);
#12626=VERTEX_POINT('',#66204);
#12627=VERTEX_POINT('',#66205);
#12628=VERTEX_POINT('',#66241);
#12629=VERTEX_POINT('',#66242);
#12630=VERTEX_POINT('',#66278);
#12631=VERTEX_POINT('',#66279);
#12632=VERTEX_POINT('',#67478);
#12633=VERTEX_POINT('',#67565);
#12634=VERTEX_POINT('',#67654);
#12635=VERTEX_POINT('',#67657);
#12636=VERTEX_POINT('',#68906);
#12637=VERTEX_POINT('',#68994);
#12638=VERTEX_POINT('',#68995);
#12639=VERTEX_POINT('',#68999);
#12640=VERTEX_POINT('',#69003);
#12641=VERTEX_POINT('',#69007);
#12642=VERTEX_POINT('',#69011);
#12643=VERTEX_POINT('',#69015);
#12644=VERTEX_POINT('',#69018);
#12645=VERTEX_POINT('',#69026);
#12646=VERTEX_POINT('',#69028);
#12647=VERTEX_POINT('',#69032);
#12648=VERTEX_POINT('',#69036);
#12649=VERTEX_POINT('',#69040);
#12650=VERTEX_POINT('',#69042);
#12651=VERTEX_POINT('',#69045);
#12652=VERTEX_POINT('',#69054);
#12653=VERTEX_POINT('',#69061);
#15930=EDGE_CURVE('',#12538,#12539,#8053,.T.);
#15931=EDGE_CURVE('',#12538,#12540,#716,.T.);
#15932=EDGE_CURVE('',#12540,#12541,#6322,.T.);
#15933=EDGE_CURVE('',#12541,#12539,#717,.T.);
#15934=EDGE_CURVE('',#12542,#12543,#8054,.T.);
#15935=EDGE_CURVE('',#12542,#12538,#718,.T.);
#15936=EDGE_CURVE('',#12539,#12543,#719,.T.);
#15937=EDGE_CURVE('',#12544,#12545,#8055,.T.);
#15938=EDGE_CURVE('',#12544,#12542,#720,.T.);
#15939=EDGE_CURVE('',#12543,#12545,#721,.T.);
#15940=EDGE_CURVE('',#12546,#12547,#8056,.T.);
#15941=EDGE_CURVE('',#12546,#12544,#722,.T.);
#15942=EDGE_CURVE('',#12545,#12547,#723,.T.);
#15943=EDGE_CURVE('',#12548,#12549,#8057,.T.);
#15944=EDGE_CURVE('',#12548,#12546,#724,.T.);
#15945=EDGE_CURVE('',#12547,#12549,#725,.T.);
#15946=EDGE_CURVE('',#12550,#12551,#8058,.T.);
#15947=EDGE_CURVE('',#12550,#12548,#726,.T.);
#15948=EDGE_CURVE('',#12549,#12551,#727,.T.);
#15949=EDGE_CURVE('',#12552,#12553,#8059,.T.);
#15950=EDGE_CURVE('',#12552,#12550,#728,.T.);
#15951=EDGE_CURVE('',#12551,#12553,#729,.T.);
#15952=EDGE_CURVE('',#12554,#12555,#8060,.T.);
#15953=EDGE_CURVE('',#12554,#12552,#730,.T.);
#15954=EDGE_CURVE('',#12553,#12555,#731,.T.);
#15955=EDGE_CURVE('',#12556,#12557,#8061,.T.);
#15956=EDGE_CURVE('',#12556,#12554,#732,.T.);
#15957=EDGE_CURVE('',#12555,#12557,#733,.T.);
#15958=EDGE_CURVE('',#12558,#12559,#8062,.T.);
#15959=EDGE_CURVE('',#12558,#12556,#734,.T.);
#15960=EDGE_CURVE('',#12557,#12559,#735,.T.);
#15961=EDGE_CURVE('',#12560,#12561,#8063,.T.);
#15962=EDGE_CURVE('',#12560,#12558,#736,.T.);
#15963=EDGE_CURVE('',#12559,#12561,#737,.T.);
#15964=EDGE_CURVE('',#12562,#12563,#8064,.T.);
#15965=EDGE_CURVE('',#12562,#12560,#738,.T.);
#15966=EDGE_CURVE('',#12561,#12563,#739,.T.);
#15967=EDGE_CURVE('',#12564,#12565,#8065,.T.);
#15968=EDGE_CURVE('',#12564,#12562,#740,.T.);
#15969=EDGE_CURVE('',#12563,#12565,#741,.T.);
#15970=EDGE_CURVE('',#12566,#12567,#8066,.T.);
#15971=EDGE_CURVE('',#12566,#12564,#742,.T.);
#15972=EDGE_CURVE('',#12565,#12567,#743,.T.);
#15973=EDGE_CURVE('',#12568,#12569,#8067,.T.);
#15974=EDGE_CURVE('',#12568,#12566,#744,.T.);
#15975=EDGE_CURVE('',#12567,#12569,#745,.T.);
#15976=EDGE_CURVE('',#12570,#12571,#8068,.T.);
#15977=EDGE_CURVE('',#12570,#12568,#746,.T.);
#15978=EDGE_CURVE('',#12569,#12571,#747,.T.);
#15979=EDGE_CURVE('',#12572,#12573,#8069,.T.);
#15980=EDGE_CURVE('',#12572,#12570,#748,.T.);
#15981=EDGE_CURVE('',#12571,#12573,#749,.T.);
#15982=EDGE_CURVE('',#12574,#12575,#8070,.T.);
#15983=EDGE_CURVE('',#12574,#12572,#750,.T.);
#15984=EDGE_CURVE('',#12573,#12575,#751,.T.);
#15985=EDGE_CURVE('',#12576,#12577,#8071,.T.);
#15986=EDGE_CURVE('',#12576,#12574,#752,.T.);
#15987=EDGE_CURVE('',#12575,#12577,#753,.T.);
#15988=EDGE_CURVE('',#12578,#12579,#8072,.T.);
#15989=EDGE_CURVE('',#12578,#12576,#754,.T.);
#15990=EDGE_CURVE('',#12577,#12579,#755,.T.);
#15991=EDGE_CURVE('',#12580,#12581,#8073,.T.);
#15992=EDGE_CURVE('',#12580,#12578,#756,.T.);
#15993=EDGE_CURVE('',#12579,#12581,#757,.T.);
#15994=EDGE_CURVE('',#12582,#12583,#8074,.T.);
#15995=EDGE_CURVE('',#12582,#12580,#758,.T.);
#15996=EDGE_CURVE('',#12581,#12583,#759,.T.);
#15997=EDGE_CURVE('',#12584,#12585,#8075,.T.);
#15998=EDGE_CURVE('',#12584,#12582,#760,.T.);
#15999=EDGE_CURVE('',#12583,#12585,#761,.T.);
#16000=EDGE_CURVE('',#12586,#12587,#8076,.T.);
#16001=EDGE_CURVE('',#12586,#12588,#762,.T.);
#16002=EDGE_CURVE('',#12589,#12588,#6323,.T.);
#16003=EDGE_CURVE('',#12587,#12589,#763,.T.);
#16004=EDGE_CURVE('',#12590,#12591,#8077,.T.);
#16005=EDGE_CURVE('',#12590,#12586,#764,.T.);
#16006=EDGE_CURVE('',#12591,#12587,#765,.T.);
#16007=EDGE_CURVE('',#12592,#12593,#8078,.T.);
#16008=EDGE_CURVE('',#12592,#12590,#766,.T.);
#16009=EDGE_CURVE('',#12593,#12591,#767,.T.);
#16010=EDGE_CURVE('',#12594,#12595,#8079,.T.);
#16011=EDGE_CURVE('',#12594,#12592,#768,.T.);
#16012=EDGE_CURVE('',#12595,#12593,#769,.T.);
#16013=EDGE_CURVE('',#12596,#12597,#8080,.T.);
#16014=EDGE_CURVE('',#12596,#12594,#770,.T.);
#16015=EDGE_CURVE('',#12597,#12595,#771,.T.);
#16016=EDGE_CURVE('',#12598,#12599,#8081,.T.);
#16017=EDGE_CURVE('',#12598,#12596,#772,.T.);
#16018=EDGE_CURVE('',#12599,#12597,#773,.T.);
#16019=EDGE_CURVE('',#12600,#12601,#8082,.T.);
#16020=EDGE_CURVE('',#12600,#12598,#774,.T.);
#16021=EDGE_CURVE('',#12601,#12599,#775,.T.);
#16022=EDGE_CURVE('',#12602,#12603,#8083,.T.);
#16023=EDGE_CURVE('',#12602,#12600,#776,.T.);
#16024=EDGE_CURVE('',#12603,#12601,#777,.T.);
#16025=EDGE_CURVE('',#12604,#12605,#8084,.T.);
#16026=EDGE_CURVE('',#12604,#12602,#778,.T.);
#16027=EDGE_CURVE('',#12605,#12603,#779,.T.);
#16028=EDGE_CURVE('',#12606,#12607,#8085,.T.);
#16029=EDGE_CURVE('',#12606,#12604,#780,.T.);
#16030=EDGE_CURVE('',#12607,#12605,#781,.T.);
#16031=EDGE_CURVE('',#12608,#12609,#8086,.T.);
#16032=EDGE_CURVE('',#12608,#12606,#782,.T.);
#16033=EDGE_CURVE('',#12609,#12607,#783,.T.);
#16034=EDGE_CURVE('',#12610,#12611,#8087,.T.);
#16035=EDGE_CURVE('',#12610,#12608,#784,.T.);
#16036=EDGE_CURVE('',#12611,#12609,#785,.T.);
#16037=EDGE_CURVE('',#12612,#12613,#8088,.T.);
#16038=EDGE_CURVE('',#12612,#12610,#786,.T.);
#16039=EDGE_CURVE('',#12613,#12611,#787,.T.);
#16040=EDGE_CURVE('',#12614,#12615,#8089,.T.);
#16041=EDGE_CURVE('',#12614,#12612,#788,.T.);
#16042=EDGE_CURVE('',#12615,#12613,#789,.T.);
#16043=EDGE_CURVE('',#12616,#12617,#8090,.T.);
#16044=EDGE_CURVE('',#12616,#12614,#790,.T.);
#16045=EDGE_CURVE('',#12617,#12615,#791,.T.);
#16046=EDGE_CURVE('',#12618,#12619,#8091,.T.);
#16047=EDGE_CURVE('',#12618,#12616,#792,.T.);
#16048=EDGE_CURVE('',#12619,#12617,#793,.T.);
#16049=EDGE_CURVE('',#12620,#12621,#8092,.T.);
#16050=EDGE_CURVE('',#12620,#12618,#794,.T.);
#16051=EDGE_CURVE('',#12621,#12619,#795,.T.);
#16052=EDGE_CURVE('',#12622,#12623,#8093,.T.);
#16053=EDGE_CURVE('',#12622,#12620,#796,.T.);
#16054=EDGE_CURVE('',#12623,#12621,#797,.T.);
#16055=EDGE_CURVE('',#12624,#12625,#8094,.T.);
#16056=EDGE_CURVE('',#12624,#12622,#798,.T.);
#16057=EDGE_CURVE('',#12625,#12623,#799,.T.);
#16058=EDGE_CURVE('',#12626,#12627,#8095,.T.);
#16059=EDGE_CURVE('',#12626,#12624,#800,.T.);
#16060=EDGE_CURVE('',#12627,#12625,#801,.T.);
#16061=EDGE_CURVE('',#12628,#12629,#8096,.T.);
#16062=EDGE_CURVE('',#12628,#12626,#802,.T.);
#16063=EDGE_CURVE('',#12629,#12627,#803,.T.);
#16064=EDGE_CURVE('',#12630,#12631,#8097,.T.);
#16065=EDGE_CURVE('',#12630,#12628,#804,.T.);
#16066=EDGE_CURVE('',#12631,#12629,#805,.T.);
#16067=EDGE_CURVE('',#12632,#12589,#806,.T.);
#16068=EDGE_CURVE('',#12585,#12632,#807,.T.);
#16069=EDGE_CURVE('',#12633,#12541,#808,.T.);
#16070=EDGE_CURVE('',#12633,#12631,#809,.T.);
#16071=EDGE_CURVE('',#12541,#12634,#6324,.T.);
#16072=EDGE_CURVE('',#12634,#12540,#6325,.T.);
#16073=EDGE_CURVE('',#12540,#12635,#810,.T.);
#16074=EDGE_CURVE('',#12635,#12633,#6326,.T.);
#16075=EDGE_CURVE('',#12635,#12630,#811,.T.);
#16076=EDGE_CURVE('',#12588,#12636,#812,.T.);
#16077=EDGE_CURVE('',#12636,#12584,#813,.T.);
#16078=EDGE_CURVE('',#12637,#12638,#130,.T.);
#16079=EDGE_CURVE('',#12639,#12637,#131,.T.);
#16080=EDGE_CURVE('',#12640,#12639,#132,.T.);
#16081=EDGE_CURVE('',#12641,#12640,#133,.T.);
#16082=EDGE_CURVE('',#12642,#12641,#134,.T.);
#16083=EDGE_CURVE('',#12642,#12643,#8098,.T.);
#16084=EDGE_CURVE('',#12643,#12643,#6327,.T.);
#16085=EDGE_CURVE('',#12644,#12642,#135,.T.);
#16086=EDGE_CURVE('',#12638,#12644,#136,.T.);
#16087=EDGE_CURVE('',#12645,#12640,#8099,.T.);
#16088=EDGE_CURVE('',#12645,#12646,#8100,.T.);
#16089=EDGE_CURVE('',#12646,#12641,#8101,.T.);
#16090=EDGE_CURVE('',#12647,#12639,#8102,.T.);
#16091=EDGE_CURVE('',#12647,#12645,#8103,.T.);
#16092=EDGE_CURVE('',#12648,#12637,#8104,.T.);
#16093=EDGE_CURVE('',#12648,#12647,#8105,.T.);
#16094=EDGE_CURVE('',#12649,#12648,#8106,.T.);
#16095=EDGE_CURVE('',#12650,#12649,#8107,.T.);
#16096=EDGE_CURVE('',#12646,#12650,#8108,.T.);
#16097=EDGE_CURVE('',#12651,#12651,#6328,.T.);
#16098=EDGE_CURVE('',#12649,#12638,#8109,.T.);
#16099=EDGE_CURVE('',#12650,#12644,#8110,.T.);
#16100=EDGE_CURVE('',#12652,#12652,#6329,.T.);
#16101=EDGE_CURVE('',#12634,#12652,#8111,.T.);
#16102=EDGE_CURVE('',#12636,#12632,#6330,.T.);
#16103=EDGE_CURVE('',#12653,#12653,#6331,.T.);
#16104=EDGE_CURVE('',#12651,#12653,#8112,.T.);
#22415=ORIENTED_EDGE('',*,*,#15930,.F.);
#22416=ORIENTED_EDGE('',*,*,#15931,.T.);
#22417=ORIENTED_EDGE('',*,*,#15932,.T.);
#22418=ORIENTED_EDGE('',*,*,#15933,.T.);
#22419=ORIENTED_EDGE('',*,*,#15934,.F.);
#22420=ORIENTED_EDGE('',*,*,#15935,.T.);
#22421=ORIENTED_EDGE('',*,*,#15930,.T.);
#22422=ORIENTED_EDGE('',*,*,#15936,.T.);
#22423=ORIENTED_EDGE('',*,*,#15937,.F.);
#22424=ORIENTED_EDGE('',*,*,#15938,.T.);
#22425=ORIENTED_EDGE('',*,*,#15934,.T.);
#22426=ORIENTED_EDGE('',*,*,#15939,.T.);
#22427=ORIENTED_EDGE('',*,*,#15940,.F.);
#22428=ORIENTED_EDGE('',*,*,#15941,.T.);
#22429=ORIENTED_EDGE('',*,*,#15937,.T.);
#22430=ORIENTED_EDGE('',*,*,#15942,.T.);
#22431=ORIENTED_EDGE('',*,*,#15943,.F.);
#22432=ORIENTED_EDGE('',*,*,#15944,.T.);
#22433=ORIENTED_EDGE('',*,*,#15940,.T.);
#22434=ORIENTED_EDGE('',*,*,#15945,.T.);
#22435=ORIENTED_EDGE('',*,*,#15946,.F.);
#22436=ORIENTED_EDGE('',*,*,#15947,.T.);
#22437=ORIENTED_EDGE('',*,*,#15943,.T.);
#22438=ORIENTED_EDGE('',*,*,#15948,.T.);
#22439=ORIENTED_EDGE('',*,*,#15949,.F.);
#22440=ORIENTED_EDGE('',*,*,#15950,.T.);
#22441=ORIENTED_EDGE('',*,*,#15946,.T.);
#22442=ORIENTED_EDGE('',*,*,#15951,.T.);
#22443=ORIENTED_EDGE('',*,*,#15952,.F.);
#22444=ORIENTED_EDGE('',*,*,#15953,.T.);
#22445=ORIENTED_EDGE('',*,*,#15949,.T.);
#22446=ORIENTED_EDGE('',*,*,#15954,.T.);
#22447=ORIENTED_EDGE('',*,*,#15955,.F.);
#22448=ORIENTED_EDGE('',*,*,#15956,.T.);
#22449=ORIENTED_EDGE('',*,*,#15952,.T.);
#22450=ORIENTED_EDGE('',*,*,#15957,.T.);
#22451=ORIENTED_EDGE('',*,*,#15958,.F.);
#22452=ORIENTED_EDGE('',*,*,#15959,.T.);
#22453=ORIENTED_EDGE('',*,*,#15955,.T.);
#22454=ORIENTED_EDGE('',*,*,#15960,.T.);
#22455=ORIENTED_EDGE('',*,*,#15961,.F.);
#22456=ORIENTED_EDGE('',*,*,#15962,.T.);
#22457=ORIENTED_EDGE('',*,*,#15958,.T.);
#22458=ORIENTED_EDGE('',*,*,#15963,.T.);
#22459=ORIENTED_EDGE('',*,*,#15964,.F.);
#22460=ORIENTED_EDGE('',*,*,#15965,.T.);
#22461=ORIENTED_EDGE('',*,*,#15961,.T.);
#22462=ORIENTED_EDGE('',*,*,#15966,.T.);
#22463=ORIENTED_EDGE('',*,*,#15967,.F.);
#22464=ORIENTED_EDGE('',*,*,#15968,.T.);
#22465=ORIENTED_EDGE('',*,*,#15964,.T.);
#22466=ORIENTED_EDGE('',*,*,#15969,.T.);
#22467=ORIENTED_EDGE('',*,*,#15970,.F.);
#22468=ORIENTED_EDGE('',*,*,#15971,.T.);
#22469=ORIENTED_EDGE('',*,*,#15967,.T.);
#22470=ORIENTED_EDGE('',*,*,#15972,.T.);
#22471=ORIENTED_EDGE('',*,*,#15973,.F.);
#22472=ORIENTED_EDGE('',*,*,#15974,.T.);
#22473=ORIENTED_EDGE('',*,*,#15970,.T.);
#22474=ORIENTED_EDGE('',*,*,#15975,.T.);
#22475=ORIENTED_EDGE('',*,*,#15976,.F.);
#22476=ORIENTED_EDGE('',*,*,#15977,.T.);
#22477=ORIENTED_EDGE('',*,*,#15973,.T.);
#22478=ORIENTED_EDGE('',*,*,#15978,.T.);
#22479=ORIENTED_EDGE('',*,*,#15979,.F.);
#22480=ORIENTED_EDGE('',*,*,#15980,.T.);
#22481=ORIENTED_EDGE('',*,*,#15976,.T.);
#22482=ORIENTED_EDGE('',*,*,#15981,.T.);
#22483=ORIENTED_EDGE('',*,*,#15982,.F.);
#22484=ORIENTED_EDGE('',*,*,#15983,.T.);
#22485=ORIENTED_EDGE('',*,*,#15979,.T.);
#22486=ORIENTED_EDGE('',*,*,#15984,.T.);
#22487=ORIENTED_EDGE('',*,*,#15985,.F.);
#22488=ORIENTED_EDGE('',*,*,#15986,.T.);
#22489=ORIENTED_EDGE('',*,*,#15982,.T.);
#22490=ORIENTED_EDGE('',*,*,#15987,.T.);
#22491=ORIENTED_EDGE('',*,*,#15988,.F.);
#22492=ORIENTED_EDGE('',*,*,#15989,.T.);
#22493=ORIENTED_EDGE('',*,*,#15985,.T.);
#22494=ORIENTED_EDGE('',*,*,#15990,.T.);
#22495=ORIENTED_EDGE('',*,*,#15991,.F.);
#22496=ORIENTED_EDGE('',*,*,#15992,.T.);
#22497=ORIENTED_EDGE('',*,*,#15988,.T.);
#22498=ORIENTED_EDGE('',*,*,#15993,.T.);
#22499=ORIENTED_EDGE('',*,*,#15994,.F.);
#22500=ORIENTED_EDGE('',*,*,#15995,.T.);
#22501=ORIENTED_EDGE('',*,*,#15991,.T.);
#22502=ORIENTED_EDGE('',*,*,#15996,.T.);
#22503=ORIENTED_EDGE('',*,*,#15997,.F.);
#22504=ORIENTED_EDGE('',*,*,#15998,.T.);
#22505=ORIENTED_EDGE('',*,*,#15994,.T.);
#22506=ORIENTED_EDGE('',*,*,#15999,.T.);
#22507=ORIENTED_EDGE('',*,*,#16000,.F.);
#22508=ORIENTED_EDGE('',*,*,#16001,.T.);
#22509=ORIENTED_EDGE('',*,*,#16002,.F.);
#22510=ORIENTED_EDGE('',*,*,#16003,.F.);
#22511=ORIENTED_EDGE('',*,*,#16004,.F.);
#22512=ORIENTED_EDGE('',*,*,#16005,.T.);
#22513=ORIENTED_EDGE('',*,*,#16000,.T.);
#22514=ORIENTED_EDGE('',*,*,#16006,.F.);
#22515=ORIENTED_EDGE('',*,*,#16007,.F.);
#22516=ORIENTED_EDGE('',*,*,#16008,.T.);
#22517=ORIENTED_EDGE('',*,*,#16004,.T.);
#22518=ORIENTED_EDGE('',*,*,#16009,.F.);
#22519=ORIENTED_EDGE('',*,*,#16010,.F.);
#22520=ORIENTED_EDGE('',*,*,#16011,.T.);
#22521=ORIENTED_EDGE('',*,*,#16007,.T.);
#22522=ORIENTED_EDGE('',*,*,#16012,.F.);
#22523=ORIENTED_EDGE('',*,*,#16013,.F.);
#22524=ORIENTED_EDGE('',*,*,#16014,.T.);
#22525=ORIENTED_EDGE('',*,*,#16010,.T.);
#22526=ORIENTED_EDGE('',*,*,#16015,.F.);
#22527=ORIENTED_EDGE('',*,*,#16016,.F.);
#22528=ORIENTED_EDGE('',*,*,#16017,.T.);
#22529=ORIENTED_EDGE('',*,*,#16013,.T.);
#22530=ORIENTED_EDGE('',*,*,#16018,.F.);
#22531=ORIENTED_EDGE('',*,*,#16019,.F.);
#22532=ORIENTED_EDGE('',*,*,#16020,.T.);
#22533=ORIENTED_EDGE('',*,*,#16016,.T.);
#22534=ORIENTED_EDGE('',*,*,#16021,.F.);
#22535=ORIENTED_EDGE('',*,*,#16022,.F.);
#22536=ORIENTED_EDGE('',*,*,#16023,.T.);
#22537=ORIENTED_EDGE('',*,*,#16019,.T.);
#22538=ORIENTED_EDGE('',*,*,#16024,.F.);
#22539=ORIENTED_EDGE('',*,*,#16025,.F.);
#22540=ORIENTED_EDGE('',*,*,#16026,.T.);
#22541=ORIENTED_EDGE('',*,*,#16022,.T.);
#22542=ORIENTED_EDGE('',*,*,#16027,.F.);
#22543=ORIENTED_EDGE('',*,*,#16028,.F.);
#22544=ORIENTED_EDGE('',*,*,#16029,.T.);
#22545=ORIENTED_EDGE('',*,*,#16025,.T.);
#22546=ORIENTED_EDGE('',*,*,#16030,.F.);
#22547=ORIENTED_EDGE('',*,*,#16031,.F.);
#22548=ORIENTED_EDGE('',*,*,#16032,.T.);
#22549=ORIENTED_EDGE('',*,*,#16028,.T.);
#22550=ORIENTED_EDGE('',*,*,#16033,.F.);
#22551=ORIENTED_EDGE('',*,*,#16034,.F.);
#22552=ORIENTED_EDGE('',*,*,#16035,.T.);
#22553=ORIENTED_EDGE('',*,*,#16031,.T.);
#22554=ORIENTED_EDGE('',*,*,#16036,.F.);
#22555=ORIENTED_EDGE('',*,*,#16037,.F.);
#22556=ORIENTED_EDGE('',*,*,#16038,.T.);
#22557=ORIENTED_EDGE('',*,*,#16034,.T.);
#22558=ORIENTED_EDGE('',*,*,#16039,.F.);
#22559=ORIENTED_EDGE('',*,*,#16040,.F.);
#22560=ORIENTED_EDGE('',*,*,#16041,.T.);
#22561=ORIENTED_EDGE('',*,*,#16037,.T.);
#22562=ORIENTED_EDGE('',*,*,#16042,.F.);
#22563=ORIENTED_EDGE('',*,*,#16043,.F.);
#22564=ORIENTED_EDGE('',*,*,#16044,.T.);
#22565=ORIENTED_EDGE('',*,*,#16040,.T.);
#22566=ORIENTED_EDGE('',*,*,#16045,.F.);
#22567=ORIENTED_EDGE('',*,*,#16046,.F.);
#22568=ORIENTED_EDGE('',*,*,#16047,.T.);
#22569=ORIENTED_EDGE('',*,*,#16043,.T.);
#22570=ORIENTED_EDGE('',*,*,#16048,.F.);
#22571=ORIENTED_EDGE('',*,*,#16049,.F.);
#22572=ORIENTED_EDGE('',*,*,#16050,.T.);
#22573=ORIENTED_EDGE('',*,*,#16046,.T.);
#22574=ORIENTED_EDGE('',*,*,#16051,.F.);
#22575=ORIENTED_EDGE('',*,*,#16052,.F.);
#22576=ORIENTED_EDGE('',*,*,#16053,.T.);
#22577=ORIENTED_EDGE('',*,*,#16049,.T.);
#22578=ORIENTED_EDGE('',*,*,#16054,.F.);
#22579=ORIENTED_EDGE('',*,*,#16055,.F.);
#22580=ORIENTED_EDGE('',*,*,#16056,.T.);
#22581=ORIENTED_EDGE('',*,*,#16052,.T.);
#22582=ORIENTED_EDGE('',*,*,#16057,.F.);
#22583=ORIENTED_EDGE('',*,*,#16058,.F.);
#22584=ORIENTED_EDGE('',*,*,#16059,.T.);
#22585=ORIENTED_EDGE('',*,*,#16055,.T.);
#22586=ORIENTED_EDGE('',*,*,#16060,.F.);
#22587=ORIENTED_EDGE('',*,*,#16061,.F.);
#22588=ORIENTED_EDGE('',*,*,#16062,.T.);
#22589=ORIENTED_EDGE('',*,*,#16058,.T.);
#22590=ORIENTED_EDGE('',*,*,#16063,.F.);
#22591=ORIENTED_EDGE('',*,*,#16064,.F.);
#22592=ORIENTED_EDGE('',*,*,#16065,.T.);
#22593=ORIENTED_EDGE('',*,*,#16061,.T.);
#22594=ORIENTED_EDGE('',*,*,#16066,.F.);
#22595=ORIENTED_EDGE('',*,*,#16067,.F.);
#22596=ORIENTED_EDGE('',*,*,#16068,.F.);
#22597=ORIENTED_EDGE('',*,*,#15999,.F.);
#22598=ORIENTED_EDGE('',*,*,#15996,.F.);
#22599=ORIENTED_EDGE('',*,*,#15993,.F.);
#22600=ORIENTED_EDGE('',*,*,#15990,.F.);
#22601=ORIENTED_EDGE('',*,*,#15987,.F.);
#22602=ORIENTED_EDGE('',*,*,#15984,.F.);
#22603=ORIENTED_EDGE('',*,*,#15981,.F.);
#22604=ORIENTED_EDGE('',*,*,#15978,.F.);
#22605=ORIENTED_EDGE('',*,*,#15975,.F.);
#22606=ORIENTED_EDGE('',*,*,#15972,.F.);
#22607=ORIENTED_EDGE('',*,*,#15969,.F.);
#22608=ORIENTED_EDGE('',*,*,#15966,.F.);
#22609=ORIENTED_EDGE('',*,*,#15963,.F.);
#22610=ORIENTED_EDGE('',*,*,#15960,.F.);
#22611=ORIENTED_EDGE('',*,*,#15957,.F.);
#22612=ORIENTED_EDGE('',*,*,#15954,.F.);
#22613=ORIENTED_EDGE('',*,*,#15951,.F.);
#22614=ORIENTED_EDGE('',*,*,#15948,.F.);
#22615=ORIENTED_EDGE('',*,*,#15945,.F.);
#22616=ORIENTED_EDGE('',*,*,#15942,.F.);
#22617=ORIENTED_EDGE('',*,*,#15939,.F.);
#22618=ORIENTED_EDGE('',*,*,#15936,.F.);
#22619=ORIENTED_EDGE('',*,*,#15933,.F.);
#22620=ORIENTED_EDGE('',*,*,#16069,.F.);
#22621=ORIENTED_EDGE('',*,*,#16070,.T.);
#22622=ORIENTED_EDGE('',*,*,#16066,.T.);
#22623=ORIENTED_EDGE('',*,*,#16063,.T.);
#22624=ORIENTED_EDGE('',*,*,#16060,.T.);
#22625=ORIENTED_EDGE('',*,*,#16057,.T.);
#22626=ORIENTED_EDGE('',*,*,#16054,.T.);
#22627=ORIENTED_EDGE('',*,*,#16051,.T.);
#22628=ORIENTED_EDGE('',*,*,#16048,.T.);
#22629=ORIENTED_EDGE('',*,*,#16045,.T.);
#22630=ORIENTED_EDGE('',*,*,#16042,.T.);
#22631=ORIENTED_EDGE('',*,*,#16039,.T.);
#22632=ORIENTED_EDGE('',*,*,#16036,.T.);
#22633=ORIENTED_EDGE('',*,*,#16033,.T.);
#22634=ORIENTED_EDGE('',*,*,#16030,.T.);
#22635=ORIENTED_EDGE('',*,*,#16027,.T.);
#22636=ORIENTED_EDGE('',*,*,#16024,.T.);
#22637=ORIENTED_EDGE('',*,*,#16021,.T.);
#22638=ORIENTED_EDGE('',*,*,#16018,.T.);
#22639=ORIENTED_EDGE('',*,*,#16015,.T.);
#22640=ORIENTED_EDGE('',*,*,#16012,.T.);
#22641=ORIENTED_EDGE('',*,*,#16009,.T.);
#22642=ORIENTED_EDGE('',*,*,#16006,.T.);
#22643=ORIENTED_EDGE('',*,*,#16003,.T.);
#22644=ORIENTED_EDGE('',*,*,#16071,.T.);
#22645=ORIENTED_EDGE('',*,*,#16072,.T.);
#22646=ORIENTED_EDGE('',*,*,#16073,.T.);
#22647=ORIENTED_EDGE('',*,*,#16074,.T.);
#22648=ORIENTED_EDGE('',*,*,#16069,.T.);
#22649=ORIENTED_EDGE('',*,*,#16064,.T.);
#22650=ORIENTED_EDGE('',*,*,#16070,.F.);
#22651=ORIENTED_EDGE('',*,*,#16074,.F.);
#22652=ORIENTED_EDGE('',*,*,#16075,.T.);
#22653=ORIENTED_EDGE('',*,*,#16076,.F.);
#22654=ORIENTED_EDGE('',*,*,#16001,.F.);
#22655=ORIENTED_EDGE('',*,*,#16005,.F.);
#22656=ORIENTED_EDGE('',*,*,#16008,.F.);
#22657=ORIENTED_EDGE('',*,*,#16011,.F.);
#22658=ORIENTED_EDGE('',*,*,#16014,.F.);
#22659=ORIENTED_EDGE('',*,*,#16017,.F.);
#22660=ORIENTED_EDGE('',*,*,#16020,.F.);
#22661=ORIENTED_EDGE('',*,*,#16023,.F.);
#22662=ORIENTED_EDGE('',*,*,#16026,.F.);
#22663=ORIENTED_EDGE('',*,*,#16029,.F.);
#22664=ORIENTED_EDGE('',*,*,#16032,.F.);
#22665=ORIENTED_EDGE('',*,*,#16035,.F.);
#22666=ORIENTED_EDGE('',*,*,#16038,.F.);
#22667=ORIENTED_EDGE('',*,*,#16041,.F.);
#22668=ORIENTED_EDGE('',*,*,#16044,.F.);
#22669=ORIENTED_EDGE('',*,*,#16047,.F.);
#22670=ORIENTED_EDGE('',*,*,#16050,.F.);
#22671=ORIENTED_EDGE('',*,*,#16053,.F.);
#22672=ORIENTED_EDGE('',*,*,#16056,.F.);
#22673=ORIENTED_EDGE('',*,*,#16059,.F.);
#22674=ORIENTED_EDGE('',*,*,#16062,.F.);
#22675=ORIENTED_EDGE('',*,*,#16065,.F.);
#22676=ORIENTED_EDGE('',*,*,#16075,.F.);
#22677=ORIENTED_EDGE('',*,*,#16073,.F.);
#22678=ORIENTED_EDGE('',*,*,#15931,.F.);
#22679=ORIENTED_EDGE('',*,*,#15935,.F.);
#22680=ORIENTED_EDGE('',*,*,#15938,.F.);
#22681=ORIENTED_EDGE('',*,*,#15941,.F.);
#22682=ORIENTED_EDGE('',*,*,#15944,.F.);
#22683=ORIENTED_EDGE('',*,*,#15947,.F.);
#22684=ORIENTED_EDGE('',*,*,#15950,.F.);
#22685=ORIENTED_EDGE('',*,*,#15953,.F.);
#22686=ORIENTED_EDGE('',*,*,#15956,.F.);
#22687=ORIENTED_EDGE('',*,*,#15959,.F.);
#22688=ORIENTED_EDGE('',*,*,#15962,.F.);
#22689=ORIENTED_EDGE('',*,*,#15965,.F.);
#22690=ORIENTED_EDGE('',*,*,#15968,.F.);
#22691=ORIENTED_EDGE('',*,*,#15971,.F.);
#22692=ORIENTED_EDGE('',*,*,#15974,.F.);
#22693=ORIENTED_EDGE('',*,*,#15977,.F.);
#22694=ORIENTED_EDGE('',*,*,#15980,.F.);
#22695=ORIENTED_EDGE('',*,*,#15983,.F.);
#22696=ORIENTED_EDGE('',*,*,#15986,.F.);
#22697=ORIENTED_EDGE('',*,*,#15989,.F.);
#22698=ORIENTED_EDGE('',*,*,#15992,.F.);
#22699=ORIENTED_EDGE('',*,*,#15995,.F.);
#22700=ORIENTED_EDGE('',*,*,#15998,.F.);
#22701=ORIENTED_EDGE('',*,*,#16077,.F.);
#22702=ORIENTED_EDGE('',*,*,#16078,.F.);
#22703=ORIENTED_EDGE('',*,*,#16079,.F.);
#22704=ORIENTED_EDGE('',*,*,#16080,.F.);
#22705=ORIENTED_EDGE('',*,*,#16081,.F.);
#22706=ORIENTED_EDGE('',*,*,#16082,.F.);
#22707=ORIENTED_EDGE('',*,*,#16083,.T.);
#22708=ORIENTED_EDGE('',*,*,#16084,.F.);
#22709=ORIENTED_EDGE('',*,*,#16083,.F.);
#22710=ORIENTED_EDGE('',*,*,#16085,.F.);
#22711=ORIENTED_EDGE('',*,*,#16086,.F.);
#22712=ORIENTED_EDGE('',*,*,#16081,.T.);
#22713=ORIENTED_EDGE('',*,*,#16087,.F.);
#22714=ORIENTED_EDGE('',*,*,#16088,.T.);
#22715=ORIENTED_EDGE('',*,*,#16089,.T.);
#22716=ORIENTED_EDGE('',*,*,#16080,.T.);
#22717=ORIENTED_EDGE('',*,*,#16090,.F.);
#22718=ORIENTED_EDGE('',*,*,#16091,.T.);
#22719=ORIENTED_EDGE('',*,*,#16087,.T.);
#22720=ORIENTED_EDGE('',*,*,#16079,.T.);
#22721=ORIENTED_EDGE('',*,*,#16092,.F.);
#22722=ORIENTED_EDGE('',*,*,#16093,.T.);
#22723=ORIENTED_EDGE('',*,*,#16090,.T.);
#22724=ORIENTED_EDGE('',*,*,#16093,.F.);
#22725=ORIENTED_EDGE('',*,*,#16094,.F.);
#22726=ORIENTED_EDGE('',*,*,#16095,.F.);
#22727=ORIENTED_EDGE('',*,*,#16096,.F.);
#22728=ORIENTED_EDGE('',*,*,#16088,.F.);
#22729=ORIENTED_EDGE('',*,*,#16091,.F.);
#22730=ORIENTED_EDGE('',*,*,#16097,.T.);
#22731=ORIENTED_EDGE('',*,*,#16078,.T.);
#22732=ORIENTED_EDGE('',*,*,#16098,.F.);
#22733=ORIENTED_EDGE('',*,*,#16094,.T.);
#22734=ORIENTED_EDGE('',*,*,#16092,.T.);
#22735=ORIENTED_EDGE('',*,*,#16086,.T.);
#22736=ORIENTED_EDGE('',*,*,#16099,.F.);
#22737=ORIENTED_EDGE('',*,*,#16095,.T.);
#22738=ORIENTED_EDGE('',*,*,#16098,.T.);
#22739=ORIENTED_EDGE('',*,*,#16085,.T.);
#22740=ORIENTED_EDGE('',*,*,#16082,.T.);
#22741=ORIENTED_EDGE('',*,*,#16089,.F.);
#22742=ORIENTED_EDGE('',*,*,#16096,.T.);
#22743=ORIENTED_EDGE('',*,*,#16099,.T.);
#22744=ORIENTED_EDGE('',*,*,#16084,.T.);
#22745=ORIENTED_EDGE('',*,*,#16100,.F.);
#22746=ORIENTED_EDGE('',*,*,#16071,.F.);
#22747=ORIENTED_EDGE('',*,*,#15932,.F.);
#22748=ORIENTED_EDGE('',*,*,#16072,.F.);
#22749=ORIENTED_EDGE('',*,*,#16101,.T.);
#22750=ORIENTED_EDGE('',*,*,#16100,.T.);
#22751=ORIENTED_EDGE('',*,*,#16101,.F.);
#22752=ORIENTED_EDGE('',*,*,#15997,.T.);
#22753=ORIENTED_EDGE('',*,*,#16068,.T.);
#22754=ORIENTED_EDGE('',*,*,#16102,.F.);
#22755=ORIENTED_EDGE('',*,*,#16077,.T.);
#22756=ORIENTED_EDGE('',*,*,#16103,.F.);
#22757=ORIENTED_EDGE('',*,*,#16102,.T.);
#22758=ORIENTED_EDGE('',*,*,#16067,.T.);
#22759=ORIENTED_EDGE('',*,*,#16002,.T.);
#22760=ORIENTED_EDGE('',*,*,#16076,.T.);
#22761=ORIENTED_EDGE('',*,*,#16097,.F.);
#22762=ORIENTED_EDGE('',*,*,#16104,.T.);
#22763=ORIENTED_EDGE('',*,*,#16103,.T.);
#22764=ORIENTED_EDGE('',*,*,#16104,.F.);
#25102=CONICAL_SURFACE('',#28613,0.972115242270663,1.0471975511966);
#25103=CONICAL_SURFACE('',#28626,0.57,0.785398163397447);
#26174=ADVANCED_FACE('',(#3586),#1414,.T.);
#26175=ADVANCED_FACE('',(#3587),#1415,.T.);
#26176=ADVANCED_FACE('',(#3588),#1416,.T.);
#26177=ADVANCED_FACE('',(#3589),#1417,.T.);
#26178=ADVANCED_FACE('',(#3590),#1418,.T.);
#26179=ADVANCED_FACE('',(#3591),#1419,.T.);
#26180=ADVANCED_FACE('',(#3592),#1420,.T.);
#26181=ADVANCED_FACE('',(#3593),#1421,.T.);
#26182=ADVANCED_FACE('',(#3594),#1422,.T.);
#26183=ADVANCED_FACE('',(#3595),#1423,.T.);
#26184=ADVANCED_FACE('',(#3596),#1424,.T.);
#26185=ADVANCED_FACE('',(#3597),#1425,.T.);
#26186=ADVANCED_FACE('',(#3598),#1426,.T.);
#26187=ADVANCED_FACE('',(#3599),#1427,.T.);
#26188=ADVANCED_FACE('',(#3600),#1428,.T.);
#26189=ADVANCED_FACE('',(#3601),#1429,.T.);
#26190=ADVANCED_FACE('',(#3602),#1430,.T.);
#26191=ADVANCED_FACE('',(#3603),#1431,.T.);
#26192=ADVANCED_FACE('',(#3604),#1432,.T.);
#26193=ADVANCED_FACE('',(#3605),#1433,.T.);
#26194=ADVANCED_FACE('',(#3606),#1434,.T.);
#26195=ADVANCED_FACE('',(#3607),#1435,.T.);
#26196=ADVANCED_FACE('',(#3608),#1436,.T.);
#26197=ADVANCED_FACE('',(#3609),#1437,.T.);
#26198=ADVANCED_FACE('',(#3610),#1438,.T.);
#26199=ADVANCED_FACE('',(#3611),#1439,.T.);
#26200=ADVANCED_FACE('',(#3612),#1440,.T.);
#26201=ADVANCED_FACE('',(#3613),#1441,.T.);
#26202=ADVANCED_FACE('',(#3614),#1442,.T.);
#26203=ADVANCED_FACE('',(#3615),#1443,.T.);
#26204=ADVANCED_FACE('',(#3616),#1444,.T.);
#26205=ADVANCED_FACE('',(#3617),#1445,.T.);
#26206=ADVANCED_FACE('',(#3618),#1446,.T.);
#26207=ADVANCED_FACE('',(#3619),#1447,.T.);
#26208=ADVANCED_FACE('',(#3620),#1448,.T.);
#26209=ADVANCED_FACE('',(#3621),#1449,.T.);
#26210=ADVANCED_FACE('',(#3622),#1450,.T.);
#26211=ADVANCED_FACE('',(#3623),#1451,.T.);
#26212=ADVANCED_FACE('',(#3624),#1452,.T.);
#26213=ADVANCED_FACE('',(#3625),#1453,.T.);
#26214=ADVANCED_FACE('',(#3626),#1454,.T.);
#26215=ADVANCED_FACE('',(#3627),#1455,.T.);
#26216=ADVANCED_FACE('',(#3628),#1456,.T.);
#26217=ADVANCED_FACE('',(#3629),#1457,.T.);
#26218=ADVANCED_FACE('',(#3630),#1458,.T.);
#26219=ADVANCED_FACE('',(#3631),#168,.F.);
#26220=ADVANCED_FACE('',(#3632),#2191,.T.);
#26221=ADVANCED_FACE('',(#3633),#1459,.T.);
#26222=ADVANCED_FACE('',(#3634),#169,.F.);
#26223=ADVANCED_FACE('',(#3635),#25102,.T.);
#26224=ADVANCED_FACE('',(#3636),#2192,.T.);
#26225=ADVANCED_FACE('',(#3637),#2193,.T.);
#26226=ADVANCED_FACE('',(#3638),#2194,.T.);
#26227=ADVANCED_FACE('',(#3639,#1650),#2195,.F.);
#26228=ADVANCED_FACE('',(#3640),#2196,.T.);
#26229=ADVANCED_FACE('',(#3641),#2197,.T.);
#26230=ADVANCED_FACE('',(#3642),#2198,.T.);
#26231=ADVANCED_FACE('',(#3643),#2199,.T.);
#26232=ADVANCED_FACE('',(#3644),#2200,.T.);
#26233=ADVANCED_FACE('',(#3645),#25103,.T.);
#26234=ADVANCED_FACE('',(#3646),#1460,.T.);
#26235=ADVANCED_FACE('',(#3647,#1651),#2201,.T.);
#26236=ADVANCED_FACE('',(#3648),#1461,.T.);
#26681=CLOSED_SHELL('',(#26174,#26175,#26176,#26177,#26178,#26179,#26180,
#26181,#26182,#26183,#26184,#26185,#26186,#26187,#26188,#26189,#26190,#26191,
#26192,#26193,#26194,#26195,#26196,#26197,#26198,#26199,#26200,#26201,#26202,
#26203,#26204,#26205,#26206,#26207,#26208,#26209,#26210,#26211,#26212,#26213,
#26214,#26215,#26216,#26217,#26218,#26219,#26220,#26221,#26222,#26223,#26224,
#26225,#26226,#26227,#26228,#26229,#26230,#26231,#26232,#26233,#26234,#26235,
#26236));
#28560=AXIS2_PLACEMENT_3D('',#63542,#34116,#34117);
#28561=AXIS2_PLACEMENT_3D('',#63543,#34118,#34119);
#28562=AXIS2_PLACEMENT_3D('',#63565,#34121,#34122);
#28563=AXIS2_PLACEMENT_3D('',#63576,#34123,#34124);
#28564=AXIS2_PLACEMENT_3D('',#63660,#34126,#34127);
#28565=AXIS2_PLACEMENT_3D('',#63750,#34129,#34130);
#28566=AXIS2_PLACEMENT_3D('',#63834,#34132,#34133);
#28567=AXIS2_PLACEMENT_3D('',#63924,#34135,#34136);
#28568=AXIS2_PLACEMENT_3D('',#64014,#34138,#34139);
#28569=AXIS2_PLACEMENT_3D('',#64098,#34141,#34142);
#28570=AXIS2_PLACEMENT_3D('',#64188,#34144,#34145);
#28571=AXIS2_PLACEMENT_3D('',#64272,#34147,#34148);
#28572=AXIS2_PLACEMENT_3D('',#64362,#34150,#34151);
#28573=AXIS2_PLACEMENT_3D('',#64452,#34153,#34154);
#28574=AXIS2_PLACEMENT_3D('',#64536,#34156,#34157);
#28575=AXIS2_PLACEMENT_3D('',#64626,#34159,#34160);
#28576=AXIS2_PLACEMENT_3D('',#64710,#34162,#34163);
#28577=AXIS2_PLACEMENT_3D('',#64800,#34165,#34166);
#28578=AXIS2_PLACEMENT_3D('',#64884,#34168,#34169);
#28579=AXIS2_PLACEMENT_3D('',#64974,#34171,#34172);
#28580=AXIS2_PLACEMENT_3D('',#65064,#34174,#34175);
#28581=AXIS2_PLACEMENT_3D('',#65148,#34177,#34178);
#28582=AXIS2_PLACEMENT_3D('',#65238,#34180,#34181);
#28583=AXIS2_PLACEMENT_3D('',#65322,#34183,#34184);
#28584=AXIS2_PLACEMENT_3D('',#65412,#34186,#34187);
#28585=AXIS2_PLACEMENT_3D('',#65499,#34189,#34190);
#28586=AXIS2_PLACEMENT_3D('',#65520,#34192,#34193);
#28587=AXIS2_PLACEMENT_3D('',#65533,#34194,#34195);
#28588=AXIS2_PLACEMENT_3D('',#65571,#34197,#34198);
#28589=AXIS2_PLACEMENT_3D('',#65608,#34200,#34201);
#28590=AXIS2_PLACEMENT_3D('',#65645,#34203,#34204);
#28591=AXIS2_PLACEMENT_3D('',#65682,#34206,#34207);
#28592=AXIS2_PLACEMENT_3D('',#65719,#34209,#34210);
#28593=AXIS2_PLACEMENT_3D('',#65757,#34212,#34213);
#28594=AXIS2_PLACEMENT_3D('',#65794,#34215,#34216);
#28595=AXIS2_PLACEMENT_3D('',#65831,#34218,#34219);
#28596=AXIS2_PLACEMENT_3D('',#65868,#34221,#34222);
#28597=AXIS2_PLACEMENT_3D('',#65905,#34224,#34225);
#28598=AXIS2_PLACEMENT_3D('',#65942,#34227,#34228);
#28599=AXIS2_PLACEMENT_3D('',#65979,#34230,#34231);
#28600=AXIS2_PLACEMENT_3D('',#66017,#34233,#34234);
#28601=AXIS2_PLACEMENT_3D('',#66054,#34236,#34237);
#28602=AXIS2_PLACEMENT_3D('',#66091,#34239,#34240);
#28603=AXIS2_PLACEMENT_3D('',#66128,#34242,#34243);
#28604=AXIS2_PLACEMENT_3D('',#66165,#34245,#34246);
#28605=AXIS2_PLACEMENT_3D('',#66203,#34248,#34249);
#28606=AXIS2_PLACEMENT_3D('',#66240,#34251,#34252);
#28607=AXIS2_PLACEMENT_3D('',#66277,#34254,#34255);
#28608=AXIS2_PLACEMENT_3D('',#67653,#34257,#34258);
#28609=AXIS2_PLACEMENT_3D('',#67655,#34259,#34260);
#28610=AXIS2_PLACEMENT_3D('',#67656,#34261,#34262);
#28611=AXIS2_PLACEMENT_3D('',#67728,#34263,#34264);
#28612=AXIS2_PLACEMENT_3D('',#67729,#34265,#34266);
#28613=AXIS2_PLACEMENT_3D('',#68993,#34267,#34268);
#28614=AXIS2_PLACEMENT_3D('',#69017,#34270,#34271);
#28615=AXIS2_PLACEMENT_3D('',#69025,#34272,#34273);
#28616=AXIS2_PLACEMENT_3D('',#69031,#34277,#34278);
#28617=AXIS2_PLACEMENT_3D('',#69035,#34281,#34282);
#28618=AXIS2_PLACEMENT_3D('',#69039,#34285,#34286);
#28619=AXIS2_PLACEMENT_3D('',#69046,#34290,#34291);
#28620=AXIS2_PLACEMENT_3D('',#69047,#34292,#34293);
#28621=AXIS2_PLACEMENT_3D('',#69049,#34295,#34296);
#28622=AXIS2_PLACEMENT_3D('',#69051,#34298,#34299);
#28623=AXIS2_PLACEMENT_3D('',#69052,#34300,#34301);
#28624=AXIS2_PLACEMENT_3D('',#69053,#34302,#34303);
#28625=AXIS2_PLACEMENT_3D('',#69055,#34304,#34305);
#28626=AXIS2_PLACEMENT_3D('',#69056,#34306,#34307);
#28627=AXIS2_PLACEMENT_3D('',#69058,#34309,#34310);
#28628=AXIS2_PLACEMENT_3D('',#69059,#34311,#34312);
#28629=AXIS2_PLACEMENT_3D('',#69060,#34313,#34314);
#28630=AXIS2_PLACEMENT_3D('',#69062,#34315,#34316);
#28631=AXIS2_PLACEMENT_3D('',#69063,#34317,#34318);
#34116=DIRECTION('axis',(0.,0.,1.));
#34117=DIRECTION('refdir',(1.,0.,0.));
#34118=DIRECTION('center_axis',(0.,0.,1.));
#34119=DIRECTION('ref_axis',(1.,0.,0.));
#34120=DIRECTION('',(0.,0.,-1.));
#34121=DIRECTION('center_axis',(0.,0.,1.));
#34122=DIRECTION('ref_axis',(1.,0.,0.));
#34123=DIRECTION('center_axis',(0.,0.,1.));
#34124=DIRECTION('ref_axis',(1.,0.,0.));
#34125=DIRECTION('',(0.,0.,-1.));
#34126=DIRECTION('center_axis',(0.,0.,1.));
#34127=DIRECTION('ref_axis',(1.,0.,0.));
#34128=DIRECTION('',(0.,0.,-1.));
#34129=DIRECTION('center_axis',(0.,0.,1.));
#34130=DIRECTION('ref_axis',(1.,0.,0.));
#34131=DIRECTION('',(0.,0.,-1.));
#34132=DIRECTION('center_axis',(0.,0.,1.));
#34133=DIRECTION('ref_axis',(1.,0.,0.));
#34134=DIRECTION('',(0.,0.,-1.));
#34135=DIRECTION('center_axis',(0.,0.,1.));
#34136=DIRECTION('ref_axis',(1.,0.,0.));
#34137=DIRECTION('',(0.,0.,-1.));
#34138=DIRECTION('center_axis',(0.,0.,1.));
#34139=DIRECTION('ref_axis',(1.,0.,0.));
#34140=DIRECTION('',(0.,0.,-1.));
#34141=DIRECTION('center_axis',(0.,0.,1.));
#34142=DIRECTION('ref_axis',(1.,0.,0.));
#34143=DIRECTION('',(0.,0.,-1.));
#34144=DIRECTION('center_axis',(0.,0.,1.));
#34145=DIRECTION('ref_axis',(1.,0.,0.));
#34146=DIRECTION('',(0.,0.,-1.));
#34147=DIRECTION('center_axis',(0.,0.,1.));
#34148=DIRECTION('ref_axis',(1.,0.,0.));
#34149=DIRECTION('',(0.,0.,-1.));
#34150=DIRECTION('center_axis',(0.,0.,1.));
#34151=DIRECTION('ref_axis',(1.,0.,0.));
#34152=DIRECTION('',(0.,0.,-1.));
#34153=DIRECTION('center_axis',(0.,0.,1.));
#34154=DIRECTION('ref_axis',(1.,0.,0.));
#34155=DIRECTION('',(0.,0.,-1.));
#34156=DIRECTION('center_axis',(0.,0.,1.));
#34157=DIRECTION('ref_axis',(1.,0.,0.));
#34158=DIRECTION('',(0.,0.,-1.));
#34159=DIRECTION('center_axis',(0.,0.,1.));
#34160=DIRECTION('ref_axis',(1.,0.,0.));
#34161=DIRECTION('',(0.,0.,-1.));
#34162=DIRECTION('center_axis',(0.,0.,1.));
#34163=DIRECTION('ref_axis',(1.,0.,0.));
#34164=DIRECTION('',(0.,0.,-1.));
#34165=DIRECTION('center_axis',(0.,0.,1.));
#34166=DIRECTION('ref_axis',(1.,0.,0.));
#34167=DIRECTION('',(0.,0.,-1.));
#34168=DIRECTION('center_axis',(0.,0.,1.));
#34169=DIRECTION('ref_axis',(1.,0.,0.));
#34170=DIRECTION('',(0.,0.,-1.));
#34171=DIRECTION('center_axis',(0.,0.,1.));
#34172=DIRECTION('ref_axis',(1.,0.,0.));
#34173=DIRECTION('',(0.,0.,-1.));
#34174=DIRECTION('center_axis',(0.,0.,1.));
#34175=DIRECTION('ref_axis',(1.,0.,0.));
#34176=DIRECTION('',(0.,0.,-1.));
#34177=DIRECTION('center_axis',(0.,0.,1.));
#34178=DIRECTION('ref_axis',(1.,0.,0.));
#34179=DIRECTION('',(0.,0.,-1.));
#34180=DIRECTION('center_axis',(0.,0.,1.));
#34181=DIRECTION('ref_axis',(1.,0.,0.));
#34182=DIRECTION('',(0.,0.,-1.));
#34183=DIRECTION('center_axis',(0.,0.,1.));
#34184=DIRECTION('ref_axis',(1.,0.,0.));
#34185=DIRECTION('',(0.,0.,-1.));
#34186=DIRECTION('center_axis',(0.,0.,1.));
#34187=DIRECTION('ref_axis',(1.,0.,0.));
#34188=DIRECTION('',(0.,0.,-1.));
#34189=DIRECTION('center_axis',(0.,0.,1.));
#34190=DIRECTION('ref_axis',(0.960739260171429,-0.277452831964742,0.));
#34191=DIRECTION('',(0.,0.,1.));
#34192=DIRECTION('center_axis',(0.,0.,1.));
#34193=DIRECTION('ref_axis',(1.,2.16645715620364E-14,0.));
#34194=DIRECTION('center_axis',(0.,0.,1.));
#34195=DIRECTION('ref_axis',(1.,2.16645715620364E-14,0.));
#34196=DIRECTION('',(0.,0.,1.));
#34197=DIRECTION('center_axis',(0.,0.,1.));
#34198=DIRECTION('ref_axis',(1.,2.16645715620364E-14,0.));
#34199=DIRECTION('',(0.,0.,1.));
#34200=DIRECTION('center_axis',(0.,0.,1.));
#34201=DIRECTION('ref_axis',(1.,2.16645715620364E-14,0.));
#34202=DIRECTION('',(0.,0.,1.));
#34203=DIRECTION('center_axis',(0.,0.,1.));
#34204=DIRECTION('ref_axis',(1.,2.16645715620364E-14,0.));
#34205=DIRECTION('',(0.,0.,1.));
#34206=DIRECTION('center_axis',(0.,0.,1.));
#34207=DIRECTION('ref_axis',(1.,2.16645715620364E-14,0.));
#34208=DIRECTION('',(0.,0.,1.));
#34209=DIRECTION('center_axis',(0.,0.,1.));
#34210=DIRECTION('ref_axis',(1.,2.16645715620364E-14,0.));
#34211=DIRECTION('',(0.,0.,1.));
#34212=DIRECTION('center_axis',(0.,0.,1.));
#34213=DIRECTION('ref_axis',(1.,2.16645715620364E-14,0.));
#34214=DIRECTION('',(0.,0.,1.));
#34215=DIRECTION('center_axis',(0.,0.,1.));
#34216=DIRECTION('ref_axis',(1.,2.16645715620364E-14,0.));
#34217=DIRECTION('',(0.,0.,1.));
#34218=DIRECTION('center_axis',(0.,0.,1.));
#34219=DIRECTION('ref_axis',(1.,2.16645715620364E-14,0.));
#34220=DIRECTION('',(0.,0.,1.));
#34221=DIRECTION('center_axis',(0.,0.,1.));
#34222=DIRECTION('ref_axis',(1.,2.16645715620364E-14,0.));
#34223=DIRECTION('',(0.,0.,1.));
#34224=DIRECTION('center_axis',(0.,0.,1.));
#34225=DIRECTION('ref_axis',(1.,2.16645715620364E-14,0.));
#34226=DIRECTION('',(0.,0.,1.));
#34227=DIRECTION('center_axis',(0.,0.,1.));
#34228=DIRECTION('ref_axis',(1.,2.16645715620364E-14,0.));
#34229=DIRECTION('',(0.,0.,1.));
#34230=DIRECTION('center_axis',(0.,0.,1.));
#34231=DIRECTION('ref_axis',(1.,2.16645715620364E-14,0.));
#34232=DIRECTION('',(0.,0.,1.));
#34233=DIRECTION('center_axis',(0.,0.,1.));
#34234=DIRECTION('ref_axis',(1.,2.16645715620364E-14,0.));
#34235=DIRECTION('',(0.,0.,1.));
#34236=DIRECTION('center_axis',(0.,0.,1.));
#34237=DIRECTION('ref_axis',(1.,2.16645715620364E-14,0.));
#34238=DIRECTION('',(0.,0.,1.));
#34239=DIRECTION('center_axis',(0.,0.,1.));
#34240=DIRECTION('ref_axis',(1.,2.16645715620364E-14,0.));
#34241=DIRECTION('',(0.,0.,1.));
#34242=DIRECTION('center_axis',(0.,0.,1.));
#34243=DIRECTION('ref_axis',(1.,2.16645715620364E-14,0.));
#34244=DIRECTION('',(0.,0.,1.));
#34245=DIRECTION('center_axis',(0.,0.,1.));
#34246=DIRECTION('ref_axis',(1.,2.16645715620364E-14,0.));
#34247=DIRECTION('',(0.,0.,1.));
#34248=DIRECTION('center_axis',(0.,0.,1.));
#34249=DIRECTION('ref_axis',(1.,2.16645715620364E-14,0.));
#34250=DIRECTION('',(0.,0.,1.));
#34251=DIRECTION('center_axis',(0.,0.,1.));
#34252=DIRECTION('ref_axis',(1.,2.16645715620364E-14,0.));
#34253=DIRECTION('',(0.,0.,1.));
#34254=DIRECTION('center_axis',(0.,0.,1.));
#34255=DIRECTION('ref_axis',(1.,2.16645715620364E-14,0.));
#34256=DIRECTION('',(0.,0.,1.));
#34257=DIRECTION('center_axis',(0.,0.,1.));
#34258=DIRECTION('ref_axis',(1.,0.,0.));
#34259=DIRECTION('center_axis',(0.,0.,1.));
#34260=DIRECTION('ref_axis',(1.,0.,0.));
#34261=DIRECTION('center_axis',(0.,0.,1.));
#34262=DIRECTION('ref_axis',(1.,0.,0.));
#34263=DIRECTION('center_axis',(0.,0.,-1.));
#34264=DIRECTION('ref_axis',(1.,2.16645715620364E-14,0.));
#34265=DIRECTION('center_axis',(0.,0.,1.));
#34266=DIRECTION('ref_axis',(0.889074692313968,0.457762156022997,0.));
#34267=DIRECTION('center_axis',(0.,0.,-1.));
#34268=DIRECTION('ref_axis',(1.,0.,0.));
#34269=DIRECTION('',(0.866025403784439,1.06057523872491E-16,0.5));
#34270=DIRECTION('center_axis',(0.,0.,1.));
#34271=DIRECTION('ref_axis',(1.,0.,0.));
#34272=DIRECTION('center_axis',(-0.5,0.866025403784439,0.));
#34273=DIRECTION('ref_axis',(-0.866025403784439,-0.5,0.));
#34274=DIRECTION('',(0.,0.,1.));
#34275=DIRECTION('',(-0.866025403784439,-0.5,0.));
#34276=DIRECTION('',(0.,0.,1.));
#34277=DIRECTION('center_axis',(0.5,0.866025403784439,0.));
#34278=DIRECTION('ref_axis',(-0.866025403784439,0.5,0.));
#34279=DIRECTION('',(0.,0.,1.));
#34280=DIRECTION('',(-0.866025403784439,0.5,0.));
#34281=DIRECTION('center_axis',(1.,-2.13662520709285E-16,0.));
#34282=DIRECTION('ref_axis',(2.13662520709285E-16,1.,0.));
#34283=DIRECTION('',(0.,0.,1.));
#34284=DIRECTION('',(2.13662520709285E-16,1.,0.));
#34285=DIRECTION('center_axis',(0.,0.,1.));
#34286=DIRECTION('ref_axis',(1.,0.,0.));
#34287=DIRECTION('',(0.866025403784439,0.5,0.));
#34288=DIRECTION('',(0.866025403784439,-0.5,0.));
#34289=DIRECTION('',(0.,-1.,0.));
#34290=DIRECTION('center_axis',(0.,0.,1.));
#34291=DIRECTION('ref_axis',(1.,0.,0.));
#34292=DIRECTION('center_axis',(0.5,-0.866025403784439,0.));
#34293=DIRECTION('ref_axis',(0.866025403784439,0.5,0.));
#34294=DIRECTION('',(0.,0.,1.));
#34295=DIRECTION('center_axis',(-0.5,-0.866025403784439,0.));
#34296=DIRECTION('ref_axis',(0.866025403784439,-0.5,0.));
#34297=DIRECTION('',(0.,0.,1.));
#34298=DIRECTION('center_axis',(-1.,0.,0.));
#34299=DIRECTION('ref_axis',(0.,-1.,0.));
#34300=DIRECTION('center_axis',(0.,0.,1.));
#34301=DIRECTION('ref_axis',(1.,0.,0.));
#34302=DIRECTION('center_axis',(0.,0.,-1.));
#34303=DIRECTION('ref_axis',(-1.,0.,0.));
#34304=DIRECTION('center_axis',(0.,0.,1.));
#34305=DIRECTION('ref_axis',(1.,0.,0.));
#34306=DIRECTION('center_axis',(0.,0.,1.));
#34307=DIRECTION('ref_axis',(1.,0.,0.));
#34308=DIRECTION('',(0.707106781186547,8.65956056235493E-17,-0.707106781186548));
#34309=DIRECTION('center_axis',(0.,0.,1.));
#34310=DIRECTION('ref_axis',(-0.357033271046359,-0.934091667539079,0.));
#34311=DIRECTION('center_axis',(0.,0.,1.));
#34312=DIRECTION('ref_axis',(1.,0.,0.));
#34313=DIRECTION('center_axis',(0.,0.,-1.));
#34314=DIRECTION('ref_axis',(-1.,0.,0.));
#34315=DIRECTION('center_axis',(0.,0.,1.));
#34316=DIRECTION('ref_axis',(1.,0.,0.));
#34317=DIRECTION('center_axis',(0.,0.,1.));
#34318=DIRECTION('ref_axis',(1.,0.,0.));
#34319=DIRECTION('',(0.,0.,-1.));
#63542=CARTESIAN_POINT('',(0.,0.,0.));
#63543=CARTESIAN_POINT('Origin',(0.,0.,-1.97));
#63544=CARTESIAN_POINT('',(-0.591686266410893,1.49359204264163E-5,-3.89198748077951));
#63545=CARTESIAN_POINT('',(-0.591672685651915,9.86808882838178E-6,-3.91716251922049));
#63546=CARTESIAN_POINT('',(-0.591675,-7.2459289488551E-17,-1.97));
#63547=CARTESIAN_POINT('',(0.258403420312052,0.532281296094751,-3.948325));
#63548=CARTESIAN_POINT('Ctrl Pts',(-0.591686266410893,1.49359204264163E-5,
-3.89198748077951));
#63549=CARTESIAN_POINT('Ctrl Pts',(-0.591706039082766,0.0191956542142459,
-3.89289044879051));
#63550=CARTESIAN_POINT('Ctrl Pts',(-0.590791776357017,0.0383744891623322,
-3.89379341680151));
#63551=CARTESIAN_POINT('Ctrl Pts',(-0.588929556550066,0.0574608246427564,
-3.89469638481251));
#63552=CARTESIAN_POINT('Ctrl Pts',(-0.579367464989497,0.155464984376378,
-3.89933292812776));
#63553=CARTESIAN_POINT('Ctrl Pts',(-0.544811556310261,0.251030305027336,
-3.90396947144302));
#63554=CARTESIAN_POINT('Ctrl Pts',(-0.489482341063839,0.332485605744252,
-3.90860601475827));
#63555=CARTESIAN_POINT('Ctrl Pts',(-0.434153125817416,0.413940906461167,
-3.91324255807352));
#63556=CARTESIAN_POINT('Ctrl Pts',(-0.358050604003807,0.481286187244039,
-3.91787910138878));
#63557=CARTESIAN_POINT('Ctrl Pts',(-0.270469482917255,0.5262949306221,-3.92251564470403));
#63558=CARTESIAN_POINT('Ctrl Pts',(-0.182888361830704,0.57130367400016,
-3.92715218801928));
#63559=CARTESIAN_POINT('Ctrl Pts',(-0.0838286414712106,0.593975879973408,
-3.93178873133454));
#63560=CARTESIAN_POINT('Ctrl Pts',(0.0146109189770026,0.591545050739007,
-3.93642527464979));
#63561=CARTESIAN_POINT('Ctrl Pts',(0.0988262243084228,0.589465469874856,
-3.94039184976653));
#63562=CARTESIAN_POINT('Ctrl Pts',(0.18258764403161,0.569013359286537,-3.94435842488326));
#63563=CARTESIAN_POINT('Ctrl Pts',(0.258414858989722,0.532291148796136,
-3.948325));
#63564=CARTESIAN_POINT('',(-0.258391981634415,0.53227144339335,-3.948325));
#63565=CARTESIAN_POINT('Origin',(0.,0.,-3.948325));
#63566=CARTESIAN_POINT('Ctrl Pts',(-0.258391981634415,0.53227144339335,
-3.948325));
#63567=CARTESIAN_POINT('Ctrl Pts',(-0.346999241769788,0.489256914213254,
-3.94368845668475));
#63568=CARTESIAN_POINT('Ctrl Pts',(-0.424612905004657,0.423710754820817,
-3.93905191336949));
#63569=CARTESIAN_POINT('Ctrl Pts',(-0.481782348966959,0.343551262433901,
-3.93441537005424));
#63570=CARTESIAN_POINT('Ctrl Pts',(-0.538951792929262,0.263391770046983,
-3.92977882673899));
#63571=CARTESIAN_POINT('Ctrl Pts',(-0.575677017618998,0.168618944665585,
-3.92514228342374));
#63572=CARTESIAN_POINT('Ctrl Pts',(-0.587468894991019,0.0708530052396791,
-3.92050574010848));
#63573=CARTESIAN_POINT('Ctrl Pts',(-0.590303107755304,0.0473546712008031,
-3.91939133314582));
#63574=CARTESIAN_POINT('Ctrl Pts',(-0.591696932244061,0.0236834263079573,
-3.91827692618316));
#63575=CARTESIAN_POINT('Ctrl Pts',(-0.591672685651915,9.86808882838178E-6,
-3.91716251922049));
#63576=CARTESIAN_POINT('Origin',(0.,0.,-1.97));
#63577=CARTESIAN_POINT('',(-0.591677080768459,-1.5385395483597E-5,-3.71698748077951));
#63578=CARTESIAN_POINT('',(-0.591691313069437,-1.42991252893039E-5,-3.74216251922049));
#63579=CARTESIAN_POINT('',(-0.591675,-7.2459289488551E-17,-1.97));
#63580=CARTESIAN_POINT('Ctrl Pts',(-0.591677080768459,-1.5385395483597E-5,
-3.71698748077951));
#63581=CARTESIAN_POINT('Ctrl Pts',(-0.591598027752696,0.076411593433387,
-3.72058526234081));
#63582=CARTESIAN_POINT('Ctrl Pts',(-0.576722878987479,0.152868446627701,
-3.72418304390211));
#63583=CARTESIAN_POINT('Ctrl Pts',(-0.547848301688052,0.223611254898452,
-3.72778082546341));
#63584=CARTESIAN_POINT('Ctrl Pts',(-0.510636974074789,0.314779128545468,
-3.73241736877866));
#63585=CARTESIAN_POINT('Ctrl Pts',(-0.450175303298876,0.396457078729179,
-3.73705391209391));
#63586=CARTESIAN_POINT('Ctrl Pts',(-0.37384776457188,0.458669384024616,
-3.74169045540916));
#63587=CARTESIAN_POINT('Ctrl Pts',(-0.297520225844884,0.520881689320052,
-3.74632699872441));
#63588=CARTESIAN_POINT('Ctrl Pts',(-0.205326819166806,0.563628349727214,
-3.75096354203967));
#63589=CARTESIAN_POINT('Ctrl Pts',(-0.108527569532848,0.58168850920162,
-3.75560008535492));
#63590=CARTESIAN_POINT('Ctrl Pts',(-0.0117283198988895,0.599748668676025,
-3.76023662867017));
#63591=CARTESIAN_POINT('Ctrl Pts',(0.0896767726909481,0.593122327217673,
-3.76487317198543));
#63592=CARTESIAN_POINT('Ctrl Pts',(0.183302615594723,0.562618792667065,
-3.76950971530068));
#63593=CARTESIAN_POINT('Ctrl Pts',(0.276928458498497,0.532115258116456,
-3.77414625861593));
#63594=CARTESIAN_POINT('Ctrl Pts',(0.362775051716209,0.477734530473591,
-3.77878280193118));
#63595=CARTESIAN_POINT('Ctrl Pts',(0.430357537219162,0.406118388435549,
-3.78341934524644));
#63596=CARTESIAN_POINT('Ctrl Pts',(0.497940022722115,0.334502246397506,
-3.78805588856169));
#63597=CARTESIAN_POINT('Ctrl Pts',(0.547258400510309,0.245650689964286,
-3.79269243187695));
#63598=CARTESIAN_POINT('Ctrl Pts',(0.572289179306194,0.150415591036874,
-3.7973289751922));
#63599=CARTESIAN_POINT('Ctrl Pts',(0.597319958102079,0.0551804921094613,
-3.80196551850745));
#63600=CARTESIAN_POINT('Ctrl Pts',(0.598063137905655,-0.0464381493121438,
-3.8066020618227));
#63601=CARTESIAN_POINT('Ctrl Pts',(0.574427950870245,-0.142029165052077,
-3.81123860513796));
#63602=CARTESIAN_POINT('Ctrl Pts',(0.550792763834835,-0.237620180792009,
-3.81587514845321));
#63603=CARTESIAN_POINT('Ctrl Pts',(0.502779209960441,-0.327183570850269,
-3.82051169176847));
#63604=CARTESIAN_POINT('Ctrl Pts',(0.436251415392235,-0.399780514746208,
-3.82514823508372));
#63605=CARTESIAN_POINT('Ctrl Pts',(0.369723620824028,-0.472377458642147,
-3.82978477839897));
#63606=CARTESIAN_POINT('Ctrl Pts',(0.284681585562009,-0.528007956375765,
-3.83442132171422));
#63607=CARTESIAN_POINT('Ctrl Pts',(0.191511904253478,-0.559877610775289,
-3.83905786502948));
#63608=CARTESIAN_POINT('Ctrl Pts',(0.0983422229449468,-0.591747265174813,
-3.84369440834473));
#63609=CARTESIAN_POINT('Ctrl Pts',(-0.00295510441009569,-0.599856076240243,
-3.84833095165998));
#63610=CARTESIAN_POINT('Ctrl Pts',(-0.100008149214248,-0.583213629709318,
-3.85296749497523));
#63611=CARTESIAN_POINT('Ctrl Pts',(-0.1970611940184,-0.566571183178393,
-3.85760403829049));
#63612=CARTESIAN_POINT('Ctrl Pts',(-0.289869956271661,-0.525177479051112,
-3.86224058160574));
#63613=CARTESIAN_POINT('Ctrl Pts',(-0.367099250476545,-0.464088219954072,
-3.86687712492099));
#63614=CARTESIAN_POINT('Ctrl Pts',(-0.444328544681429,-0.402998960857032,
-3.87151366823625));
#63615=CARTESIAN_POINT('Ctrl Pts',(-0.505978370837935,-0.322214146790233,
-3.8761502115515));
#63616=CARTESIAN_POINT('Ctrl Pts',(-0.544519146695237,-0.231600240348692,
-3.88078675486675));
#63617=CARTESIAN_POINT('Ctrl Pts',(-0.575554096476506,-0.158633415645678,
-3.88452033017101));
#63618=CARTESIAN_POINT('Ctrl Pts',(-0.591604510735713,-0.0792931406306882,
-3.88825390547526));
#63619=CARTESIAN_POINT('Ctrl Pts',(-0.591686266410893,1.49359204264163E-5,
-3.89198748077951));
#63620=CARTESIAN_POINT('Ctrl Pts',(-0.591672685651915,9.86808882838178E-6,
-3.91716251922049));
#63621=CARTESIAN_POINT('Ctrl Pts',(-0.591596053141098,-0.074811541676493,
-3.9136403828679));
#63622=CARTESIAN_POINT('Ctrl Pts',(-0.577354221098841,-0.149656059400805,
-3.91011824651531));
#63623=CARTESIAN_POINT('Ctrl Pts',(-0.549651763576913,-0.219137766588835,
-3.90659611016272));
#63624=CARTESIAN_POINT('Ctrl Pts',(-0.513184224736479,-0.310603545521029,
-3.90195956684747));
#63625=CARTESIAN_POINT('Ctrl Pts',(-0.453390617001303,-0.392776049915004,
-3.89732302353222));
#63626=CARTESIAN_POINT('Ctrl Pts',(-0.377572641459037,-0.455609324446237,
-3.89268648021696));
#63627=CARTESIAN_POINT('Ctrl Pts',(-0.301754665916771,-0.518442598977469,
-3.88804993690171));
#63628=CARTESIAN_POINT('Ctrl Pts',(-0.209912322567414,-0.56193664364596,
-3.88341339358646));
#63629=CARTESIAN_POINT('Ctrl Pts',(-0.113263366397263,-0.580784325059894,
-3.8787768502712));
#63630=CARTESIAN_POINT('Ctrl Pts',(-0.0166144102271124,-0.599632006473828,
-3.87414030695595));
#63631=CARTESIAN_POINT('Ctrl Pts',(0.0848411587638334,-0.593833324633207,
-3.8695037636407));
#63632=CARTESIAN_POINT('Ctrl Pts',(0.17871239403648,-0.56409394180932,-3.86486722032545));
#63633=CARTESIAN_POINT('Ctrl Pts',(0.272583629309127,-0.534354558985432,
-3.86023067701019));
#63634=CARTESIAN_POINT('Ctrl Pts',(0.358870530863474,-0.48067447517828,
-3.85559413369494));
#63635=CARTESIAN_POINT('Ctrl Pts',(0.427034304402794,-0.409611207177925,
-3.85095759037968));
#63636=CARTESIAN_POINT('Ctrl Pts',(0.495198077942114,-0.33854793917757,
-3.84632104706443));
#63637=CARTESIAN_POINT('Ctrl Pts',(0.545238723466406,-0.250101486984014,
-3.84168450374918));
#63638=CARTESIAN_POINT('Ctrl Pts',(0.571044617305461,-0.155073571731536,
-3.83704796043393));
#63639=CARTESIAN_POINT('Ctrl Pts',(0.596850511144516,-0.0600456564790578,
-3.83241141711867));
#63640=CARTESIAN_POINT('Ctrl Pts',(0.598421653298335,0.0415637218323413,
-3.82777487380342));
#63641=CARTESIAN_POINT('Ctrl Pts',(0.5755661108858,0.137344177102385,-3.82313833048817));
#63642=CARTESIAN_POINT('Ctrl Pts',(0.552710568473265,0.233124632372429,
-3.81850178717291));
#63643=CARTESIAN_POINT('Ctrl Pts',(0.505428341494376,0.323076164601118,
-3.81386524385766));
#63644=CARTESIAN_POINT('Ctrl Pts',(0.439494257526417,0.396212735327201,
-3.80922870054241));
#63645=CARTESIAN_POINT('Ctrl Pts',(0.373560173558458,0.469349306053284,
-3.80459215722716));
#63646=CARTESIAN_POINT('Ctrl Pts',(0.288974232601431,0.525670915276761,
-3.7999556139119));
#63647=CARTESIAN_POINT('Ctrl Pts',(0.196067312291794,0.558298643565172,
-3.79531907059665));
#63648=CARTESIAN_POINT('Ctrl Pts',(0.103160391982157,0.590926371853582,
-3.7906825272814));
#63649=CARTESIAN_POINT('Ctrl Pts',(0.00193249231991062,0.599860219206927,
-3.78604598396614));
#63650=CARTESIAN_POINT('Ctrl Pts',(-0.0952529299216813,0.584009097814957,
-3.78140944065089));
#63651=CARTESIAN_POINT('Ctrl Pts',(-0.192438352163274,0.568157976422986,
-3.77677289733564));
#63652=CARTESIAN_POINT('Ctrl Pts',(-0.285581296984212,0.527521886285701,
-3.77213635402039));
#63653=CARTESIAN_POINT('Ctrl Pts',(-0.363305770565049,0.467063885351627,
-3.76749981070513));
#63654=CARTESIAN_POINT('Ctrl Pts',(-0.441030244145885,0.406605884417554,
-3.76286326738988));
#63655=CARTESIAN_POINT('Ctrl Pts',(-0.503336246486619,0.326325972686693,
-3.75822672407463));
#63656=CARTESIAN_POINT('Ctrl Pts',(-0.542614043818136,0.236029134685033,
-3.75359018075937));
#63657=CARTESIAN_POINT('Ctrl Pts',(-0.574883297252459,0.161844436261137,
-3.74978096024641));
#63658=CARTESIAN_POINT('Ctrl Pts',(-0.591609234805437,0.0808986268811383,
-3.74597173973345));
#63659=CARTESIAN_POINT('Ctrl Pts',(-0.591691313069437,-1.42991252893039E-5,
-3.74216251922049));
#63660=CARTESIAN_POINT('Origin',(0.,0.,-1.97));
#63661=CARTESIAN_POINT('',(-0.591640224643815,1.16845008508032E-5,-3.54198748077951));
#63662=CARTESIAN_POINT('',(-0.591631758215553,8.49683898327695E-6,-3.56716251922049));
#63663=CARTESIAN_POINT('',(-0.591675,-7.2459289488551E-17,-1.97));
#63664=CARTESIAN_POINT('Ctrl Pts',(-0.591640224643815,1.16845008508032E-5,
-3.54198748077951));
#63665=CARTESIAN_POINT('Ctrl Pts',(-0.59166519960911,0.0351971653384486,
-3.54364353257585));
#63666=CARTESIAN_POINT('Ctrl Pts',(-0.588577633489791,0.0703783135634807,
-3.54529958437219));
#63667=CARTESIAN_POINT('Ctrl Pts',(-0.582337221164469,0.104991027297213,
-3.54695563616854));
#63668=CARTESIAN_POINT('Ctrl Pts',(-0.564865580413074,0.201898229619839,
-3.55159217948379));
#63669=CARTESIAN_POINT('Ctrl Pts',(-0.522679908086348,0.294349677665667,
-3.55622872279904));
#63670=CARTESIAN_POINT('Ctrl Pts',(-0.460932543627806,0.371053830584308,
-3.5608652661143));
#63671=CARTESIAN_POINT('Ctrl Pts',(-0.399185179169264,0.44775798350295,
-3.56550180942955));
#63672=CARTESIAN_POINT('Ctrl Pts',(-0.317876122578908,0.508714841294403,
-3.5701383527448));
#63673=CARTESIAN_POINT('Ctrl Pts',(-0.226936040746222,0.546479449180746,
-3.57477489606005));
#63674=CARTESIAN_POINT('Ctrl Pts',(-0.135995958913538,0.584244057067088,
-3.57941143937531));
#63675=CARTESIAN_POINT('Ctrl Pts',(-0.0354248518385249,0.598816415048318,
-3.58404798269056));
#63676=CARTESIAN_POINT('Ctrl Pts',(0.0624940465446171,0.588416730823486,
-3.58868452600582));
#63677=CARTESIAN_POINT('Ctrl Pts',(0.16041294492776,0.578017046598654,-3.59332106932107));
#63678=CARTESIAN_POINT('Ctrl Pts',(0.255679634619035,0.542645320167759,
-3.59795761263632));
#63679=CARTESIAN_POINT('Ctrl Pts',(0.336658735739967,0.486621670927618,
-3.60259415595157));
#63680=CARTESIAN_POINT('Ctrl Pts',(0.417637836860899,0.430598021687478,
-3.60723069926683));
#63681=CARTESIAN_POINT('Ctrl Pts',(0.48432934941149,0.353922449638093,-3.61186724258208));
#63682=CARTESIAN_POINT('Ctrl Pts',(0.528587917594161,0.265959711873829,
-3.61650378589733));
#63683=CARTESIAN_POINT('Ctrl Pts',(0.572846485776831,0.177996974109566,
-3.62114032921259));
#63684=CARTESIAN_POINT('Ctrl Pts',(0.594672109591582,0.0787470706304238,
-3.62577687252784));
#63685=CARTESIAN_POINT('Ctrl Pts',(0.591399120429623,-0.0196681295900901,
-3.63041341584309));
#63686=CARTESIAN_POINT('Ctrl Pts',(0.588126131267663,-0.118083329810605,
-3.63504995915834));
#63687=CARTESIAN_POINT('Ctrl Pts',(0.559754529128993,-0.215663826772493,
-3.6396865024736));
#63688=CARTESIAN_POINT('Ctrl Pts',(0.509749474498588,-0.300491644167661,
-3.64432304578885));
#63689=CARTESIAN_POINT('Ctrl Pts',(0.459744419868183,-0.38531946156283,
-3.6489595891041));
#63690=CARTESIAN_POINT('Ctrl Pts',(0.388105912746044,-0.45739459939128,
-3.65359613241935));
#63691=CARTESIAN_POINT('Ctrl Pts',(0.303583509214952,-0.507914173753984,
-3.65823267573461));
#63692=CARTESIAN_POINT('Ctrl Pts',(0.21906110568386,-0.558433748116688,
-3.66286921904986));
#63693=CARTESIAN_POINT('Ctrl Pts',(0.121654805743816,-0.587397759013646,
-3.66750576236512));
#63694=CARTESIAN_POINT('Ctrl Pts',(0.0232613101835599,-0.591268692231257,
-3.67214230568037));
#63695=CARTESIAN_POINT('Ctrl Pts',(-0.0751321853766959,-0.595139625448867,
-3.67677884899562));
#63696=CARTESIAN_POINT('Ctrl Pts',(-0.174512876557163,-0.573917480987128,
-3.68141539231087));
#63697=CARTESIAN_POINT('Ctrl Pts',(-0.262742920653841,-0.53019422159853,
-3.68605193562613));
#63698=CARTESIAN_POINT('Ctrl Pts',(-0.350972964750519,-0.486470962209931,
-3.69068847894138));
#63699=CARTESIAN_POINT('Ctrl Pts',(-0.428052361763407,-0.420246587894471,
-3.69532502225664));
#63700=CARTESIAN_POINT('Ctrl Pts',(-0.484567033507559,-0.339609400635107,
-3.69996156557189));
#63701=CARTESIAN_POINT('Ctrl Pts',(-0.541081705251711,-0.258972213375742,
-3.70459810888714));
#63702=CARTESIAN_POINT('Ctrl Pts',(-0.577031651727126,-0.163922213172471,
-3.70923465220239));
#63703=CARTESIAN_POINT('Ctrl Pts',(-0.588026132739526,-0.0660683145156767,
-3.71387119551764));
#63704=CARTESIAN_POINT('Ctrl Pts',(-0.59048931395099,-0.0441453256662729,
-3.7149099572716));
#63705=CARTESIAN_POINT('Ctrl Pts',(-0.591699905180646,-0.022081600707655,
-3.71594871902555));
#63706=CARTESIAN_POINT('Ctrl Pts',(-0.591677080768459,-1.5385395483597E-5,
-3.71698748077951));
#63707=CARTESIAN_POINT('Ctrl Pts',(-0.591691313069437,-1.42991252893039E-5,
-3.74216251922049));
#63708=CARTESIAN_POINT('Ctrl Pts',(-0.591709139608791,-0.0175877392707435,
-3.7413351964182));
#63709=CARTESIAN_POINT('Ctrl Pts',(-0.590941853822676,-0.0351596282650225,
-3.74050787361591));
#63710=CARTESIAN_POINT('Ctrl Pts',(-0.589378180522454,-0.0526603608866166,
-3.73968055081362));
#63711=CARTESIAN_POINT('Ctrl Pts',(-0.580614927572954,-0.150739254184145,
-3.73504400749836));
#63712=CARTESIAN_POINT('Ctrl Pts',(-0.546838829351652,-0.24658327650674,
-3.73040746418311));
#63713=CARTESIAN_POINT('Ctrl Pts',(-0.492175123108772,-0.328486532400379,
-3.72577092086785));
#63714=CARTESIAN_POINT('Ctrl Pts',(-0.437511416865892,-0.410389788294018,
-3.7211343775526));
#63715=CARTESIAN_POINT('Ctrl Pts',(-0.361960102601434,-0.4783522777587,
-3.71649783423735));
#63716=CARTESIAN_POINT('Ctrl Pts',(-0.274748626586135,-0.524073416078952,
-3.7118612909221));
#63717=CARTESIAN_POINT('Ctrl Pts',(-0.187537150570835,-0.569794554399205,
-3.70722474760684));
#63718=CARTESIAN_POINT('Ctrl Pts',(-0.0886655128046928,-0.593274341575028,
-3.70258820429159));
#63719=CARTESIAN_POINT('Ctrl Pts',(0.00979061725475591,-0.591645077227593,
-3.69795166097634));
#63720=CARTESIAN_POINT('Ctrl Pts',(0.108246747314204,-0.590015812880158,
-3.69331511766108));
#63721=CARTESIAN_POINT('Ctrl Pts',(0.206287369666958,-0.563277497009465,
-3.68867857434583));
#63722=CARTESIAN_POINT('Ctrl Pts',(0.291938310620198,-0.514695809401822,
-3.68404203103058));
#63723=CARTESIAN_POINT('Ctrl Pts',(0.377589251573439,-0.466114121794178,
-3.67940548771533));
#63724=CARTESIAN_POINT('Ctrl Pts',(0.450850511127164,-0.395689062449585,
-3.67476894440007));
#63725=CARTESIAN_POINT('Ctrl Pts',(0.502774338650679,-0.312021983009729,
-3.67013240108482));
#63726=CARTESIAN_POINT('Ctrl Pts',(0.554698166174194,-0.228354903569872,
-3.66549585776957));
#63727=CARTESIAN_POINT('Ctrl Pts',(0.585284561667497,-0.131445804034753,
-3.66085931445431));
#63728=CARTESIAN_POINT('Ctrl Pts',(0.590797861247265,-0.0331306598224494,
-3.65622277113906));
#63729=CARTESIAN_POINT('Ctrl Pts',(0.596311160827033,0.0651844843898538,
-3.65158622782381));
#63730=CARTESIAN_POINT('Ctrl Pts',(0.576751364493266,0.164905673279341,
-3.64694968450856));
#63731=CARTESIAN_POINT('Ctrl Pts',(0.534507404432907,0.253853477572184,
-3.6423131411933));
#63732=CARTESIAN_POINT('Ctrl Pts',(0.492263444372549,0.342801281865026,
-3.63767659787805));
#63733=CARTESIAN_POINT('Ctrl Pts',(0.427335320585598,0.420975701561225,
-3.6330400545628));
#63734=CARTESIAN_POINT('Ctrl Pts',(0.347653017699086,0.478828918051121,
-3.62840351124754));
#63735=CARTESIAN_POINT('Ctrl Pts',(0.267970714812574,0.536682134541016,
-3.62376696793229));
#63736=CARTESIAN_POINT('Ctrl Pts',(0.173534232826499,0.574214147824609,
-3.61913042461704));
#63737=CARTESIAN_POINT('Ctrl Pts',(0.0758775543535335,0.586840992277037,
-3.61449388130178));
#63738=CARTESIAN_POINT('Ctrl Pts',(-0.0217791241194331,0.599467836729464,
-3.60985733798653));
#63739=CARTESIAN_POINT('Ctrl Pts',(-0.122655999079291,0.587189512350725,
-3.60522079467128));
#63740=CARTESIAN_POINT('Ctrl Pts',(-0.214432491687569,0.551505630055761,
-3.60058425135602));
#63741=CARTESIAN_POINT('Ctrl Pts',(-0.306208984295846,0.515821747760798,
-3.59594770804077));
#63742=CARTESIAN_POINT('Ctrl Pts',(-0.388885094552543,0.456732307549611,
-3.59131116472552));
#63743=CARTESIAN_POINT('Ctrl Pts',(-0.452363190715939,0.381454187496397,
-3.58667462141027));
#63744=CARTESIAN_POINT('Ctrl Pts',(-0.515841286879337,0.306176067443183,
-3.58203807809501));
#63745=CARTESIAN_POINT('Ctrl Pts',(-0.560121368949433,0.214709267547942,
-3.57740153477976));
#63746=CARTESIAN_POINT('Ctrl Pts',(-0.579795297128556,0.118225068835626,
-3.57276499146451));
#63747=CARTESIAN_POINT('Ctrl Pts',(-0.587719493313795,0.0793634997371216,
-3.5708975007165));
#63748=CARTESIAN_POINT('Ctrl Pts',(-0.591651859745899,0.0396879634509739,
-3.5690300099685));
#63749=CARTESIAN_POINT('Ctrl Pts',(-0.591631758215553,8.49683898327695E-6,
-3.56716251922049));
#63750=CARTESIAN_POINT('Origin',(0.,0.,-1.97));
#63751=CARTESIAN_POINT('',(-0.591720711673068,-6.25964164063797E-6,-3.36698748077951));
#63752=CARTESIAN_POINT('',(-0.591725682421883,-1.68028488189446E-6,-3.39216251922049));
#63753=CARTESIAN_POINT('',(-0.591675,-7.2459289488551E-17,-1.97));
#63754=CARTESIAN_POINT('Ctrl Pts',(-0.591720711673068,-6.25964164063797E-6,
-3.36698748077951));
#63755=CARTESIAN_POINT('Ctrl Pts',(-0.591670632807954,0.0923986416864466,
-3.37133834612615));
#63756=CARTESIAN_POINT('Ctrl Pts',(-0.569664035056796,0.18482655914794,
-3.37568921147279));
#63757=CARTESIAN_POINT('Ctrl Pts',(-0.527928364019782,0.267266528824463,
-3.38004007681943));
#63758=CARTESIAN_POINT('Ctrl Pts',(-0.483452327384057,0.355119509751242,
-3.38467662013468));
#63759=CARTESIAN_POINT('Ctrl Pts',(-0.416571337426255,0.431629864460194,
-3.38931316344994));
#63760=CARTESIAN_POINT('Ctrl Pts',(-0.335453891732765,0.487453014646359,
-3.39394970676519));
#63761=CARTESIAN_POINT('Ctrl Pts',(-0.254336446039275,0.543276164832523,
-3.39858625008044));
#63762=CARTESIAN_POINT('Ctrl Pts',(-0.158982544610098,0.578412110495901,
-3.40322279339569));
#63763=CARTESIAN_POINT('Ctrl Pts',(-0.0610382189134935,0.588569529281247,
-3.40785933671095));
#63764=CARTESIAN_POINT('Ctrl Pts',(0.036906106783112,0.598726948066594,
-3.4124958800262));
#63765=CARTESIAN_POINT('Ctrl Pts',(0.137440856747144,0.583905839973908,
-3.41713242334146));
#63766=CARTESIAN_POINT('Ctrl Pts',(0.22828723751356,0.545916378353781,-3.42176896665671));
#63767=CARTESIAN_POINT('Ctrl Pts',(0.319133618279975,0.507926916733654,
-3.42640550997196));
#63768=CARTESIAN_POINT('Ctrl Pts',(0.400291629848773,0.446769101586084,
-3.43104205328721));
#63769=CARTESIAN_POINT('Ctrl Pts',(0.461849053186801,0.369912431579334,
-3.43567859660246));
#63770=CARTESIAN_POINT('Ctrl Pts',(0.523406476524829,0.293055761572585,
-3.44031513991772));
#63771=CARTESIAN_POINT('Ctrl Pts',(0.565363311632086,0.200500236706655,
-3.44495168323297));
#63772=CARTESIAN_POINT('Ctrl Pts',(0.582595168057379,0.103550109235457,
-3.44958822654822));
#63773=CARTESIAN_POINT('Ctrl Pts',(0.599827024482672,0.00659998176425772,
-3.45422476986348));
#63774=CARTESIAN_POINT('Ctrl Pts',(0.592333902226001,-0.0947447483122083,
-3.45886131317873));
#63775=CARTESIAN_POINT('Ctrl Pts',(0.561030972416062,-0.188106360754677,
-3.46349785649398));
#63776=CARTESIAN_POINT('Ctrl Pts',(0.529728042606125,-0.281467973197144,
-3.46813439980924));
#63777=CARTESIAN_POINT('Ctrl Pts',(0.474615305242921,-0.366846468005612,
-3.47277094312449));
#63778=CARTESIAN_POINT('Ctrl Pts',(0.402423944515183,-0.43381415819141,
-3.47740748643974));
#63779=CARTESIAN_POINT('Ctrl Pts',(0.330232583787443,-0.500781848377208,
-3.482044029755));
#63780=CARTESIAN_POINT('Ctrl Pts',(0.240962599695169,-0.549338733940336,
-3.48668057307025));
#63781=CARTESIAN_POINT('Ctrl Pts',(0.145516965565382,-0.57355432846342,
-3.4913171163855));
#63782=CARTESIAN_POINT('Ctrl Pts',(0.0500713314355945,-0.597769922986504,
-3.49595365970075));
#63783=CARTESIAN_POINT('Ctrl Pts',(-0.0515499527317057,-0.597644226469546,
-3.50059020301601));
#63784=CARTESIAN_POINT('Ctrl Pts',(-0.146935389813492,-0.573192590833864,
-3.50522674633126));
#63785=CARTESIAN_POINT('Ctrl Pts',(-0.242320826895278,-0.548740955198182,
-3.50986328964651));
#63786=CARTESIAN_POINT('Ctrl Pts',(-0.331470416891551,-0.499963380443776,
-3.51449983296176));
#63787=CARTESIAN_POINT('Ctrl Pts',(-0.403495890786381,-0.43281730682239,
-3.51913637627702));
#63788=CARTESIAN_POINT('Ctrl Pts',(-0.475521364681212,-0.365671233201003,
-3.52377291959227));
#63789=CARTESIAN_POINT('Ctrl Pts',(-0.530422722474602,-0.280156660712634,
-3.52840946290753));
#63790=CARTESIAN_POINT('Ctrl Pts',(-0.561494596783265,-0.186717896168737,
-3.53304600622278));
#63791=CARTESIAN_POINT('Ctrl Pts',(-0.581468411661466,-0.126653010255906,
-3.53602649774169));
#63792=CARTESIAN_POINT('Ctrl Pts',(-0.591595275764553,-0.0633136459368033,
-3.5390069892606));
#63793=CARTESIAN_POINT('Ctrl Pts',(-0.591640224643815,1.16845008508032E-5,
-3.54198748077951));
#63794=CARTESIAN_POINT('Ctrl Pts',(-0.591631758215553,8.49683898327695E-6,
-3.56716251922049));
#63795=CARTESIAN_POINT('Ctrl Pts',(-0.591601952341403,-0.0588268837412697,
-3.56439346665324));
#63796=CARTESIAN_POINT('Ctrl Pts',(-0.582882265224252,-0.117670905521185,
-3.561624414086));
#63797=CARTESIAN_POINT('Ctrl Pts',(-0.565601016486239,-0.173882844534329,
-3.55885536151875));
#63798=CARTESIAN_POINT('Ctrl Pts',(-0.536665033376649,-0.268004961662577,
-3.55421881820349));
#63799=CARTESIAN_POINT('Ctrl Pts',(-0.483725292869318,-0.354747598389681,
-3.54958227488824));
#63800=CARTESIAN_POINT('Ctrl Pts',(-0.413247580575901,-0.423516458501507,
-3.54494573157299));
#63801=CARTESIAN_POINT('Ctrl Pts',(-0.342769868282486,-0.492285318613332,
-3.54030918825774));
#63802=CARTESIAN_POINT('Ctrl Pts',(-0.254754184202987,-0.54308040210988,
-3.53567264494248));
#63803=CARTESIAN_POINT('Ctrl Pts',(-0.159950307959673,-0.569697860674586,
-3.53103610162723));
#63804=CARTESIAN_POINT('Ctrl Pts',(-0.0651464317163584,-0.596315319239292,
-3.52639955831198));
#63805=CARTESIAN_POINT('Ctrl Pts',(0.0364456366907705,-0.598755152872157,
-3.52176301499672));
#63806=CARTESIAN_POINT('Ctrl Pts',(0.132417968400244,-0.576719372934783,
-3.51712647168147));
#63807=CARTESIAN_POINT('Ctrl Pts',(0.228390300109719,-0.554683592997408,
-3.51248992836622));
#63808=CARTESIAN_POINT('Ctrl Pts',(0.318742895121539,-0.508172199489795,
-3.50785338505096));
#63809=CARTESIAN_POINT('Ctrl Pts',(0.392440555620253,-0.442865853027787,
-3.50321684173571));
#63810=CARTESIAN_POINT('Ctrl Pts',(0.466138216118966,-0.37755950656578,
-3.49858029842046));
#63811=CARTESIAN_POINT('Ctrl Pts',(0.523180942104573,-0.293458207149378,
-3.49394375510521));
#63812=CARTESIAN_POINT('Ctrl Pts',(0.556601830577751,-0.20083365173957,
-3.48930721178995));
#63813=CARTESIAN_POINT('Ctrl Pts',(0.59002271905093,-0.10820909632976,-3.4846706684747));
#63814=CARTESIAN_POINT('Ctrl Pts',(0.599821770011678,-0.00706128492654368,
-3.48003412515945));
#63815=CARTESIAN_POINT('Ctrl Pts',(0.584802178146975,0.0902561128572957,
-3.4753975818442));
#63816=CARTESIAN_POINT('Ctrl Pts',(0.569782586282271,0.187573510641134,
-3.47076103852894));
#63817=CARTESIAN_POINT('Ctrl Pts',(0.529944351592118,0.281060494805596,
-3.46612449521369));
#63818=CARTESIAN_POINT('Ctrl Pts',(0.470153109649757,0.35929904948416,-3.46148795189844));
#63819=CARTESIAN_POINT('Ctrl Pts',(0.410361867707395,0.437537604162725,
-3.45685140858318));
#63820=CARTESIAN_POINT('Ctrl Pts',(0.330617618512825,0.500527729355392,
-3.45221486526793));
#63821=CARTESIAN_POINT('Ctrl Pts',(0.240659911487869,0.540576137538651,
-3.44757832195268));
#63822=CARTESIAN_POINT('Ctrl Pts',(0.150702204462913,0.580624545721909,
-3.44294177863742));
#63823=CARTESIAN_POINT('Ctrl Pts',(0.0505310396075721,0.597731236895759,
-3.43830523532217));
#63824=CARTESIAN_POINT('Ctrl Pts',(-0.0476191960144642,0.58980688843425,
-3.43366869200692));
#63825=CARTESIAN_POINT('Ctrl Pts',(-0.1457694316365,0.581882539972741,-3.42903214869166));
#63826=CARTESIAN_POINT('Ctrl Pts',(-0.24189873802523,0.548927151875873,
-3.42439560537641));
#63827=CARTESIAN_POINT('Ctrl Pts',(-0.324266379768199,0.494965724495729,
-3.41975906206116));
#63828=CARTESIAN_POINT('Ctrl Pts',(-0.406634021511169,0.441004297115584,
-3.41512251874591));
#63829=CARTESIAN_POINT('Ctrl Pts',(-0.475239998608377,0.366036830452165,
-3.41048597543065));
#63830=CARTESIAN_POINT('Ctrl Pts',(-0.521705132481815,0.279219462458633,
-3.4058494321154));
#63831=CARTESIAN_POINT('Ctrl Pts',(-0.567426279806072,0.193792189545821,
-3.4012871278171));
#63832=CARTESIAN_POINT('Ctrl Pts',(-0.591709933354533,0.0968914518041998,
-3.39672482351879));
#63833=CARTESIAN_POINT('Ctrl Pts',(-0.591725682421883,-1.68028488189446E-6,
-3.39216251922049));
#63834=CARTESIAN_POINT('Origin',(0.,0.,-1.97));
#63835=CARTESIAN_POINT('',(-0.591624439693044,-1.80568084665045E-6,-3.19198748077951));
#63836=CARTESIAN_POINT('',(-0.591627593882854,-5.87472452489096E-6,-3.21716251922049));
#63837=CARTESIAN_POINT('',(-0.591675,-7.2459289488551E-17,-1.97));
#63838=CARTESIAN_POINT('Ctrl Pts',(-0.591624439693044,-1.80568084665045E-6,
-3.19198748077951));
#63839=CARTESIAN_POINT('Ctrl Pts',(-0.591619011968859,0.0511880591375139,
-3.19439661636119));
#63840=CARTESIAN_POINT('Ctrl Pts',(-0.585043627760961,0.102379292407691,
-3.19680575194288));
#63841=CARTESIAN_POINT('Ctrl Pts',(-0.571915327198982,0.15183087130542,
-3.19921488752456));
#63842=CARTESIAN_POINT('Ctrl Pts',(-0.546649030576224,0.247003757925056,
-3.20385143083982));
#63843=CARTESIAN_POINT('Ctrl Pts',(-0.497111001113603,0.335733036251805,
-3.20848797415507));
#63844=CARTESIAN_POINT('Ctrl Pts',(-0.429351557060823,0.407181771959315,
-3.21312451747032));
#63845=CARTESIAN_POINT('Ctrl Pts',(-0.361592113008042,0.478630507666826,
-3.21776106078557));
#63846=CARTESIAN_POINT('Ctrl Pts',(-0.275611254365102,0.532798700755097,
-3.22239760410083));
#63847=CARTESIAN_POINT('Ctrl Pts',(-0.181910237718421,0.563070528779219,
-3.22703414741608));
#63848=CARTESIAN_POINT('Ctrl Pts',(-0.0882092210717391,0.59334235680334,
-3.23167069073133));
#63849=CARTESIAN_POINT('Ctrl Pts',(0.0132119535786834,0.599717819763311,
-3.23630723404658));
#63850=CARTESIAN_POINT('Ctrl Pts',(0.109966229449395,0.581418251646062,
-3.24094377736184));
#63851=CARTESIAN_POINT('Ctrl Pts',(0.206720505320107,0.563118683528813,
-3.24558032067709));
#63852=CARTESIAN_POINT('Ctrl Pts',(0.298807882411109,0.520144084334345,
-3.25021686399235));
#63853=CARTESIAN_POINT('Ctrl Pts',(0.374981285612127,0.457743148946173,
-3.2548534073076));
#63854=CARTESIAN_POINT('Ctrl Pts',(0.451154688813143,0.395342213558001,
-3.25948995062285));
#63855=CARTESIAN_POINT('Ctrl Pts',(0.511414118124177,0.313514941976128,
-3.2641264939381));
#63856=CARTESIAN_POINT('Ctrl Pts',(0.548399799068281,0.222255293184099,
-3.26876303725335));
#63857=CARTESIAN_POINT('Ctrl Pts',(0.585385480012385,0.130995644392071,
-3.27339958056861));
#63858=CARTESIAN_POINT('Ctrl Pts',(0.599097412589559,0.0303036183898887,
-3.27803612388387));
#63859=CARTESIAN_POINT('Ctrl Pts',(0.587860892399763,-0.0675227824769924,
-3.28267266719912));
#63860=CARTESIAN_POINT('Ctrl Pts',(0.576624372209967,-0.165349183343875,
-3.28730921051437));
#63861=CARTESIAN_POINT('Ctrl Pts',(0.5404393992532,-0.260309959075456,-3.29194575382962));
#63862=CARTESIAN_POINT('Ctrl Pts',(0.483725418643049,-0.340807092539295,
-3.29658229714487));
#63863=CARTESIAN_POINT('Ctrl Pts',(0.427011438032899,-0.421304226003134,
-3.30121884046013));
#63864=CARTESIAN_POINT('Ctrl Pts',(0.349768449769366,-0.487337717199232,
-3.30585538377538));
#63865=CARTESIAN_POINT('Ctrl Pts',(0.261430512223809,-0.530842577648852,
-3.31049192709064));
#63866=CARTESIAN_POINT('Ctrl Pts',(0.173092574678252,-0.574347438098472,
-3.31512847040589));
#63867=CARTESIAN_POINT('Ctrl Pts',(0.073659687850671,-0.595323667801614,
-3.31976501372114));
#63868=CARTESIAN_POINT('Ctrl Pts',(-0.0247239306483499,-0.591209338745403,
-3.32440155703639));
#63869=CARTESIAN_POINT('Ctrl Pts',(-0.123107549147369,-0.587095009689192,
-3.32903810035165));
#63870=CARTESIAN_POINT('Ctrl Pts',(-0.220441899317829,-0.557890121873629,
-3.3336746436669));
#63871=CARTESIAN_POINT('Ctrl Pts',(-0.304839067943404,-0.507161608978714,
-3.33831118698215));
#63872=CARTESIAN_POINT('Ctrl Pts',(-0.389236236568979,-0.456433096083798,
-3.34294773029741));
#63873=CARTESIAN_POINT('Ctrl Pts',(-0.46069622364967,-0.38418095810953,
-3.34758427361266));
#63874=CARTESIAN_POINT('Ctrl Pts',(-0.510491276615423,-0.299229696831776,
-3.35222081692791));
#63875=CARTESIAN_POINT('Ctrl Pts',(-0.560286329581176,-0.214278435554019,
-3.35685736024317));
#63876=CARTESIAN_POINT('Ctrl Pts',(-0.58841644843199,-0.116628050972775,
-3.36149390355842));
#63877=CARTESIAN_POINT('Ctrl Pts',(-0.591445966200572,-0.0182050551098478,
-3.36613044687367));
#63878=CARTESIAN_POINT('Ctrl Pts',(-0.591632628207839,-0.012140778425441,
-3.36641612484229));
#63879=CARTESIAN_POINT('Ctrl Pts',(-0.591723999853077,-0.00607356864757978,
-3.3667018028109));
#63880=CARTESIAN_POINT('Ctrl Pts',(-0.591720711673068,-6.25964164063797E-6,
-3.36698748077951));
#63881=CARTESIAN_POINT('Ctrl Pts',(-0.591725682421883,-1.68028488189446E-6,
-3.39216251922049));
#63882=CARTESIAN_POINT('Ctrl Pts',(-0.591725938694854,-0.00157835084546417,
-3.39208828020354));
#63883=CARTESIAN_POINT('Ctrl Pts',(-0.591719769153025,-0.00315501939217195,
-3.39201404118659));
#63884=CARTESIAN_POINT('Ctrl Pts',(-0.591707161601071,-0.0047316364567862,
-3.39193980216964));
#63885=CARTESIAN_POINT('Ctrl Pts',(-0.590919766197223,-0.10319809805503,
-3.38730325885439));
#63886=CARTESIAN_POINT('Ctrl Pts',(-0.565020684739859,-0.201463751927878,
-3.38266671553913));
#63887=CARTESIAN_POINT('Ctrl Pts',(-0.517173096848594,-0.287526940250111,
-3.37803017222388));
#63888=CARTESIAN_POINT('Ctrl Pts',(-0.469325508957329,-0.373590128572344,
-3.37339362890863));
#63889=CARTESIAN_POINT('Ctrl Pts',(-0.399529414632163,-0.447450851343963,
-3.36875708559337));
#63890=CARTESIAN_POINT('Ctrl Pts',(-0.316309347203035,-0.500088142576432,
-3.36412054227812));
#63891=CARTESIAN_POINT('Ctrl Pts',(-0.233089279773905,-0.552725433808902,
-3.35948399896287));
#63892=CARTESIAN_POINT('Ctrl Pts',(-0.136445239240813,-0.584139293502221,
-3.35484745564762));
#63893=CARTESIAN_POINT('Ctrl Pts',(-0.0381808279776381,-0.590492995596474,
-3.35021091233237));
#63894=CARTESIAN_POINT('Ctrl Pts',(0.0600835832855345,-0.596846697690727,
-3.34557436901711));
#63895=CARTESIAN_POINT('Ctrl Pts',(0.159968365278788,-0.578140242185915,
-3.34093782570186));
#63896=CARTESIAN_POINT('Ctrl Pts',(0.249274108257385,-0.536658338634592,
-3.3363012823866));
#63897=CARTESIAN_POINT('Ctrl Pts',(0.338579851235984,-0.495176435083269,
-3.33166473907135));
#63898=CARTESIAN_POINT('Ctrl Pts',(0.417306555199926,-0.430919083485436,
-3.3270281957561));
#63899=CARTESIAN_POINT('Ctrl Pts',(0.475838948429704,-0.351734343831918,
-3.32239165244085));
#63900=CARTESIAN_POINT('Ctrl Pts',(0.53437134165948,-0.272549604178401,
-3.31775510912559));
#63901=CARTESIAN_POINT('Ctrl Pts',(0.572709424155094,-0.1784374764692,-3.31311856581034));
#63902=CARTESIAN_POINT('Ctrl Pts',(0.586170781159679,-0.0808923283643585,
-3.30848202249509));
#63903=CARTESIAN_POINT('Ctrl Pts',(0.599632138164264,0.0166528197404849,
-3.30384547917983));
#63904=CARTESIAN_POINT('Ctrl Pts',(0.58821676967782,0.11763098824097,-3.29920893586458));
#63905=CARTESIAN_POINT('Ctrl Pts',(0.553318889661415,0.209709226829473,
-3.29457239254933));
#63906=CARTESIAN_POINT('Ctrl Pts',(0.518421009645009,0.301787465417976,
-3.28993584923408));
#63907=CARTESIAN_POINT('Ctrl Pts',(0.460040618098642,0.384965774094497,
-3.28529930591882));
#63908=CARTESIAN_POINT('Ctrl Pts',(0.385307993562448,0.449085185204808,
-3.28066276260357));
#63909=CARTESIAN_POINT('Ctrl Pts',(0.310575369026254,0.513204596315118,
-3.27602621928831));
#63910=CARTESIAN_POINT('Ctrl Pts',(0.219490511500231,0.558265109859217,
-3.27138967597306));
#63911=CARTESIAN_POINT('Ctrl Pts',(0.123178053549291,0.578763268182565,
-3.26675313265781));
#63912=CARTESIAN_POINT('Ctrl Pts',(0.0268655955983512,0.599261426505914,
-3.26211658934256));
#63913=CARTESIAN_POINT('Ctrl Pts',(-0.0746744627775051,0.595197229608512,
-3.2574800460273));
#63914=CARTESIAN_POINT('Ctrl Pts',(-0.169040544952571,0.567067057441793,
-3.25284350271205));
#63915=CARTESIAN_POINT('Ctrl Pts',(-0.263406627127637,0.538936885275074,
-3.2482069593968));
#63916=CARTESIAN_POINT('Ctrl Pts',(-0.350598733101911,0.486740737839038,
-3.24357041608154));
#63917=CARTESIAN_POINT('Ctrl Pts',(-0.419967670815699,0.416853582140291,
-3.23893387276629));
#63918=CARTESIAN_POINT('Ctrl Pts',(-0.489336608529489,0.346966426441542,
-3.23429732945104));
#63919=CARTESIAN_POINT('Ctrl Pts',(-0.540882377982793,0.259388262480081,
-3.22966078613579));
#63920=CARTESIAN_POINT('Ctrl Pts',(-0.568309445966046,0.164815433437894,
-3.22502424282053));
#63921=CARTESIAN_POINT('Ctrl Pts',(-0.583811226278298,0.111362865331991,
-3.22240366828719));
#63922=CARTESIAN_POINT('Ctrl Pts',(-0.591608260843235,0.0556758437625984,
-3.21978309375384));
#63923=CARTESIAN_POINT('Ctrl Pts',(-0.591627593882854,-5.87472452489096E-6,
-3.21716251922049));
#63924=CARTESIAN_POINT('Origin',(0.,0.,-1.97));
#63925=CARTESIAN_POINT('',(-0.591712848140847,9.68948221328342E-6,-3.01698748077951));
#63926=CARTESIAN_POINT('',(-0.591700856122533,1.27964970961225E-5,-3.04216251922049));
#63927=CARTESIAN_POINT('',(-0.591675,-7.2459289488551E-17,-1.97));
#63928=CARTESIAN_POINT('Ctrl Pts',(-0.591712848140847,9.68948221328342E-6,
-3.01698748077951));
#63929=CARTESIAN_POINT('Ctrl Pts',(-0.591720547203392,0.0099369683863286,
-3.01745488659624));
#63930=CARTESIAN_POINT('Ctrl Pts',(-0.591475882675022,0.0198638677682085,
-3.01792229241297));
#63931=CARTESIAN_POINT('Ctrl Pts',(-0.5909763364076,0.0297779242515645,
-3.0183896982297));
#63932=CARTESIAN_POINT('Ctrl Pts',(-0.586020968237206,0.128122768645358,
-3.02302624154495));
#63933=CARTESIAN_POINT('Ctrl Pts',(-0.555984929782598,0.225203856347231,
-3.0276627848602));
#63934=CARTESIAN_POINT('Ctrl Pts',(-0.504536667156429,0.309164206306557,
-3.03229932817546));
#63935=CARTESIAN_POINT('Ctrl Pts',(-0.453088404530261,0.393124556265883,
-3.03693587149071));
#63936=CARTESIAN_POINT('Ctrl Pts',(-0.380227917732533,0.463964168482661,
-3.04157241480596));
#63937=CARTESIAN_POINT('Ctrl Pts',(-0.294854009112401,0.513031059758399,
-3.04620895812121));
#63938=CARTESIAN_POINT('Ctrl Pts',(-0.209480100492271,0.562097951034135,
-3.05084550143647));
#63939=CARTESIAN_POINT('Ctrl Pts',(-0.111592770049739,0.589392121368831,
-3.05548204475172));
#63940=CARTESIAN_POINT('Ctrl Pts',(-0.0131474691464297,0.591580002215698,
-3.06011858806697));
#63941=CARTESIAN_POINT('Ctrl Pts',(0.0852978317568821,0.593767883062565,
-3.06475513138223));
#63942=CARTESIAN_POINT('Ctrl Pts',(0.18430110312097,0.570849474421601,-3.06939167469748));
#63943=CARTESIAN_POINT('Ctrl Pts',(0.271770598342017,0.525623911978235,
-3.07402821801273));
#63944=CARTESIAN_POINT('Ctrl Pts',(0.359240093563065,0.480398349534868,
-3.07866476132798));
#63945=CARTESIAN_POINT('Ctrl Pts',(0.435175812641071,0.412865633289098,
-3.08330130464324));
#63946=CARTESIAN_POINT('Ctrl Pts',(0.49030336028971,0.331273859299371,-3.08793784795849));
#63947=CARTESIAN_POINT('Ctrl Pts',(0.545430907938349,0.249682085309644,
-3.09257439127375));
#63948=CARTESIAN_POINT('Ctrl Pts',(0.579750284157621,0.15403125357596,-3.097210934589));
#63949=CARTESIAN_POINT('Ctrl Pts',(0.589069898153335,0.0560036610955033,
-3.10184747790425));
#63950=CARTESIAN_POINT('Ctrl Pts',(0.598389512149049,-0.0420239313849538,
-3.1064840212195));
#63951=CARTESIAN_POINT('Ctrl Pts',(0.582709363921205,-0.142428284612183,
-3.11112056453476));
#63952=CARTESIAN_POINT('Ctrl Pts',(0.543944545531601,-0.232946531102958,
-3.11575710785001));
#63953=CARTESIAN_POINT('Ctrl Pts',(0.505179727141996,-0.323464777593732,
-3.12039365116526));
#63954=CARTESIAN_POINT('Ctrl Pts',(0.443330238590631,-0.404096917348053,
-3.12503019448051));
#63955=CARTESIAN_POINT('Ctrl Pts',(0.365950055951575,-0.464994958591511,
-3.12966673779577));
#63956=CARTESIAN_POINT('Ctrl Pts',(0.28856987331252,-0.525892999834967,
-3.13430328111102));
#63957=CARTESIAN_POINT('Ctrl Pts',(0.195658996585775,-0.567056942567562,
-3.13893982442627));
#63958=CARTESIAN_POINT('Ctrl Pts',(0.0985650788603642,-0.583459236104572,
-3.14357636774153));
#63959=CARTESIAN_POINT('Ctrl Pts',(0.00147116113495045,-0.599861529641583,
-3.14821291105678));
#63960=CARTESIAN_POINT('Ctrl Pts',(-0.0998057975891291,-0.591502173983006,
-3.15284945437203));
#63961=CARTESIAN_POINT('Ctrl Pts',(-0.192896354314448,-0.559402137517078,
-3.15748599768729));
#63962=CARTESIAN_POINT('Ctrl Pts',(-0.285986911039766,-0.52730210105115,
-3.16212254100254));
#63963=CARTESIAN_POINT('Ctrl Pts',(-0.370891065766324,-0.471461383777871,
-3.16675908431779));
#63964=CARTESIAN_POINT('Ctrl Pts',(-0.437239064945378,-0.398700081580343,
-3.17139562763305));
#63965=CARTESIAN_POINT('Ctrl Pts',(-0.503587064124432,-0.325938779382816,
-3.1760321709483));
#63966=CARTESIAN_POINT('Ctrl Pts',(-0.551378907755982,-0.23625689226104,
-3.18066871426355));
#63967=CARTESIAN_POINT('Ctrl Pts',(-0.574777547680309,-0.14060770124389,
-3.1853052575788));
#63968=CARTESIAN_POINT('Ctrl Pts',(-0.586018316498532,-0.0946575756232986,
-3.18753266531237));
#63969=CARTESIAN_POINT('Ctrl Pts',(-0.591629457988783,-0.0473302755451445,
-3.18976007304594));
#63970=CARTESIAN_POINT('Ctrl Pts',(-0.591624439693044,-1.80568084665045E-6,
-3.19198748077951));
#63971=CARTESIAN_POINT('Ctrl Pts',(-0.591627593882854,-5.87472452489096E-6,
-3.21716251922049));
#63972=CARTESIAN_POINT('Ctrl Pts',(-0.591642466500989,-0.0428409876986071,
-3.21514655043859));
#63973=CARTESIAN_POINT('Ctrl Pts',(-0.587054499469894,-0.0856729623114073,
-3.21313058165668));
#63974=CARTESIAN_POINT('Ctrl Pts',(-0.577830478761204,-0.127482121445141,
-3.21111461287477));
#63975=CARTESIAN_POINT('Ctrl Pts',(-0.556616077059905,-0.223639353163076,
-3.20647806955952));
#63976=CARTESIAN_POINT('Ctrl Pts',(-0.510878907144102,-0.314386322476033,
-3.20184152624427));
#63977=CARTESIAN_POINT('Ctrl Pts',(-0.446205069971652,-0.388639664734763,
-3.19720498292902));
#63978=CARTESIAN_POINT('Ctrl Pts',(-0.381531232799202,-0.462893006993493,
-3.19256843961376));
#63979=CARTESIAN_POINT('Ctrl Pts',(-0.297920728370106,-0.520652722197995,
-3.18793189629851));
#63980=CARTESIAN_POINT('Ctrl Pts',(-0.205585310488494,-0.554864338000655,
-3.18329535298325));
#63981=CARTESIAN_POINT('Ctrl Pts',(-0.113249892606884,-0.589075953803315,
-3.178658809668));
#63982=CARTESIAN_POINT('Ctrl Pts',(-0.0121895612727601,-0.599739470204133,
-3.17402226635275));
#63983=CARTESIAN_POINT('Ctrl Pts',(0.0852526982634587,-0.585552500560244,
-3.1693857230375));
#63984=CARTESIAN_POINT('Ctrl Pts',(0.182694957799679,-0.571365530916356,
-3.16474917972224));
#63985=CARTESIAN_POINT('Ctrl Pts',(0.276519145537995,-0.532328075227762,
-3.16011263640699));
#63986=CARTESIAN_POINT('Ctrl Pts',(0.355266061314518,-0.473207966069491,
-3.15547609309174));
#63987=CARTESIAN_POINT('Ctrl Pts',(0.434012977091042,-0.414087856911221,
-3.15083954977648));
#63988=CARTESIAN_POINT('Ctrl Pts',(0.497682620905773,-0.334885094283273,
-3.14620300646123));
#63989=CARTESIAN_POINT('Ctrl Pts',(0.538498712351454,-0.2452730932438,-3.14156646314598));
#63990=CARTESIAN_POINT('Ctrl Pts',(0.579314803797134,-0.155661092204328,
-3.13692991983072));
#63991=CARTESIAN_POINT('Ctrl Pts',(0.597277342873764,-0.0556398527533296,
-3.13229337651547));
#63992=CARTESIAN_POINT('Ctrl Pts',(0.59019247812691,0.0425745491575879,
-3.12765683320022));
#63993=CARTESIAN_POINT('Ctrl Pts',(0.583107613380057,0.140788951068506,
-3.12302028988497));
#63994=CARTESIAN_POINT('Ctrl Pts',(0.55097534480972,0.237196515439342,-3.11838374656972));
#63995=CARTESIAN_POINT('Ctrl Pts',(0.497720141213799,0.320022521869433,
-3.11374720325446));
#63996=CARTESIAN_POINT('Ctrl Pts',(0.444464937617877,0.402848528299525,
-3.10911065993921));
#63997=CARTESIAN_POINT('Ctrl Pts',(0.37008679899637,0.47209297678887,-3.10447411662396));
#63998=CARTESIAN_POINT('Ctrl Pts',(0.283669885828859,0.519298709171704,
-3.0998375733087));
#63999=CARTESIAN_POINT('Ctrl Pts',(0.197252972661348,0.566504441554536,
-3.09520102999345));
#64000=CARTESIAN_POINT('Ctrl Pts',(0.0987972849478337,0.591671457830858,
-3.09056448667819));
#64001=CARTESIAN_POINT('Ctrl Pts',(0.000327690262219633,0.591725989029253,
-3.08592794336294));
#64002=CARTESIAN_POINT('Ctrl Pts',(-0.0981419044233951,0.591780520227648,
-3.08129140004769));
#64003=CARTESIAN_POINT('Ctrl Pts',(-0.196625406081108,0.566722566348117,
-3.07665485673244));
#64004=CARTESIAN_POINT('Ctrl Pts',(-0.283094550085985,0.519612576046009,
-3.07201831341718));
#64005=CARTESIAN_POINT('Ctrl Pts',(-0.36956369409086,0.472502585743902,
-3.06738177010193));
#64006=CARTESIAN_POINT('Ctrl Pts',(-0.444018480442898,0.403340559019219,
-3.06274522678668));
#64007=CARTESIAN_POINT('Ctrl Pts',(-0.497365387305842,0.320573587470437,
-3.05810868347143));
#64008=CARTESIAN_POINT('Ctrl Pts',(-0.550712294168785,0.237806615921655,
-3.05347214015617));
#64009=CARTESIAN_POINT('Ctrl Pts',(-0.582951321542635,0.141434699548774,
-3.04883559684092));
#64010=CARTESIAN_POINT('Ctrl Pts',(-0.590144961662373,0.0432282048906904,
-3.04419905352567));
#64011=CARTESIAN_POINT('Ctrl Pts',(-0.591198195640563,0.0288496127827775,
-3.04352020875727));
#64012=CARTESIAN_POINT('Ctrl Pts',(-0.591714546116039,0.0144316938796439,
-3.04284136398888));
#64013=CARTESIAN_POINT('Ctrl Pts',(-0.591700856122533,1.27964970961225E-5,
-3.04216251922049));
#64014=CARTESIAN_POINT('Origin',(0.,0.,-1.97));
#64015=CARTESIAN_POINT('',(-0.591649561283706,-1.37437984600031E-5,-2.84198748077951));
#64016=CARTESIAN_POINT('',(-0.591662271106711,-1.51681700886687E-5,-2.86716251922049));
#64017=CARTESIAN_POINT('',(-0.591675,-7.2459289488551E-17,-1.97));
#64018=CARTESIAN_POINT('Ctrl Pts',(-0.591649561283706,-1.37437984600031E-5,
-2.84198748077951));
#64019=CARTESIAN_POINT('Ctrl Pts',(-0.591592208586822,0.0671696477833834,
-2.84514970014654));
#64020=CARTESIAN_POINT('Ctrl Pts',(-0.580167345362705,0.134372049477458,
-2.84831191951356));
#64021=CARTESIAN_POINT('Ctrl Pts',(-0.557732407245809,0.197672246090027,
-2.85147413888059));
#64022=CARTESIAN_POINT('Ctrl Pts',(-0.524837610813068,0.290484941666613,
-2.85611068219584));
#64023=CARTESIAN_POINT('Ctrl Pts',(-0.468272995893203,0.374908549350676,
-2.8607472255111));
#64024=CARTESIAN_POINT('Ctrl Pts',(-0.394947071477179,0.440632007119412,
-2.86538376882635));
#64025=CARTESIAN_POINT('Ctrl Pts',(-0.321621147061154,0.506355464888148,
-2.8700203121416));
#64026=CARTESIAN_POINT('Ctrl Pts',(-0.231533913148968,0.553378772741556,
-2.87465685545685));
#64027=CARTESIAN_POINT('Ctrl Pts',(-0.135688157726274,0.575958747497883,
-2.87929339877211));
#64028=CARTESIAN_POINT('Ctrl Pts',(-0.0398424023035795,0.598538722254211,
-2.88392994208736));
#64029=CARTESIAN_POINT('Ctrl Pts',(0.0617618746296242,0.596675363913459,
-2.88856648540261));
#64030=CARTESIAN_POINT('Ctrl Pts',(0.156715253125765,0.570596253408843,
-2.89320302871787));
#64031=CARTESIAN_POINT('Ctrl Pts',(0.251668631621909,0.544517142904226,
-2.89783957203312));
#64032=CARTESIAN_POINT('Ctrl Pts',(0.339971111680989,0.494222280235743,
-2.90247611534837));
#64033=CARTESIAN_POINT('Ctrl Pts',(0.410837885905719,0.425854419339521,
-2.90711265866362));
#64034=CARTESIAN_POINT('Ctrl Pts',(0.481704660130446,0.357486558443301,
-2.91174920197888));
#64035=CARTESIAN_POINT('Ctrl Pts',(0.535135728520824,0.271045699319343,
-2.91638574529413));
#64036=CARTESIAN_POINT('Ctrl Pts',(0.564605297223316,0.177089280629439,
-2.92102228860939));
#64037=CARTESIAN_POINT('Ctrl Pts',(0.594074865925808,0.0831328619395355,
-2.92565883192464));
#64038=CARTESIAN_POINT('Ctrl Pts',(0.599582934940414,-0.0183391163163137,
-2.93029537523989));
#64039=CARTESIAN_POINT('Ctrl Pts',(0.580456777256368,-0.114933392465516,
-2.93493191855514));
#64040=CARTESIAN_POINT('Ctrl Pts',(0.561330619572321,-0.21152766861472,
-2.93956846187039));
#64041=CARTESIAN_POINT('Ctrl Pts',(0.517570235189621,-0.303244242657277,
-2.94420500518565));
#64042=CARTESIAN_POINT('Ctrl Pts',(0.454520290723326,-0.378881327446028,
-2.9488415485009));
#64043=CARTESIAN_POINT('Ctrl Pts',(0.391470346257031,-0.45451841223478,
-2.95347809181616));
#64044=CARTESIAN_POINT('Ctrl Pts',(0.309130841707141,-0.514076007769726,
-2.95811463513141));
#64045=CARTESIAN_POINT('Ctrl Pts',(0.217558297537912,-0.550280057914955,
-2.96275117844666));
#64046=CARTESIAN_POINT('Ctrl Pts',(0.125985753368682,-0.586484108060185,
-2.96738772176191));
#64047=CARTESIAN_POINT('Ctrl Pts',(0.0251801695801122,-0.599334612815697,
-2.97202426507717));
#64048=CARTESIAN_POINT('Ctrl Pts',(-0.0725465821226823,-0.587262078112317,
-2.97666080839242));
#64049=CARTESIAN_POINT('Ctrl Pts',(-0.170273333825474,-0.575189543408938,
-2.98129735170767));
#64050=CARTESIAN_POINT('Ctrl Pts',(-0.26492125344249,-0.538193969246669,
-2.98593389502292));
#64051=CARTESIAN_POINT('Ctrl Pts',(-0.34493053446614,-0.48079380337041,
-2.99057043833818));
#64052=CARTESIAN_POINT('Ctrl Pts',(-0.424939815489789,-0.423393637494151,
-2.99520698165343));
#64053=CARTESIAN_POINT('Ctrl Pts',(-0.490310457920072,-0.345588879903902,
-2.99984352496868));
#64054=CARTESIAN_POINT('Ctrl Pts',(-0.533058430192123,-0.256882200565921,
-3.00448006828394));
#64055=CARTESIAN_POINT('Ctrl Pts',(-0.57149701731779,-0.177117962845787,
-3.00864920578246));
#64056=CARTESIAN_POINT('Ctrl Pts',(-0.591644174518881,-0.0885390389592056,
-3.01281834328099));
#64057=CARTESIAN_POINT('Ctrl Pts',(-0.591712848140847,9.68948221328342E-6,
-3.01698748077951));
#64058=CARTESIAN_POINT('Ctrl Pts',(-0.591700856122533,1.27964970961225E-5,
-3.04216251922049));
#64059=CARTESIAN_POINT('Ctrl Pts',(-0.591621042783862,-0.0840500877960021,
-3.03820482067363));
#64060=CARTESIAN_POINT('Ctrl Pts',(-0.573525431531148,-0.168146230091878,
-3.03424712212677));
#64061=CARTESIAN_POINT('Ctrl Pts',(-0.538770040159903,-0.244676515627578,
-3.03028942357991));
#64062=CARTESIAN_POINT('Ctrl Pts',(-0.498053225672066,-0.334333668544475,
-3.02565288026465));
#64063=CARTESIAN_POINT('Ctrl Pts',(-0.434471343830764,-0.413606901434981,
-3.0210163369494));
#64064=CARTESIAN_POINT('Ctrl Pts',(-0.355789956250539,-0.472814192368202,
-3.01637979363415));
#64065=CARTESIAN_POINT('Ctrl Pts',(-0.277108568670313,-0.532021483301424,
-3.01174325031889));
#64066=CARTESIAN_POINT('Ctrl Pts',(-0.183327675351164,-0.571162832277359,
-3.00710670700364));
#64067=CARTESIAN_POINT('Ctrl Pts',(-0.0859011887009397,-0.585457717733161,
-3.00247016368839));
#64068=CARTESIAN_POINT('Ctrl Pts',(0.0115252979492829,-0.599752603188962,
-2.99783362037314));
#64069=CARTESIAN_POINT('Ctrl Pts',(0.11259737793058,-0.58920102512463,-2.99319707705788));
#64070=CARTESIAN_POINT('Ctrl Pts',(0.20497063107364,-0.555091698614589,
-2.98856053374263));
#64071=CARTESIAN_POINT('Ctrl Pts',(0.2973438842167,-0.520982372104548,-2.98392399042738));
#64072=CARTESIAN_POINT('Ctrl Pts',(0.381018310521524,-0.463315297148798,
-2.97928744711212));
#64073=CARTESIAN_POINT('Ctrl Pts',(0.44577434909727,-0.389133631494966,
-2.97465090379687));
#64074=CARTESIAN_POINT('Ctrl Pts',(0.510530387673018,-0.314951965841133,
-2.97001436048162));
#64075=CARTESIAN_POINT('Ctrl Pts',(0.556368038519687,-0.224255709489217,
-2.96537781716636));
#64076=CARTESIAN_POINT('Ctrl Pts',(0.577688928459145,-0.128122033270162,
-2.96074127385111));
#64077=CARTESIAN_POINT('Ctrl Pts',(0.599009818398603,-0.031988357051106,
-2.95610473053586));
#64078=CARTESIAN_POINT('Ctrl Pts',(0.59581394743085,0.0695827390350898,
-2.95146818722061));
#64079=CARTESIAN_POINT('Ctrl Pts',(0.568491642677283,0.164185887577588,
-2.94683164390535));
#64080=CARTESIAN_POINT('Ctrl Pts',(0.541169337923717,0.258789036120085,
-2.9421951005901));
#64081=CARTESIAN_POINT('Ctrl Pts',(0.489720599384338,0.346424237118884,
-2.93755855727485));
#64082=CARTESIAN_POINT('Ctrl Pts',(0.420429109415626,0.416388181183784,
-2.9329220139596));
#64083=CARTESIAN_POINT('Ctrl Pts',(0.351137619446914,0.486352125248683,
-2.92828547064434));
#64084=CARTESIAN_POINT('Ctrl Pts',(0.264003378048868,0.538644812379682,
-2.92364892732909));
#64085=CARTESIAN_POINT('Ctrl Pts',(0.169668510001653,0.566879484712028,
-2.91901238401383));
#64086=CARTESIAN_POINT('Ctrl Pts',(0.0753336419544367,0.595114157044375,
-2.91437584069858));
#64087=CARTESIAN_POINT('Ctrl Pts',(-0.0262018527419497,0.599290814578069,
-2.90973929738333));
#64088=CARTESIAN_POINT('Ctrl Pts',(-0.122536954845961,0.578899342002247,
-2.90510275406808));
#64089=CARTESIAN_POINT('Ctrl Pts',(-0.218872056949972,0.558507869426425,
-2.90046621075283));
#64090=CARTESIAN_POINT('Ctrl Pts',(-0.310006766461608,0.513548266741087,
-2.89582966743757));
#64091=CARTESIAN_POINT('Ctrl Pts',(-0.384810362152732,0.449511666871328,
-2.89119312412232));
#64092=CARTESIAN_POINT('Ctrl Pts',(-0.459613957843854,0.385475067001569,
-2.88655658080706));
#64093=CARTESIAN_POINT('Ctrl Pts',(-0.518086439714465,0.30236146994739,
-2.88192003749181));
#64094=CARTESIAN_POINT('Ctrl Pts',(-0.553086281789371,0.210321939820753,
-2.87728349417656));
#64095=CARTESIAN_POINT('Ctrl Pts',(-0.57855299272904,0.143351805962961,
-2.87390983585787));
#64096=CARTESIAN_POINT('Ctrl Pts',(-0.59159244086834,0.071655960936958,
-2.87053617753918));
#64097=CARTESIAN_POINT('Ctrl Pts',(-0.591662271106711,-1.51681700886687E-5,
-2.86716251922049));
#64098=CARTESIAN_POINT('Origin',(0.,0.,-1.97));
#64099=CARTESIAN_POINT('',(-0.591664998266214,1.53149428433475E-5,-2.66698748077951));
#64100=CARTESIAN_POINT('',(-0.591651969453636,1.41180927115857E-5,-2.69216251922049));
#64101=CARTESIAN_POINT('',(-0.591675,-7.2459289488551E-17,-1.97));
#64102=CARTESIAN_POINT('Ctrl Pts',(-0.591664998266214,1.53149428433474E-5,
-2.66698748077951));
#64103=CARTESIAN_POINT('Ctrl Pts',(-0.591690704561656,0.0259434623775831,
-2.66820797038158));
#64104=CARTESIAN_POINT('Ctrl Pts',(-0.590018051085986,0.0518683175442941,
-2.66942845998365));
#64105=CARTESIAN_POINT('Ctrl Pts',(-0.586620331737737,0.0775650782142885,
-2.67064894958572));
#64106=CARTESIAN_POINT('Ctrl Pts',(-0.573712665089448,0.175185036390063,
-2.67528549290097));
#64107=CARTESIAN_POINT('Ctrl Pts',(-0.535909194301578,0.269513180609145,
-2.67992203621623));
#64108=CARTESIAN_POINT('Ctrl Pts',(-0.477827039426967,0.34902876007421,
-2.68455857953148));
#64109=CARTESIAN_POINT('Ctrl Pts',(-0.419744884552355,0.428544339539276,
-2.68919512284673));
#64110=CARTESIAN_POINT('Ctrl Pts',(-0.341384045591001,0.493247354250325,
-2.69383166616199));
#64111=CARTESIAN_POINT('Ctrl Pts',(-0.252315109406633,0.535235313232974,
-2.69846820947724));
#64112=CARTESIAN_POINT('Ctrl Pts',(-0.163246173222264,0.577223272215623,
-2.70310475279249));
#64113=CARTESIAN_POINT('Ctrl Pts',(-0.0634691398148823,0.596496175469871,
-2.70774129610775));
#64114=CARTESIAN_POINT('Ctrl Pts',(0.0348297409247821,0.590700130449955,
-2.712377839423));
#64115=CARTESIAN_POINT('Ctrl Pts',(0.133128621664444,0.584904085430038,
-2.71701438273825));
#64116=CARTESIAN_POINT('Ctrl Pts',(0.229949349736388,0.554039092135958,
-2.72165092605351));
#64117=CARTESIAN_POINT('Ctrl Pts',(0.313466743066199,0.50187484092944,-2.72628746936876));
#64118=CARTESIAN_POINT('Ctrl Pts',(0.396984136396013,0.449710589722921,
-2.73092401268401));
#64119=CARTESIAN_POINT('Ctrl Pts',(0.467198194983692,0.376247080603962,
-2.73556055599926));
#64120=CARTESIAN_POINT('Ctrl Pts',(0.515533337509855,0.290456765943627,
-2.74019709931452));
#64121=CARTESIAN_POINT('Ctrl Pts',(0.563868480036017,0.204666451283292,
-2.74483364262977));
#64122=CARTESIAN_POINT('Ctrl Pts',(0.590324706500662,0.106549331081582,
-2.74947018594502));
#64123=CARTESIAN_POINT('Ctrl Pts',(0.591670790479691,0.00808892203070965,
-2.75410672926028));
#64124=CARTESIAN_POINT('Ctrl Pts',(0.59301687445872,-0.0903714870201624,
-2.75874327257553));
#64125=CARTESIAN_POINT('Ctrl Pts',(0.569252815952134,-0.189175184920196,
-2.76337981589078));
#64126=CARTESIAN_POINT('Ctrl Pts',(0.523281033938426,-0.276254799934433,
-2.76801635920603));
#64127=CARTESIAN_POINT('Ctrl Pts',(0.477309251924718,-0.363334414948667,
-2.77265290252129));
#64128=CARTESIAN_POINT('Ctrl Pts',(0.409129746403889,-0.438689947077106,
-2.77728944583654));
#64129=CARTESIAN_POINT('Ctrl Pts',(0.327069608925263,-0.49311786206135,
-2.78192598915179));
#64130=CARTESIAN_POINT('Ctrl Pts',(0.245009471446634,-0.547545777045597,
-2.78656253246705));
#64131=CARTESIAN_POINT('Ctrl Pts',(0.149068702010206,-0.581046074885647,
-2.7911990757823));
#64132=CARTESIAN_POINT('Ctrl Pts',(0.0509650091019394,-0.589527202776699,
-2.79583561909755));
#64133=CARTESIAN_POINT('Ctrl Pts',(-0.0471386838063262,-0.598008330667752,
-2.80047216241281));
#64134=CARTESIAN_POINT('Ctrl Pts',(-0.147405300186431,-0.581470288609808,
-2.80510870572806));
#64135=CARTESIAN_POINT('Ctrl Pts',(-0.237588795020007,-0.541932947372111,
-2.80974524904331));
#64136=CARTESIAN_POINT('Ctrl Pts',(-0.327772289853581,-0.502395606134414,
-2.81438179235857));
#64137=CARTESIAN_POINT('Ctrl Pts',(-0.407872663140626,-0.439858965716965,
-2.81901833567382));
#64138=CARTESIAN_POINT('Ctrl Pts',(-0.468106870307834,-0.361960927362451,
-2.82365487898907));
#64139=CARTESIAN_POINT('Ctrl Pts',(-0.528341077475043,-0.284062889007937,
-2.82829142230432));
#64140=CARTESIAN_POINT('Ctrl Pts',(-0.568709118522414,-0.190803452716357,
-2.83292796561958));
#64141=CARTESIAN_POINT('Ctrl Pts',(-0.584280650073291,-0.0935728428360127,
-2.83756450893483));
#64142=CARTESIAN_POINT('Ctrl Pts',(-0.589232071922516,-0.0626555393837431,
-2.83903883288306));
#64143=CARTESIAN_POINT('Ctrl Pts',(-0.591676300875334,-0.0313367077158365,
-2.84051315683128));
#64144=CARTESIAN_POINT('Ctrl Pts',(-0.591649561283706,-1.37437984600031E-5,
-2.84198748077951));
#64145=CARTESIAN_POINT('Ctrl Pts',(-0.591662271106711,-1.51681700886687E-5,
-2.86716251922049));
#64146=CARTESIAN_POINT('Ctrl Pts',(-0.591688411145806,-0.0268443207059845,
-2.86589963422393));
#64147=CARTESIAN_POINT('Ctrl Pts',(-0.589897142504733,-0.0536700098456575,
-2.86463674922736));
#64148=CARTESIAN_POINT('Ctrl Pts',(-0.586260015865897,-0.08024305122859,
-2.8633738642308));
#64149=CARTESIAN_POINT('Ctrl Pts',(-0.572906705588316,-0.177803048952202,
-2.85873732091555));
#64150=CARTESIAN_POINT('Ctrl Pts',(-0.534672882753952,-0.271957581200331,
-2.85410077760029));
#64151=CARTESIAN_POINT('Ctrl Pts',(-0.476228228384843,-0.351207101242258,
-2.84946423428504));
#64152=CARTESIAN_POINT('Ctrl Pts',(-0.417783574015732,-0.430456621284187,
-2.84482769096979));
#64153=CARTESIAN_POINT('Ctrl Pts',(-0.339128088111874,-0.494801129119914,
-2.84019114765453));
#64154=CARTESIAN_POINT('Ctrl Pts',(-0.249868344187915,-0.536381919947294,
-2.83555460433928));
#64155=CARTESIAN_POINT('Ctrl Pts',(-0.160608600263956,-0.577962710774674,
-2.83091806102403));
#64156=CARTESIAN_POINT('Ctrl Pts',(-0.0607445983199012,-0.596779784593707,
-2.82628151770878));
#64157=CARTESIAN_POINT('Ctrl Pts',(0.0375267898670622,-0.590534921504079,
-2.82164497439352));
#64158=CARTESIAN_POINT('Ctrl Pts',(0.135798178054023,-0.584290058414453,
-2.81700843107827));
#64159=CARTESIAN_POINT('Ctrl Pts',(0.232476952483891,-0.552983258416165,
-2.81237188776302));
#64160=CARTESIAN_POINT('Ctrl Pts',(0.315755268564591,-0.500438171852686,
-2.80773534444776));
#64161=CARTESIAN_POINT('Ctrl Pts',(0.39903358464529,-0.447893085289208,
-2.80309880113251));
#64162=CARTESIAN_POINT('Ctrl Pts',(0.468911442376825,-0.374109712160539,
-2.79846225781726));
#64163=CARTESIAN_POINT('Ctrl Pts',(0.516854322270441,-0.288099571370592,
-2.793825714502));
#64164=CARTESIAN_POINT('Ctrl Pts',(0.564797202164058,-0.202089430580642,
-2.78918917118675));
#64165=CARTESIAN_POINT('Ctrl Pts',(0.590805104219755,-0.103852522129414,
-2.7845526278715));
#64166=CARTESIAN_POINT('Ctrl Pts',(0.591701558033863,-0.00538699302526537,
-2.77991608455625));
#64167=CARTESIAN_POINT('Ctrl Pts',(0.592598011847971,0.0930785360788831,
-2.77527954124099));
#64168=CARTESIAN_POINT('Ctrl Pts',(0.568383017420491,0.191772685835952,
-2.77064299792574));
#64169=CARTESIAN_POINT('Ctrl Pts',(0.52201406870688,0.278641464153569,-2.76600645461049));
#64170=CARTESIAN_POINT('Ctrl Pts',(0.475645119993269,0.365510242471186,
-2.76136991129523));
#64171=CARTESIAN_POINT('Ctrl Pts',(0.407122216993528,0.440553649349351,
-2.75673336797998));
#64172=CARTESIAN_POINT('Ctrl Pts',(0.32481439204583,0.494606271890535,-2.75209682466473));
#64173=CARTESIAN_POINT('Ctrl Pts',(0.242506567098132,0.548658894431719,
-2.74746028134948));
#64174=CARTESIAN_POINT('Ctrl Pts',(0.146413820202477,0.581720732635921,
-2.74282373803422));
#64175=CARTESIAN_POINT('Ctrl Pts',(0.0482724215842585,0.589753784886496,
-2.73818719471897));
#64176=CARTESIAN_POINT('Ctrl Pts',(-0.0498689770339597,0.59778683713707,
-2.73355065140372));
#64177=CARTESIAN_POINT('Ctrl Pts',(-0.150059027374741,0.580791103434017,
-2.72891410808846));
#64178=CARTESIAN_POINT('Ctrl Pts',(-0.240061035799051,0.540842354632699,
-2.72427756477321));
#64179=CARTESIAN_POINT('Ctrl Pts',(-0.330063044223363,0.500893605831381,
-2.71964102145796));
#64180=CARTESIAN_POINT('Ctrl Pts',(-0.409877010731205,0.437991841931797,
-2.7150044781427));
#64181=CARTESIAN_POINT('Ctrl Pts',(-0.469754870989334,0.359819558466949,
-2.71036793482745));
#64182=CARTESIAN_POINT('Ctrl Pts',(-0.529632731247464,0.2816472750021,-2.7057313915122));
#64183=CARTESIAN_POINT('Ctrl Pts',(-0.569574485255881,0.188204471971986,
-2.70109484819695));
#64184=CARTESIAN_POINT('Ctrl Pts',(-0.584701854128169,0.090903769188283,
-2.69645830488169));
#64185=CARTESIAN_POINT('Ctrl Pts',(-0.58937372063696,0.0608538709902104,
-2.69502637632796));
#64186=CARTESIAN_POINT('Ctrl Pts',(-0.591678808869539,0.0304360090776029,
-2.69359444777423));
#64187=CARTESIAN_POINT('Ctrl Pts',(-0.591651969453636,1.41180927115857E-5,
-2.69216251922049));
#64188=CARTESIAN_POINT('Origin',(0.,0.,-1.97));
#64189=CARTESIAN_POINT('',(-0.591698200799366,-1.32858733848662E-5,-2.49198748077951));
#64190=CARTESIAN_POINT('',(-0.591710646980237,-1.03961135234074E-5,-2.51716251922049));
#64191=CARTESIAN_POINT('',(-0.591675,-7.2459289488551E-17,-1.97));
#64192=CARTESIAN_POINT('Ctrl Pts',(-0.591698200799366,-1.32858733848662E-5,
-2.49198748077951));
#64193=CARTESIAN_POINT('Ctrl Pts',(-0.591617318058343,0.0831501844531302,
-2.49590278393188));
#64194=CARTESIAN_POINT('Ctrl Pts',(-0.573918730141509,0.166346986995152,
-2.49981808708425));
#64195=CARTESIAN_POINT('Ctrl Pts',(-0.539881730934194,0.24221368988969,
-2.50373339023661));
#64196=CARTESIAN_POINT('Ctrl Pts',(-0.499574757245456,0.332055840156694,
-2.50836993355187));
#64197=CARTESIAN_POINT('Ctrl Pts',(-0.436355536734211,0.411618591198725,
-2.51300647686712));
#64198=CARTESIAN_POINT('Ctrl Pts',(-0.357945337439186,0.471184560837925,
-2.51764302018237));
#64199=CARTESIAN_POINT('Ctrl Pts',(-0.279535138144161,0.530750530477125,
-2.52227956349763));
#64200=CARTESIAN_POINT('Ctrl Pts',(-0.185933960065355,0.570319718713494,
-2.52691610681288));
#64201=CARTESIAN_POINT('Ctrl Pts',(-0.0885737661223129,0.585059349913657,
-2.53155265012813));
#64202=CARTESIAN_POINT('Ctrl Pts',(0.00878642782072664,0.599798981113819,
-2.53618919344339));
#64203=CARTESIAN_POINT('Ctrl Pts',(0.109905637628004,0.589709055277775,
-2.54082573675864));
#64204=CARTESIAN_POINT('Ctrl Pts',(0.202433686937452,0.556021903668723,
-2.54546228007389));
#64205=CARTESIAN_POINT('Ctrl Pts',(0.294961736246904,0.522334752059669,
-2.55009882338915));
#64206=CARTESIAN_POINT('Ctrl Pts',(0.378898625058528,0.465050374677606,
-2.5547353667044));
#64207=CARTESIAN_POINT('Ctrl Pts',(0.443992736670785,0.39116518857136,-2.55937191001965));
#64208=CARTESIAN_POINT('Ctrl Pts',(0.509086848283043,0.317280002465114,
-2.5640084533349));
#64209=CARTESIAN_POINT('Ctrl Pts',(0.555338182695934,0.226794007634685,
-2.56864499665016));
#64210=CARTESIAN_POINT('Ctrl Pts',(0.577097841563945,0.1307586946582,-2.57328153996541));
#64211=CARTESIAN_POINT('Ctrl Pts',(0.598857500431956,0.0347233816817167,
-2.57791808328066));
#64212=CARTESIAN_POINT('Ctrl Pts',(0.596125483755088,-0.0668612494408195,
-2.58255462659592));
#64213=CARTESIAN_POINT('Ctrl Pts',(0.569235465894994,-0.161588178199368,
-2.58719116991117));
#64214=CARTESIAN_POINT('Ctrl Pts',(0.542345448034899,-0.256315106957918,
-2.59182771322642));
#64215=CARTESIAN_POINT('Ctrl Pts',(0.491297428991578,-0.344184333352478,
-2.59646425654168));
#64216=CARTESIAN_POINT('Ctrl Pts',(0.42232614931849,-0.414463965343548,
-2.60110079985693));
#64217=CARTESIAN_POINT('Ctrl Pts',(0.353354869645401,-0.484743597334618,
-2.60573734317218));
#64218=CARTESIAN_POINT('Ctrl Pts',(0.266460329342544,-0.537433634922199,
-2.61037388648743));
#64219=CARTESIAN_POINT('Ctrl Pts',(0.172255377340268,-0.566098789915544,
-2.61501042980269));
#64220=CARTESIAN_POINT('Ctrl Pts',(0.078050425337992,-0.594763944908889,
-2.61964697311794));
#64221=CARTESIAN_POINT('Ctrl Pts',(-0.0234649383637043,-0.599404217307997,
-2.62428351643319));
#64222=CARTESIAN_POINT('Ctrl Pts',(-0.119892153218662,-0.579452868284448,
-2.62892005974845));
#64223=CARTESIAN_POINT('Ctrl Pts',(-0.21631936807362,-0.559501519260899,
-2.6335566030637));
#64224=CARTESIAN_POINT('Ctrl Pts',(-0.30765843408184,-0.514958548814693,
-2.63819314637895));
#64225=CARTESIAN_POINT('Ctrl Pts',(-0.382753670971514,-0.451264204567913,
-2.6428296896942));
#64226=CARTESIAN_POINT('Ctrl Pts',(-0.457848907861189,-0.387569860321132,
-2.64746623300946));
#64227=CARTESIAN_POINT('Ctrl Pts',(-0.516700315632318,-0.304724142273775,
-2.65210277632471));
#64228=CARTESIAN_POINT('Ctrl Pts',(-0.552120088263528,-0.212845397183861,
-2.65673931963997));
#64229=CARTESIAN_POINT('Ctrl Pts',(-0.578216220142391,-0.145152138006409,
-2.66015537335315));
#64230=CARTESIAN_POINT('Ctrl Pts',(-0.591593048381636,-0.0725555157877893,
-2.66357142706633));
#64231=CARTESIAN_POINT('Ctrl Pts',(-0.591664998266214,1.53149428433474E-5,
-2.66698748077951));
#64232=CARTESIAN_POINT('Ctrl Pts',(-0.591651969453636,1.41180927115857E-5,
-2.69216251922049));
#64233=CARTESIAN_POINT('Ctrl Pts',(-0.591591903615735,-0.0680691956098775,
-2.68895790445897));
#64234=CARTESIAN_POINT('Ctrl Pts',(-0.57985234370179,-0.13617268898052,
-2.68575328969745));
#64235=CARTESIAN_POINT('Ctrl Pts',(-0.556823927312267,-0.200217050837582,
-2.68254867493593));
#64236=CARTESIAN_POINT('Ctrl Pts',(-0.523505647887919,-0.292878565542456,
-2.67791213162068));
#64237=CARTESIAN_POINT('Ctrl Pts',(-0.466556105303064,-0.377042992414913,
-2.67327558830543));
#64238=CARTESIAN_POINT('Ctrl Pts',(-0.392930821619261,-0.442430924433598,
-2.66863904499017));
#64239=CARTESIAN_POINT('Ctrl Pts',(-0.319305537935459,-0.507818856452282,
-2.66400250167492));
#64240=CARTESIAN_POINT('Ctrl Pts',(-0.229004513152709,-0.554430293617193,
-2.65936595835967));
#64241=CARTESIAN_POINT('Ctrl Pts',(-0.133056646565889,-0.576572356498467,
-2.65472941504442));
#64242=CARTESIAN_POINT('Ctrl Pts',(-0.0371087799790665,-0.598714419379742,
-2.65009287172916));
#64243=CARTESIAN_POINT('Ctrl Pts',(0.0644859284118255,-0.596387107977379,
-2.64545632841391));
#64244=CARTESIAN_POINT('Ctrl Pts',(0.159319227311396,-0.569874668047682,
-2.64081978509866));
#64245=CARTESIAN_POINT('Ctrl Pts',(0.254152526210965,-0.543362228117985,
-2.6361832417834));
#64246=CARTESIAN_POINT('Ctrl Pts',(0.342224415619212,-0.492664659660956,
-2.63154669846815));
#64247=CARTESIAN_POINT('Ctrl Pts',(0.412778251286195,-0.423973901011214,
-2.6269101551529));
#64248=CARTESIAN_POINT('Ctrl Pts',(0.483332086953178,-0.355283142361472,
-2.62227361183765));
#64249=CARTESIAN_POINT('Ctrl Pts',(0.536367868878897,-0.268599193519018,
-2.61763706852239));
#64250=CARTESIAN_POINT('Ctrl Pts',(0.565408081450532,-0.174509182864352,
-2.61300052520714));
#64251=CARTESIAN_POINT('Ctrl Pts',(0.594448294022167,-0.0804191722096898,
-2.60836398189189));
#64252=CARTESIAN_POINT('Ctrl Pts',(0.599492937239718,0.0210769002571867,
-2.60372743857663));
#64253=CARTESIAN_POINT('Ctrl Pts',(0.579925884518147,0.117582830121581,
-2.59909089526138));
#64254=CARTESIAN_POINT('Ctrl Pts',(0.560358831796575,0.214088759985979,
-2.59445435194613));
#64255=CARTESIAN_POINT('Ctrl Pts',(0.516180083135882,0.305604547247894,
-2.58981780863087));
#64256=CARTESIAN_POINT('Ctrl Pts',(0.452785401996388,0.380952927817237,
-2.58518126531562));
#64257=CARTESIAN_POINT('Ctrl Pts',(0.389390720856894,0.45630130838658,-2.58054472200037));
#64258=CARTESIAN_POINT('Ctrl Pts',(0.306780107238598,0.515482282263348,
-2.57590817868511));
#64259=CARTESIAN_POINT('Ctrl Pts',(0.215043193462692,0.551267791929587,
-2.57127163536986));
#64260=CARTESIAN_POINT('Ctrl Pts',(0.123306279686785,0.587053301595827,
-2.56663509205461));
#64261=CARTESIAN_POINT('Ctrl Pts',(0.0224430657532648,0.599443347051538,
-2.56199854873936));
#64262=CARTESIAN_POINT('Ctrl Pts',(-0.075227537985446,0.586924672340671,
-2.5573620054241));
#64263=CARTESIAN_POINT('Ctrl Pts',(-0.172898141724155,0.574405997629804,
-2.55272546210885));
#64264=CARTESIAN_POINT('Ctrl Pts',(-0.267376135268055,0.536978602752358,
-2.5480889187936));
#64265=CARTESIAN_POINT('Ctrl Pts',(-0.347122465999695,0.479213675798017,
-2.54345237547834));
#64266=CARTESIAN_POINT('Ctrl Pts',(-0.426868796731334,0.421448748843675,
-2.53881583216309));
#64267=CARTESIAN_POINT('Ctrl Pts',(-0.491883464650713,0.343346289812437,
-2.53417928884784));
#64268=CARTESIAN_POINT('Ctrl Pts',(-0.534225915075338,0.254445328382098,
-2.52954274553259));
#64269=CARTESIAN_POINT('Ctrl Pts',(-0.571912691855857,0.175319282170792,
-2.52541600342855));
#64270=CARTESIAN_POINT('Ctrl Pts',(-0.59163890281563,0.0876388361461731,
-2.52128926132452));
#64271=CARTESIAN_POINT('Ctrl Pts',(-0.591710646980237,-1.03961135234074E-5,
-2.51716251922049));
#64272=CARTESIAN_POINT('Origin',(0.,0.,-1.97));
#64273=CARTESIAN_POINT('',(-0.591628625190756,6.64897484074778E-6,-2.31698748077951));
#64274=CARTESIAN_POINT('',(-0.591624801665701,2.64146101175725E-6,-2.34216251922049));
#64275=CARTESIAN_POINT('',(-0.591675,-7.2459289488551E-17,-1.97));
#64276=CARTESIAN_POINT('Ctrl Pts',(-0.591628625190756,6.64897484074778E-6,
-2.31698748077951));
#64277=CARTESIAN_POINT('Ctrl Pts',(-0.591645139193398,0.041940739843989,
-2.31896105416692));
#64278=CARTESIAN_POINT('Ctrl Pts',(-0.58724964040398,0.083871419065752,
-2.32093462755434));
#64279=CARTESIAN_POINT('Ctrl Pts',(-0.57840659812157,0.124842149196146,
-2.32290820094175));
#64280=CARTESIAN_POINT('Ctrl Pts',(-0.557631516311841,0.22109525339722,
-2.327544744257));
#64281=CARTESIAN_POINT('Ctrl Pts',(-0.512309216138202,0.312050133983124,
-2.33218128757225));
#64282=CARTESIAN_POINT('Ctrl Pts',(-0.447975128517742,0.386598033098972,
-2.33681783088751));
#64283=CARTESIAN_POINT('Ctrl Pts',(-0.383641040897284,0.461145932214817,
-2.34145437420276));
#64284=CARTESIAN_POINT('Ctrl Pts',(-0.300295165830006,0.519286849860608,
-2.34609091751801));
#64285=CARTESIAN_POINT('Ctrl Pts',(-0.208116936660901,0.553919755597653,
-2.35072746083327));
#64286=CARTESIAN_POINT('Ctrl Pts',(-0.115938707491793,0.588552661334699,
-2.35536400414852));
#64287=CARTESIAN_POINT('Ctrl Pts',(-0.0149281242208578,0.599677555162998,
-2.36000054746377));
#64288=CARTESIAN_POINT('Ctrl Pts',(0.0825779038721678,0.585935700191207,
-2.36463709077902));
#64289=CARTESIAN_POINT('Ctrl Pts',(0.180083931965194,0.572193845219415,
-2.36927363409428));
#64290=CARTESIAN_POINT('Ctrl Pts',(0.27408540488031,0.533585241447532,-2.37391017740953));
#64291=CARTESIAN_POINT('Ctrl Pts',(0.353101469760693,0.47482534369947,-2.37854672072478));
#64292=CARTESIAN_POINT('Ctrl Pts',(0.432117534641076,0.416065445951407,
-2.38318326404004));
#64293=CARTESIAN_POINT('Ctrl Pts',(0.496148191486726,0.337154254227165,
-2.38781980735529));
#64294=CARTESIAN_POINT('Ctrl Pts',(0.537373067629286,0.247729572625416,
-2.39245635067054));
#64295=CARTESIAN_POINT('Ctrl Pts',(0.578597943771846,0.15830489102367,-2.39709289398579));
#64296=CARTESIAN_POINT('Ctrl Pts',(0.597017039211317,0.0583667195444171,
-2.40172943730105));
#64297=CARTESIAN_POINT('Ctrl Pts',(0.590380741064641,-0.0398790113524088,
-2.4063659806163));
#64298=CARTESIAN_POINT('Ctrl Pts',(0.583744442917966,-0.138124742249238,
-2.41100252393155));
#64299=CARTESIAN_POINT('Ctrl Pts',(0.552052751185142,-0.234678032563639,
-2.41563906724681));
#64300=CARTESIAN_POINT('Ctrl Pts',(0.499176324891873,-0.317746363683244,
-2.42027561056206));
#64301=CARTESIAN_POINT('Ctrl Pts',(0.446299898598605,-0.400814694802848,
-2.42491215387731));
#64302=CARTESIAN_POINT('Ctrl Pts',(0.372238737744891,-0.470398066727654,
-2.42954869719257));
#64303=CARTESIAN_POINT('Ctrl Pts',(0.286038288788097,-0.517997926939537,
-2.43418524050782));
#64304=CARTESIAN_POINT('Ctrl Pts',(0.199837839831306,-0.565597787151419,
-2.43882178382307));
#64305=CARTESIAN_POINT('Ctrl Pts',(0.101498102771434,-0.591214135650378,
-2.44345832713832));
#64306=CARTESIAN_POINT('Ctrl Pts',(0.00302978357031825,-0.59171832435543,
-2.44809487045358));
#64307=CARTESIAN_POINT('Ctrl Pts',(-0.0954385356308003,-0.592222513060482,
-2.45273141376883));
#64308=CARTESIAN_POINT('Ctrl Pts',(-0.194035436973163,-0.567614541971626,
-2.45736795708408));
#64309=CARTESIAN_POINT('Ctrl Pts',(-0.2807188057819,-0.520899901177631,
-2.46200450039934));
#64310=CARTESIAN_POINT('Ctrl Pts',(-0.367402174590638,-0.474185260383635,
-2.46664104371459));
#64311=CARTESIAN_POINT('Ctrl Pts',(-0.44217201086575,-0.4053639498845,-2.47127758702984));
#64312=CARTESIAN_POINT('Ctrl Pts',(-0.495896314205729,-0.32284144796425,
-2.4759141303451));
#64313=CARTESIAN_POINT('Ctrl Pts',(-0.549620617545708,-0.240318946044,-2.48055067366035));
#64314=CARTESIAN_POINT('Ctrl Pts',(-0.582299387950553,-0.144095252702636,
-2.4851872169756));
#64315=CARTESIAN_POINT('Ctrl Pts',(-0.589941409719859,-0.0459226312859645,
-2.48982376029085));
#64316=CARTESIAN_POINT('Ctrl Pts',(-0.591130168812766,-0.0306513326811538,
-2.49054500045374));
#64317=CARTESIAN_POINT('Ctrl Pts',(-0.591713100253902,-0.015332874817107,
-2.49126624061662));
#64318=CARTESIAN_POINT('Ctrl Pts',(-0.591698200799366,-1.32858733848662E-5,
-2.49198748077951));
#64319=CARTESIAN_POINT('Ctrl Pts',(-0.591710646980237,-1.03961135234074E-5,
-2.51716251922049));
#64320=CARTESIAN_POINT('Ctrl Pts',(-0.591719509967333,-0.0108382316414618,
-2.51665271800927));
#64321=CARTESIAN_POINT('Ctrl Pts',(-0.59142842332184,-0.0216655908116636,
-2.51614291679805));
#64322=CARTESIAN_POINT('Ctrl Pts',(-0.590834193531263,-0.0324762871618411,
-2.51563311558682));
#64323=CARTESIAN_POINT('Ctrl Pts',(-0.585429788632694,-0.130797477445996,
-2.51099657227157));
#64324=CARTESIAN_POINT('Ctrl Pts',(-0.554950745905688,-0.227740394184864,
-2.50636002895632));
#64325=CARTESIAN_POINT('Ctrl Pts',(-0.503119617709414,-0.311464931813341,
-2.50172348564107));
#64326=CARTESIAN_POINT('Ctrl Pts',(-0.451288489513141,-0.395189469441816,
-2.49708694232582));
#64327=CARTESIAN_POINT('Ctrl Pts',(-0.3781052758476,-0.4656956279599,-2.49245039901056));
#64328=CARTESIAN_POINT('Ctrl Pts',(-0.292508195249456,-0.514372150476152,
-2.48781385569531));
#64329=CARTESIAN_POINT('Ctrl Pts',(-0.206911114651311,-0.563048672992405,
-2.48317731238005));
#64330=CARTESIAN_POINT('Ctrl Pts',(-0.108900167120564,-0.589895559506825,
-2.4785407690648));
#64331=CARTESIAN_POINT('Ctrl Pts',(-0.0104459019694992,-0.591633870400943,
-2.47390422574955));
#64332=CARTESIAN_POINT('Ctrl Pts',(0.0880083631815653,-0.593372181295061,
-2.4692676824343));
#64333=CARTESIAN_POINT('Ctrl Pts',(0.186905945952945,-0.570001916568875,
-2.46463113911904));
#64334=CARTESIAN_POINT('Ctrl Pts',(0.274168007997934,-0.524377399268885,
-2.45999459580379));
#64335=CARTESIAN_POINT('Ctrl Pts',(0.361430070042924,-0.478752881968895,
-2.45535805248854));
#64336=CARTESIAN_POINT('Ctrl Pts',(0.437056611361525,-0.4108741120951,-2.45072150917328));
#64337=CARTESIAN_POINT('Ctrl Pts',(0.491810998037018,-0.329031450903083,
-2.44608496585803));
#64338=CARTESIAN_POINT('Ctrl Pts',(0.54656538471251,-0.247188789711066,
-2.44144842254278));
#64339=CARTESIAN_POINT('Ctrl Pts',(0.580447616744896,-0.151382237200826,
-2.43681187922752));
#64340=CARTESIAN_POINT('Ctrl Pts',(0.589319493866015,-0.053313109298369,
-2.43217533591227));
#64341=CARTESIAN_POINT('Ctrl Pts',(0.598191370987134,0.0447560186040879,
-2.42753879259702));
#64342=CARTESIAN_POINT('Ctrl Pts',(0.582052893196987,0.145087721898763,
-2.42290224928177));
#64343=CARTESIAN_POINT('Ctrl Pts',(0.542875130555393,0.235428006188772,
-2.41826570596651));
#64344=CARTESIAN_POINT('Ctrl Pts',(0.503697367913799,0.325768290478781,
-2.41362916265126));
#64345=CARTESIAN_POINT('Ctrl Pts',(0.441480320420757,0.406117155764124,
-2.40899261933601));
#64346=CARTESIAN_POINT('Ctrl Pts',(0.363822855895058,0.466661207946321,
-2.40435607602075));
#64347=CARTESIAN_POINT('Ctrl Pts',(0.286165391369361,0.527205260128516,
-2.3997195327055));
#64348=CARTESIAN_POINT('Ctrl Pts',(0.193067509811008,0.567944499207565,
-2.39508298939025));
#64349=CARTESIAN_POINT('Ctrl Pts',(0.0958997041102385,0.583903245602492,
-2.39044644607499));
#64350=CARTESIAN_POINT('Ctrl Pts',(-0.00126810159053549,0.59986199199742,
-2.38580990275974));
#64351=CARTESIAN_POINT('Ctrl Pts',(-0.102505831433723,0.591040245708224,
-2.38117335944449));
#64352=CARTESIAN_POINT('Ctrl Pts',(-0.195448833634162,0.558515449119003,
-2.37653681612924));
#64353=CARTESIAN_POINT('Ctrl Pts',(-0.288391835834599,0.525990652529782,
-2.37190027281398));
#64354=CARTESIAN_POINT('Ctrl Pts',(-0.373040110392285,0.469762805640536,
-2.36726372949873));
#64355=CARTESIAN_POINT('Ctrl Pts',(-0.439055155636522,0.396699286339848,
-2.36262718618348));
#64356=CARTESIAN_POINT('Ctrl Pts',(-0.505070200880759,0.32363576703916,
-2.35799064286822));
#64357=CARTESIAN_POINT('Ctrl Pts',(-0.552452016811549,0.233736575327029,
-2.35335409955297));
#64358=CARTESIAN_POINT('Ctrl Pts',(-0.575413633928087,0.137981532689086,
-2.34871755623772));
#64359=CARTESIAN_POINT('Ctrl Pts',(-0.586234500533539,0.092856115871717,
-2.34653254389864));
#64360=CARTESIAN_POINT('Ctrl Pts',(-0.591632008304765,0.0464302026459444,
-2.34434753155957));
#64361=CARTESIAN_POINT('Ctrl Pts',(-0.591624801665701,2.64146101175725E-6,
-2.34216251922049));
#64362=CARTESIAN_POINT('Origin',(0.,0.,-1.97));
#64363=CARTESIAN_POINT('',(-0.591726041258602,7.22680221576831E-7,-2.14198748077951));
#64364=CARTESIAN_POINT('',(-0.591722112168784,5.38077801797166E-6,-2.16716251922049));
#64365=CARTESIAN_POINT('',(-0.591675,-7.2459289488551E-17,-1.97));
#64366=CARTESIAN_POINT('Ctrl Pts',(-0.591726006610465,7.22189647403126E-7,
-2.14198748077951));
#64367=CARTESIAN_POINT('Ctrl Pts',(-0.591726055065786,0.000677008384288284,
-2.14201932440197));
#64368=CARTESIAN_POINT('Ctrl Pts',(-0.591724919978352,0.00135329441552927,
-2.14205116802442));
#64369=CARTESIAN_POINT('Ctrl Pts',(-0.591722600367928,0.00202957638392072,
-2.14208301164688));
#64370=CARTESIAN_POINT('Ctrl Pts',(-0.591384856940035,0.100498607159696,
-2.14671955496213));
#64371=CARTESIAN_POINT('Ctrl Pts',(-0.565934772246907,0.198881503968735,
-2.15135609827739));
#64372=CARTESIAN_POINT('Ctrl Pts',(-0.518480687769739,0.28516228954106,
-2.15599264159264));
#64373=CARTESIAN_POINT('Ctrl Pts',(-0.471026603292572,0.371443075113383,
-2.16062918490789));
#64374=CARTESIAN_POINT('Ctrl Pts',(-0.401568519031367,0.44562174944899,
-2.16526572822314));
#64375=CARTESIAN_POINT('Ctrl Pts',(-0.318589685518163,0.498638513602709,
-2.1699022715384));
#64376=CARTESIAN_POINT('Ctrl Pts',(-0.235610852004958,0.551655277756428,
-2.17453881485365));
#64377=CARTESIAN_POINT('Ctrl Pts',(-0.139111269239756,0.583510131728257,
-2.17917535816891));
#64378=CARTESIAN_POINT('Ctrl Pts',(-0.0408768962731364,0.590312488702006,
-2.18381190148416));
#64379=CARTESIAN_POINT('Ctrl Pts',(0.0573574766934885,0.597114845675755,
-2.18844844479941));
#64380=CARTESIAN_POINT('Ctrl Pts',(0.157326639861528,0.578864705651421,
-2.19308498811466));
#64381=CARTESIAN_POINT('Ctrl Pts',(0.246820877606758,0.537791046173057,
-2.19772153142992));
#64382=CARTESIAN_POINT('Ctrl Pts',(0.336315115351985,0.496717386694694,
-2.20235807474517));
#64383=CARTESIAN_POINT('Ctrl Pts',(0.4153344276744,0.432820207762303,-2.20699461806042));
#64384=CARTESIAN_POINT('Ctrl Pts',(0.474227805185672,0.353903579743497,
-2.21163116137568));
#64385=CARTESIAN_POINT('Ctrl Pts',(0.533121182696942,0.274986951724692,
-2.21626770469093));
#64386=CARTESIAN_POINT('Ctrl Pts',(0.57188862539707,0.18105087461947,-2.22090424800618));
#64387=CARTESIAN_POINT('Ctrl Pts',(0.585795278698428,0.0835682141792701,
-2.22554079132143));
#64388=CARTESIAN_POINT('Ctrl Pts',(0.599701931999787,-0.0139144462609336,
-2.23017733463669));
#64389=CARTESIAN_POINT('Ctrl Pts',(0.588747795902376,-0.114943690036117,
-2.23481387795194));
#64390=CARTESIAN_POINT('Ctrl Pts',(0.554270751833028,-0.207180328769239,
-2.23945042126719));
#64391=CARTESIAN_POINT('Ctrl Pts',(0.519793707763683,-0.299416967502356,
-2.24408696458245));
#64392=CARTESIAN_POINT('Ctrl Pts',(0.461793755722403,-0.382861001193412,
-2.2487235078977));
#64393=CARTESIAN_POINT('Ctrl Pts',(0.387354709339321,-0.447321007911691,
-2.25336005121295));
#64394=CARTESIAN_POINT('Ctrl Pts',(0.31291566295624,-0.51178101462997,-2.25799659452821));
#64395=CARTESIAN_POINT('Ctrl Pts',(0.222037522231357,-0.557256994375471,
-2.26263313784346));
#64396=CARTESIAN_POINT('Ctrl Pts',(0.125819672410541,-0.57819474660445,
-2.26726968115871));
#64397=CARTESIAN_POINT('Ctrl Pts',(0.0296018225897245,-0.599132498833431,
-2.27190622447397));
#64398=CARTESIAN_POINT('Ctrl Pts',(-0.0719557363270286,-0.595532023545888,
-2.27654276778922));
#64399=CARTESIAN_POINT('Ctrl Pts',(-0.166449290288611,-0.567833064138483,
-2.28117931110447));
#64400=CARTESIAN_POINT('Ctrl Pts',(-0.260942844250194,-0.540134104731079,
-2.28581585441972));
#64401=CARTESIAN_POINT('Ctrl Pts',(-0.348372393256609,-0.488336661203813,
-2.29045239773498));
#64402=CARTESIAN_POINT('Ctrl Pts',(-0.418059745186469,-0.418767004933657,
-2.29508894105023));
#64403=CARTESIAN_POINT('Ctrl Pts',(-0.487747097116328,-0.349197348663502,
-2.29972548436548));
#64404=CARTESIAN_POINT('Ctrl Pts',(-0.539692251969632,-0.261855479650458,
-2.30436202768074));
#64405=CARTESIAN_POINT('Ctrl Pts',(-0.567550897673375,-0.167408881235814,
-2.30899857099599));
#64406=CARTESIAN_POINT('Ctrl Pts',(-0.583551338237656,-0.113164062571531,
-2.31166154092383));
#64407=CARTESIAN_POINT('Ctrl Pts',(-0.591606342618086,-0.0565756010940282,
-2.31432451085167));
#64408=CARTESIAN_POINT('Ctrl Pts',(-0.591628625190756,6.64897484074778E-6,
-2.31698748077951));
#64409=CARTESIAN_POINT('Ctrl Pts',(-0.591624801665701,2.64146101175725E-6,
-2.34216251922049));
#64410=CARTESIAN_POINT('Ctrl Pts',(-0.591616715991041,-0.052087958833455,
-2.33971098824431));
#64411=CARTESIAN_POINT('Ctrl Pts',(-0.584805015269325,-0.104180633627865,
-2.33725945726814));
#64412=CARTESIAN_POINT('Ctrl Pts',(-0.571216032446229,-0.154440919933626,
-2.33480792629196));
#64413=CARTESIAN_POINT('Ctrl Pts',(-0.545515395545548,-0.249497436354648,
-2.33017138297671));
#64414=CARTESIAN_POINT('Ctrl Pts',(-0.495572703441898,-0.337999575632937,
-2.32553483966145));
#64415=CARTESIAN_POINT('Ctrl Pts',(-0.4274876977833,-0.409138145028656,
-2.3208982963462));
#64416=CARTESIAN_POINT('Ctrl Pts',(-0.359402692124703,-0.480276714424375,
-2.31626175303095));
#64417=CARTESIAN_POINT('Ctrl Pts',(-0.273175372911158,-0.534051713937523,
-2.31162520971569));
#64418=CARTESIAN_POINT('Ctrl Pts',(-0.179337098146204,-0.563895343749223,
-2.30698866640044));
#64419=CARTESIAN_POINT('Ctrl Pts',(-0.0854988233812528,-0.593738973560922,
-2.30235212308519));
#64420=CARTESIAN_POINT('Ctrl Pts',(0.0159504069351066,-0.599651233671174,
-2.29771557976993));
#64421=CARTESIAN_POINT('Ctrl Pts',(0.11262010944575,-0.580910031263003,
-2.29307903645468));
#64422=CARTESIAN_POINT('Ctrl Pts',(0.209289811956395,-0.562168828854832,
-2.28844249313943));
#64423=CARTESIAN_POINT('Ctrl Pts',(0.301179986661323,-0.518774163928237,
-2.28380594982418));
#64424=CARTESIAN_POINT('Ctrl Pts',(0.377067643727942,-0.456026036018793,
-2.27916940650892));
#64425=CARTESIAN_POINT('Ctrl Pts',(0.452955300794561,-0.393277908109348,
-2.27453286319367));
#64426=CARTESIAN_POINT('Ctrl Pts',(0.51284044022287,-0.311176317217054,
-2.26989631987842));
#64427=CARTESIAN_POINT('Ctrl Pts',(0.54940900136291,-0.219748726264717,
-2.26525977656316));
#64428=CARTESIAN_POINT('Ctrl Pts',(0.58597756250295,-0.128321135312378,
-2.26062323324791));
#64429=CARTESIAN_POINT('Ctrl Pts',(0.59922954535472,-0.0275675442999919,
-2.25598668993266));
#64430=CARTESIAN_POINT('Ctrl Pts',(0.587546421394525,0.0702065251956151,
-2.2513501466174));
#64431=CARTESIAN_POINT('Ctrl Pts',(0.575863297434331,0.167980594691218,
-2.24671360330215));
#64432=CARTESIAN_POINT('Ctrl Pts',(0.539245066662175,0.262775142670045,
-2.2420770599869));
#64433=CARTESIAN_POINT('Ctrl Pts',(0.4821640900564,0.343012454196112,-2.23744051667165));
#64434=CARTESIAN_POINT('Ctrl Pts',(0.425083113450623,0.423249765722182,
-2.23280397335639));
#64435=CARTESIAN_POINT('Ctrl Pts',(0.347539391011226,0.48892984079549,-2.22816743004114));
#64436=CARTESIAN_POINT('Ctrl Pts',(0.259003711223628,0.532030855351401,
-2.22353088672589));
#64437=CARTESIAN_POINT('Ctrl Pts',(0.170468031436031,0.575131869907311,
-2.21889434341063));
#64438=CARTESIAN_POINT('Ctrl Pts',(0.0709403943002352,0.595653823945825,
-2.21425780009538));
#64439=CARTESIAN_POINT('Ctrl Pts',(-0.0274234102614568,0.591090272330029,
-2.20962125678013));
#64440=CARTESIAN_POINT('Ctrl Pts',(-0.125787214823146,0.586526720714233,
-2.20498471346488));
#64441=CARTESIAN_POINT('Ctrl Pts',(-0.22298718681073,0.556877663444129,
-2.20034817014962));
#64442=CARTESIAN_POINT('Ctrl Pts',(-0.307151825262896,0.505764282755542,
-2.19571162683437));
#64443=CARTESIAN_POINT('Ctrl Pts',(-0.391316463715064,0.454650902066953,
-2.19107508351912));
#64444=CARTESIAN_POINT('Ctrl Pts',(-0.462445768631812,0.382073197959879,
-2.18643854020386));
#64445=CARTESIAN_POINT('Ctrl Pts',(-0.511852375249243,0.296895435170809,
-2.18180199688861));
#64446=CARTESIAN_POINT('Ctrl Pts',(-0.561258981866674,0.211717672381738,
-2.17716545357336));
#64447=CARTESIAN_POINT('Ctrl Pts',(-0.588942890184788,0.11393985091067,
-2.17252891025811));
#64448=CARTESIAN_POINT('Ctrl Pts',(-0.591522931078829,0.0155040472608508,
-2.16789236694285));
#64449=CARTESIAN_POINT('Ctrl Pts',(-0.591658307575361,0.0103390538445895,
-2.16764908436873));
#64450=CARTESIAN_POINT('Ctrl Pts',(-0.591724568804173,0.0051722488901429,
-2.16740580179461));
#64451=CARTESIAN_POINT('Ctrl Pts',(-0.591722112168784,5.38077801797166E-6,
-2.16716251922049));
#64452=CARTESIAN_POINT('Origin',(0.,0.,-1.97));
#64453=CARTESIAN_POINT('',(-0.591630412993812,-7.77508703958541E-6,-1.96698748077951));
#64454=CARTESIAN_POINT('',(-0.591638304234624,-1.11070860510166E-5,-1.99216251922049));
#64455=CARTESIAN_POINT('',(-0.591675,-7.2459289488551E-17,-1.97));
#64456=CARTESIAN_POINT('Ctrl Pts',(-0.591630412993812,-7.77508703958541E-6,
-1.96698748077951));
#64457=CARTESIAN_POINT('Ctrl Pts',(-0.591603633133982,0.0579271878064958,
-1.96971413795226));
#64458=CARTESIAN_POINT('Ctrl Pts',(-0.583152878724501,0.115869795114227,
-1.97244079512502));
#64459=CARTESIAN_POINT('Ctrl Pts',(-0.566389150662593,0.171298234019464,
-1.97516745229777));
#64460=CARTESIAN_POINT('Ctrl Pts',(-0.537883274654121,0.265551505185685,
-1.97980399561303));
#64461=CARTESIAN_POINT('Ctrl Pts',(-0.485340193320855,0.352534985223169,
-1.98444053892828));
#64462=CARTESIAN_POINT('Ctrl Pts',(-0.415177246378055,0.421624962563196,
-1.98907708224353));
#64463=CARTESIAN_POINT('Ctrl Pts',(-0.345014299435256,0.490714939903223,
-1.99371362555878));
#64464=CARTESIAN_POINT('Ctrl Pts',(-0.257231486882922,0.541911414545796,
-1.99835016887404));
#64465=CARTESIAN_POINT('Ctrl Pts',(-0.162550146621597,0.568961514339747,
-2.00298671218929));
#64466=CARTESIAN_POINT('Ctrl Pts',(-0.0678688063602742,0.596011614133698,
-2.00762325550455));
#64467=CARTESIAN_POINT('Ctrl Pts',(0.033711061610042,0.598915339079029,
-2.0122597988198));
#64468=CARTESIAN_POINT('Ctrl Pts',(0.129783018526036,0.57731804325584,-2.01689634213505));
#64469=CARTESIAN_POINT('Ctrl Pts',(0.225854975442031,0.555720747432651,
-2.0215328854503));
#64470=CARTESIAN_POINT('Ctrl Pts',(0.316419021303705,0.509622430840941,
-2.02616942876556));
#64471=CARTESIAN_POINT('Ctrl Pts',(0.390414132784378,0.444653303022369,
-2.03080597208081));
#64472=CARTESIAN_POINT('Ctrl Pts',(0.464409244265055,0.379684175203794,
-2.03544251539606));
#64473=CARTESIAN_POINT('Ctrl Pts',(0.52183542136473,0.295844236158354,-2.04007905871132));
#64474=CARTESIAN_POINT('Ctrl Pts',(0.555678928351764,0.203373261645469,
-2.04471560202657));
#64475=CARTESIAN_POINT('Ctrl Pts',(0.589522435338797,0.110902287132586,
-2.04935214534182));
#64476=CARTESIAN_POINT('Ctrl Pts',(0.599783272213191,0.0098002771522647,
-2.05398868865707));
#64477=CARTESIAN_POINT('Ctrl Pts',(0.58520823352306,-0.0875846926311919,
-2.05862523197233));
#64478=CARTESIAN_POINT('Ctrl Pts',(0.570633194832929,-0.184969662414646,
-2.06326177528758));
#64479=CARTESIAN_POINT('Ctrl Pts',(0.531222280578273,-0.278637592001229,
-2.06789831860283));
#64480=CARTESIAN_POINT('Ctrl Pts',(0.471788935628397,-0.357148365788093,
-2.07253486191809));
#64481=CARTESIAN_POINT('Ctrl Pts',(0.412355590678518,-0.435659139574962,
-2.07717140523334));
#64482=CARTESIAN_POINT('Ctrl Pts',(0.332899815033417,-0.499012757562111,
-2.08180794854859));
#64483=CARTESIAN_POINT('Ctrl Pts',(0.243125925450237,-0.539471537099453,
-2.08644449186384));
#64484=CARTESIAN_POINT('Ctrl Pts',(0.15335203586706,-0.579930316636794,
-2.0910810351791));
#64485=CARTESIAN_POINT('Ctrl Pts',(0.0532600323458043,-0.59749425772433,
-2.09571757849435));
#64486=CARTESIAN_POINT('Ctrl Pts',(-0.0449253664050277,-0.59001819160078,
-2.10035412180961));
#64487=CARTESIAN_POINT('Ctrl Pts',(-0.14311076515586,-0.58254212547723,
-2.10499066512486));
#64488=CARTESIAN_POINT('Ctrl Pts',(-0.23938955913627,-0.550026052142593,
-2.10962720844011));
#64489=CARTESIAN_POINT('Ctrl Pts',(-0.322002755293884,-0.496441316320094,
-2.11426375175536));
#64490=CARTESIAN_POINT('Ctrl Pts',(-0.404615951451499,-0.442856580497594,
-2.11890029507062));
#64491=CARTESIAN_POINT('Ctrl Pts',(-0.473563549786321,-0.368203182187231,
-2.12353683838587));
#64492=CARTESIAN_POINT('Ctrl Pts',(-0.520424647872401,-0.281598900660794,
-2.12817338170112));
#64493=CARTESIAN_POINT('Ctrl Pts',(-0.56696390552393,-0.195589414406746,
-2.13277808139392));
#64494=CARTESIAN_POINT('Ctrl Pts',(-0.591718999800854,-0.0977926377482492,
-2.13738278108671));
#64495=CARTESIAN_POINT('Ctrl Pts',(-0.591726006610465,7.22189647403126E-7,
-2.14198748077951));
#64496=CARTESIAN_POINT('Ctrl Pts',(-0.591722112168784,5.38077801797166E-6,
-2.16716251922049));
#64497=CARTESIAN_POINT('Ctrl Pts',(-0.5916777496005,-0.0932992832067527,
-2.16276925847936));
#64498=CARTESIAN_POINT('Ctrl Pts',(-0.569224431891521,-0.186624542965204,
-2.15837599773822));
#64499=CARTESIAN_POINT('Ctrl Pts',(-0.526702394959567,-0.269674508653324,
-2.15398273699709));
#64500=CARTESIAN_POINT('Ctrl Pts',(-0.481825644476292,-0.357323475089116,
-2.14934619368184));
#64501=CARTESIAN_POINT('Ctrl Pts',(-0.414595970039771,-0.433527622132128,
-2.14470965036659));
#64502=CARTESIAN_POINT('Ctrl Pts',(-0.333224455752003,-0.488979770095182,
-2.14007310705133));
#64503=CARTESIAN_POINT('Ctrl Pts',(-0.251852941464236,-0.544431918058235,
-2.13543656373608));
#64504=CARTESIAN_POINT('Ctrl Pts',(-0.156339587325221,-0.579132066941329,
-2.13080002042083));
#64505=CARTESIAN_POINT('Ctrl Pts',(-0.0583498995310369,-0.588842120349991,
-2.12616347710557));
#64506=CARTESIAN_POINT('Ctrl Pts',(0.0396397882631472,-0.598552173758654,
-2.12152693379032));
#64507=CARTESIAN_POINT('Ctrl Pts',(0.140105809712501,-0.583272131692884,
-2.11689039047507));
#64508=CARTESIAN_POINT('Ctrl Pts',(0.230777765496664,-0.544868219320894,
-2.11225384715982));
#64509=CARTESIAN_POINT('Ctrl Pts',(0.321449721280828,-0.506464306948905,
-2.10761730384456));
#64510=CARTESIAN_POINT('Ctrl Pts',(0.402327611399801,-0.444936524270695,
-2.10298076052931));
#64511=CARTESIAN_POINT('Ctrl Pts',(0.463533429402933,-0.367799555871825,
-2.09834421721406));
#64512=CARTESIAN_POINT('Ctrl Pts',(0.524739247406063,-0.290662587472958,
-2.0937076738988));
#64513=CARTESIAN_POINT('Ctrl Pts',(0.566272993293352,-0.19791643335343,
-2.08907113058355));
#64514=CARTESIAN_POINT('Ctrl Pts',(0.583061950538804,-0.100888628236492,
-2.0844345872683));
#64515=CARTESIAN_POINT('Ctrl Pts',(0.599850907784255,-0.00386082311955339,
-2.07979804395305));
#64516=CARTESIAN_POINT('Ctrl Pts',(0.591895076387869,0.0974486329947963,
-2.07516150063779));
#64517=CARTESIAN_POINT('Ctrl Pts',(0.560166140375257,0.19066632804626,-2.07052495732254));
#64518=CARTESIAN_POINT('Ctrl Pts',(0.528437204362642,0.28388402309773,-2.06588841400729));
#64519=CARTESIAN_POINT('Ctrl Pts',(0.472935163733799,0.369009957086312,
-2.06125187069203));
#64520=CARTESIAN_POINT('Ctrl Pts',(0.400438750161246,0.435647289493295,
-2.05661532737678));
#64521=CARTESIAN_POINT('Ctrl Pts',(0.327942336588698,0.502284621900274,
-2.05197878406153));
#64522=CARTESIAN_POINT('Ctrl Pts',(0.238451550072442,0.550433352725655,
-2.04734224074627));
#64523=CARTESIAN_POINT('Ctrl Pts',(0.142896331603534,0.574212845456986,
-2.04270569743102));
#64524=CARTESIAN_POINT('Ctrl Pts',(0.0473411131346229,0.597992338188318,
-2.03806915411577));
#64525=CARTESIAN_POINT('Ctrl Pts',(-0.0542785372869409,0.597402592825597,
-2.03343261080051));
#64526=CARTESIAN_POINT('Ctrl Pts',(-0.149551322075371,0.57251563781181,
-2.02879606748526));
#64527=CARTESIAN_POINT('Ctrl Pts',(-0.244824106863801,0.547628682798024,
-2.02415952417001));
#64528=CARTESIAN_POINT('Ctrl Pts',(-0.333750026019097,0.498444518133171,
-2.01952298085476));
#64529=CARTESIAN_POINT('Ctrl Pts',(-0.405468128522953,0.430970242854016,
-2.0148864375395));
#64530=CARTESIAN_POINT('Ctrl Pts',(-0.477186231026809,0.363495967574862,
-2.01024989422425));
#64531=CARTESIAN_POINT('Ctrl Pts',(-0.531696516879226,0.277731581681406,
-2.005613350909));
#64532=CARTESIAN_POINT('Ctrl Pts',(-0.562341382197547,0.184151902900045,
-2.00097680759374));
#64533=CARTESIAN_POINT('Ctrl Pts',(-0.581760495511739,0.124852102842694,
-1.99803871146933));
#64534=CARTESIAN_POINT('Ctrl Pts',(-0.591596366956281,0.0624140449901387,
-1.99510061534491));
#64535=CARTESIAN_POINT('Ctrl Pts',(-0.591638304234624,-1.11070860510166E-5,
-1.99216251922049));
#64536=CARTESIAN_POINT('Origin',(0.,0.,-1.97));
#64537=CARTESIAN_POINT('',(-0.591694101178176,1.39310560667294E-5,-1.79198748077951));
#64538=CARTESIAN_POINT('',(-0.591679947997511,1.52687619238092E-5,-1.81716251922049));
#64539=CARTESIAN_POINT('',(-0.591675,-7.2459289488551E-17,-1.97));
#64540=CARTESIAN_POINT('Ctrl Pts',(-0.591694101178176,1.39310560667294E-5,
-1.79198748077951));
#64541=CARTESIAN_POINT('Ctrl Pts',(-0.59171078017241,0.0166866101387685,
-1.79277240818731));
#64542=CARTESIAN_POINT('Ctrl Pts',(-0.591020216129536,0.033357911865641,
-1.79355733559511));
#64543=CARTESIAN_POINT('Ctrl Pts',(-0.589612508562732,0.049968437166311,
-1.79434226300291));
#64544=CARTESIAN_POINT('Ctrl Pts',(-0.581297221003853,0.148086325878601,
-1.79897880631816));
#64545=CARTESIAN_POINT('Ctrl Pts',(-0.547959143171164,0.244083585015765,
-1.80361534963341));
#64546=CARTESIAN_POINT('Ctrl Pts',(-0.493670015158273,0.326235606732483,
-1.80825189294867));
#64547=CARTESIAN_POINT('Ctrl Pts',(-0.439380887145383,0.408387628449198,
-1.81288843626392));
#64548=CARTESIAN_POINT('Ctrl Pts',(-0.364140708952291,0.476694412745469,
-1.81752497957917));
#64549=CARTESIAN_POINT('Ctrl Pts',(-0.27713892610541,0.5228133229018,-1.82216152289442));
#64550=CARTESIAN_POINT('Ctrl Pts',(-0.190137143258528,0.56893223305813,
-1.82679806620968));
#64551=CARTESIAN_POINT('Ctrl Pts',(-0.0913737557578566,0.592863269074521,
-1.83143460952493));
#64552=CARTESIAN_POINT('Ctrl Pts',(0.00708878796496597,0.591683618204585,
-1.83607115284018));
#64553=CARTESIAN_POINT('Ctrl Pts',(0.105551331687789,0.590503967334648,
-1.84070769615544));
#64554=CARTESIAN_POINT('Ctrl Pts',(0.203713031632762,0.564213629578384,
-1.84534423947069));
#64555=CARTESIAN_POINT('Ctrl Pts',(0.289584926368809,0.516023570572558,
-1.84998078278594));
#64556=CARTESIAN_POINT('Ctrl Pts',(0.375456821104856,0.467833511566733,
-1.8546173261012));
#64557=CARTESIAN_POINT('Ctrl Pts',(0.449038910631976,0.397743731311347,
-1.85925386941645));
#64558=CARTESIAN_POINT('Ctrl Pts',(0.501344259782448,0.314314632414194,
-1.8638904127317));
#64559=CARTESIAN_POINT('Ctrl Pts',(0.553649608932919,0.230885533517044,
-1.86852695604696));
#64560=CARTESIAN_POINT('Ctrl Pts',(0.584678217706743,0.134117115978128,
-1.87316349936221));
#64561=CARTESIAN_POINT('Ctrl Pts',(0.590640412595231,0.0358281729343923,
-1.87780004267746));
#64562=CARTESIAN_POINT('Ctrl Pts',(0.596602607483719,-0.0624607701093437,
-1.88243658599271));
#64563=CARTESIAN_POINT('Ctrl Pts',(0.57749838848687,-0.1622702386579,-1.88707312930797));
#64564=CARTESIAN_POINT('Ctrl Pts',(0.535661045929247,-0.251410021360458,
-1.89170967262322));
#64565=CARTESIAN_POINT('Ctrl Pts',(0.493823703371622,-0.340549804063018,
-1.89634621593847));
#64566=CARTESIAN_POINT('Ctrl Pts',(0.429253237253222,-0.419019900919579,
-1.90098275925373));
#64567=CARTESIAN_POINT('Ctrl Pts',(0.34983594975009,-0.477236380873183,
-1.90561930256898));
#64568=CARTESIAN_POINT('Ctrl Pts',(0.270418662246957,-0.535452860826788,
-1.91025584588423));
#64569=CARTESIAN_POINT('Ctrl Pts',(0.176154553359092,-0.573415723877436,
-1.91489238919948));
#64570=CARTESIAN_POINT('Ctrl Pts',(0.0785565529402472,-0.586488382627164,
-1.91952893251474));
#64571=CARTESIAN_POINT('Ctrl Pts',(-0.0190414474785949,-0.599561041376893,
-1.92416547582999));
#64572=CARTESIAN_POINT('Ctrl Pts',(-0.119973339428416,-0.587743495825703,
-1.92880201914524));
#64573=CARTESIAN_POINT('Ctrl Pts',(-0.211911824579722,-0.552479079757573,
-1.9334385624605));
#64574=CARTESIAN_POINT('Ctrl Pts',(-0.303850309731033,-0.51721466368944,
-1.93807510577575));
#64575=CARTESIAN_POINT('Ctrl Pts',(-0.386795388083827,-0.458503377104364,
-1.942711649091));
#64576=CARTESIAN_POINT('Ctrl Pts',(-0.450616577527191,-0.383515912348056,
-1.94734819240626));
#64577=CARTESIAN_POINT('Ctrl Pts',(-0.514437766970553,-0.30852844759175,
-1.95198473572151));
#64578=CARTESIAN_POINT('Ctrl Pts',(-0.559135067504486,-0.217264804664214,
-1.95662127903676));
#64579=CARTESIAN_POINT('Ctrl Pts',(-0.579249382429614,-0.120871452052966,
-1.96125782235201));
#64580=CARTESIAN_POINT('Ctrl Pts',(-0.587534876326536,-0.0811650768799965,
-1.96316770849451));
#64581=CARTESIAN_POINT('Ctrl Pts',(-0.591649170938044,-0.0405883012720437,
-1.96507759463701));
#64582=CARTESIAN_POINT('Ctrl Pts',(-0.591630412993812,-7.77508703958541E-6,
-1.96698748077951));
#64583=CARTESIAN_POINT('Ctrl Pts',(-0.591638304234624,-1.11070860510166E-5,
-1.99216251922049));
#64584=CARTESIAN_POINT('Ctrl Pts',(-0.591662547230624,-0.0360976814156448,
-1.99046407202966));
#64585=CARTESIAN_POINT('Ctrl Pts',(-0.588413916302922,-0.0721799429759043,
-1.98876562483882));
#64586=CARTESIAN_POINT('Ctrl Pts',(-0.581851710290273,-0.107649155620656,
-1.98706717764798));
#64587=CARTESIAN_POINT('Ctrl Pts',(-0.56393772828045,-0.204475563690727,
-1.98243063433273));
#64588=CARTESIAN_POINT('Ctrl Pts',(-0.521330319476581,-0.296733408161606,
-1.97779409101748));
#64589=CARTESIAN_POINT('Ctrl Pts',(-0.459233332030376,-0.373154793920477,
-1.97315754770223));
#64590=CARTESIAN_POINT('Ctrl Pts',(-0.39713634458417,-0.449576179679351,
-1.96852100438697));
#64591=CARTESIAN_POINT('Ctrl Pts',(-0.315549778495629,-0.510161106726214,
-1.96388446107172));
#64592=CARTESIAN_POINT('Ctrl Pts',(-0.224438194226501,-0.547510045977152,
-1.95924791775647));
#64593=CARTESIAN_POINT('Ctrl Pts',(-0.133326609957372,-0.58485898522809,
-1.95461137444121));
#64594=CARTESIAN_POINT('Ctrl Pts',(-0.032690007507657,-0.598971936683102,
-1.94997483112596));
#64595=CARTESIAN_POINT('Ctrl Pts',(0.0651803799227252,-0.588125217574187,
-1.94533828781071));
#64596=CARTESIAN_POINT('Ctrl Pts',(0.163050767353107,-0.577278498465272,
-1.94070174449545));
#64597=CARTESIAN_POINT('Ctrl Pts',(0.258154939764155,-0.541472108792431,
-1.9360652011802));
#64598=CARTESIAN_POINT('Ctrl Pts',(0.338877366295973,-0.485079255468486,
-1.93142865786495));
#64599=CARTESIAN_POINT('Ctrl Pts',(0.419599792827792,-0.42868640214454,
-1.9267921145497));
#64600=CARTESIAN_POINT('Ctrl Pts',(0.485940473480379,-0.351707085169493,
-1.92215557123444));
#64601=CARTESIAN_POINT('Ctrl Pts',(0.52979690124641,-0.263543159469671,
-1.91751902791919));
#64602=CARTESIAN_POINT('Ctrl Pts',(0.573653329012439,-0.175379233769854,
-1.91288248460394));
#64603=CARTESIAN_POINT('Ctrl Pts',(0.595025503891914,-0.0760306993452581,
-1.90824594128868));
#64604=CARTESIAN_POINT('Ctrl Pts',(0.591303139179611,0.0223685285589705,
-1.90360939797343));
#64605=CARTESIAN_POINT('Ctrl Pts',(0.587580774467307,0.120767756463208,
-1.89897285465818));
#64606=CARTESIAN_POINT('Ctrl Pts',(0.558763870163224,0.218217677847083,
-1.89433631134293));
#64607=CARTESIAN_POINT('Ctrl Pts',(0.508371973651507,0.30281626422507,-1.88969976802767));
#64608=CARTESIAN_POINT('Ctrl Pts',(0.457980077139792,0.387414850603052,
-1.88506322471242));
#64609=CARTESIAN_POINT('Ctrl Pts',(0.386013188420449,0.459162101975147,
-1.88042668139717));
#64610=CARTESIAN_POINT('Ctrl Pts',(0.30126097040329,0.509295180799135,-1.87579013808191));
#64611=CARTESIAN_POINT('Ctrl Pts',(0.216508752386129,0.559428259623125,
-1.87115359476666));
#64612=CARTESIAN_POINT('Ctrl Pts',(0.118971205071153,0.587947165899007,
-1.86651705145141));
#64613=CARTESIAN_POINT('Ctrl Pts',(0.0205610591211027,0.591368748177796,
-1.86188050813615));
#64614=CARTESIAN_POINT('Ctrl Pts',(-0.0778490868289508,0.594790330456586,
-1.8572439648209));
#64615=CARTESIAN_POINT('Ctrl Pts',(-0.177131831414078,0.573114588738283,
-1.85260742150565));
#64616=CARTESIAN_POINT('Ctrl Pts',(-0.265161294619265,0.528988885808947,
-1.84797087819039));
#64617=CARTESIAN_POINT('Ctrl Pts',(-0.353190757824444,0.484863182879615,
-1.84333433487514));
#64618=CARTESIAN_POINT('Ctrl Pts',(-0.429966939649683,0.418287518739253,
-1.83869779155989));
#64619=CARTESIAN_POINT('Ctrl Pts',(-0.486112795043358,0.337393100060878,
-1.83406124824464));
#64620=CARTESIAN_POINT('Ctrl Pts',(-0.542258650437036,0.256498681382499,
-1.82942470492938));
#64621=CARTESIAN_POINT('Ctrl Pts',(-0.577774179399147,0.161285508166105,
-1.82478816161413));
#64622=CARTESIAN_POINT('Ctrl Pts',(-0.588321699237055,0.0633824240651956,
-1.82015161829888));
#64623=CARTESIAN_POINT('Ctrl Pts',(-0.59058830028609,0.0423436171667834,
-1.81915525193941));
#64624=CARTESIAN_POINT('Ctrl Pts',(-0.591701890513321,0.0211805914592501,
-1.81815888557995));
#64625=CARTESIAN_POINT('Ctrl Pts',(-0.591679947997511,1.52687619238092E-5,
-1.81716251922049));
#64626=CARTESIAN_POINT('Origin',(0.,0.,-1.97));
#64627=CARTESIAN_POINT('',(-0.591669172308873,-1.54438390886913E-5,-1.61698748077951));
#64628=CARTESIAN_POINT('',(-0.591683400125346,-1.50610791253661E-5,-1.64216251922049));
#64629=CARTESIAN_POINT('',(-0.591675,-7.2459289488551E-17,-1.97));
#64630=CARTESIAN_POINT('Ctrl Pts',(-0.591669172308873,-1.54438390886913E-5,
-1.61698748077951));
#64631=CARTESIAN_POINT('Ctrl Pts',(-0.591594341966499,0.0739068633259733,
-1.62046722173761));
#64632=CARTESIAN_POINT('Ctrl Pts',(-0.577702068741859,0.147856503492052,
-1.6239469626957));
#64633=CARTESIAN_POINT('Ctrl Pts',(-0.550647018423414,0.216627828470594,
-1.6274267036538));
#64634=CARTESIAN_POINT('Ctrl Pts',(-0.51459780837922,0.308261438831276,
-1.63206324696905));
#64635=CARTESIAN_POINT('Ctrl Pts',(-0.455179479368241,0.390701498104475,
-1.6366997902843));
#64636=CARTESIAN_POINT('Ctrl Pts',(-0.379649078234728,0.453879204593031,
-1.64133633359956));
#64637=CARTESIAN_POINT('Ctrl Pts',(-0.304118677101214,0.517056911081587,
-1.64597287691481));
#64638=CARTESIAN_POINT('Ctrl Pts',(-0.212476203845164,0.5609722647855,-1.65060942023006));
#64639=CARTESIAN_POINT('Ctrl Pts',(-0.115914395327608,0.580261671939752,
-1.65524596354532));
#64640=CARTESIAN_POINT('Ctrl Pts',(-0.0193525868100518,0.599551079094004,
-1.65988250686057));
#64641=CARTESIAN_POINT('Ctrl Pts',(0.0821285569690107,0.594214539698594,
-1.66451905017582));
#64642=CARTESIAN_POINT('Ctrl Pts',(0.176134654907471,0.564903831025341,
-1.66915559349108));
#64643=CARTESIAN_POINT('Ctrl Pts',(0.270140752845928,0.535593122352088,
-1.67379213680633));
#64644=CARTESIAN_POINT('Ctrl Pts',(0.356671804943783,0.482308244400993,
-1.67842868012158));
#64645=CARTESIAN_POINT('Ctrl Pts',(0.425159356836724,0.411557136082785,
-1.68306522343683));
#64646=CARTESIAN_POINT('Ctrl Pts',(0.493646908729669,0.340806027764573,
-1.68770176675209));
#64647=CARTESIAN_POINT('Ctrl Pts',(0.544090960417698,0.252588689079246,
-1.69233831006734));
#64648=CARTESIAN_POINT('Ctrl Pts',(0.570330536790822,0.157679528697842,
-1.69697485338259));
#64649=CARTESIAN_POINT('Ctrl Pts',(0.596570113163946,0.062770368316437,
-1.70161139669785));
#64650=CARTESIAN_POINT('Ctrl Pts',(0.598605214222167,-0.0388306137610455,
-1.7062479400131));
#64651=CARTESIAN_POINT('Ctrl Pts',(0.576187283266596,-0.13471440000364,
-1.71088448332835));
#64652=CARTESIAN_POINT('Ctrl Pts',(0.553769352311027,-0.230598186246228,
-1.71552102664361));
#64653=CARTESIAN_POINT('Ctrl Pts',(0.50689838934167,-0.32076477665393,-1.72015756995886));
#64654=CARTESIAN_POINT('Ctrl Pts',(0.441298970925477,-0.394201691049895,
-1.72479411327411));
#64655=CARTESIAN_POINT('Ctrl Pts',(0.375699552509279,-0.467638605445864,
-1.72943065658937));
#64656=CARTESIAN_POINT('Ctrl Pts',(0.291371678646244,-0.524345843830095,
-1.73406719990462));
#64657=CARTESIAN_POINT('Ctrl Pts',(0.198614718926297,-0.557397477920656,
-1.73870374321987));
#64658=CARTESIAN_POINT('Ctrl Pts',(0.105857759206355,-0.590449112011215,
-1.74334028653512));
#64659=CARTESIAN_POINT('Ctrl Pts',(0.00467171362950315,-0.599845141808107,
-1.74797682985038));
#64660=CARTESIAN_POINT('Ctrl Pts',(-0.092585078467592,-0.584437984915107,
-1.75261337316563));
#64661=CARTESIAN_POINT('Ctrl Pts',(-0.189841870564687,-0.569030828022107,
-1.75724991648088));
#64662=CARTESIAN_POINT('Ctrl Pts',(-0.283169409182025,-0.528820484439216,
-1.76188645979614));
#64663=CARTESIAN_POINT('Ctrl Pts',(-0.361169152306093,-0.468718037191848,
-1.76652300311139));
#64664=CARTESIAN_POINT('Ctrl Pts',(-0.439168895430163,-0.408615589944479,
-1.77115954642664));
#64665=CARTESIAN_POINT('Ctrl Pts',(-0.501840843060962,-0.328621039032634,
-1.7757960897419));
#64666=CARTESIAN_POINT('Ctrl Pts',(-0.541530568233824,-0.238504504433004,
-1.78043263305715));
#64667=CARTESIAN_POINT('Ctrl Pts',(-0.574501159996734,-0.163643933833635,
-1.7842842489646));
#64668=CARTESIAN_POINT('Ctrl Pts',(-0.591612257839709,-0.0817984191520354,
-1.78813586487205));
#64669=CARTESIAN_POINT('Ctrl Pts',(-0.591694101178176,1.39310560667294E-5,
-1.79198748077951));
#64670=CARTESIAN_POINT('Ctrl Pts',(-0.591679947997511,1.52687619238092E-5,
-1.81716251922049));
#64671=CARTESIAN_POINT('Ctrl Pts',(-0.591599782062918,-0.0773112278756028,
-1.8135223422647));
#64672=CARTESIAN_POINT('Ctrl Pts',(-0.576362850266228,-0.154668384075078,
-1.80988216530891));
#64673=CARTESIAN_POINT('Ctrl Pts',(-0.546821475223447,-0.22611065368091,
-1.80624198835312));
#64674=CARTESIAN_POINT('Ctrl Pts',(-0.509194220658233,-0.317107652340668,
-1.80160544503786));
#64675=CARTESIAN_POINT('Ctrl Pts',(-0.4483602008141,-0.398508654674769,
-1.79696890172261));
#64676=CARTESIAN_POINT('Ctrl Pts',(-0.371749367678615,-0.46037176401698,
-1.79233235840736));
#64677=CARTESIAN_POINT('Ctrl Pts',(-0.295138534543124,-0.522234873359194,
-1.78769581509211));
#64678=CARTESIAN_POINT('Ctrl Pts',(-0.202750888116276,-0.564560089709517,
-1.78305927177685));
#64679=CARTESIAN_POINT('Ctrl Pts',(-0.105870176849256,-0.5821780304404,
-1.7784227284616));
#64680=CARTESIAN_POINT('Ctrl Pts',(-0.00898946558223347,-0.599795971171284,
-1.77378618514635));
#64681=CARTESIAN_POINT('Ctrl Pts',(0.0923843105249564,-0.592706636282727,
-1.76914964183109));
#64682=CARTESIAN_POINT('Ctrl Pts',(0.185869883701361,-0.561775880406411,
-1.76451309851584));
#64683=CARTESIAN_POINT('Ctrl Pts',(0.279355456877761,-0.530845124530096,
-1.75987655520059));
#64684=CARTESIAN_POINT('Ctrl Pts',(0.36495282712337,-0.476072947666023,
-1.75524001188534));
#64685=CARTESIAN_POINT('Ctrl Pts',(0.43220757513767,-0.404148939708088,
-1.75060346857008));
#64686=CARTESIAN_POINT('Ctrl Pts',(0.499462323151974,-0.332224931750148,
-1.74596692525483));
#64687=CARTESIAN_POINT('Ctrl Pts',(0.548374448934968,-0.243149092698343,
-1.74133038193958));
#64688=CARTESIAN_POINT('Ctrl Pts',(0.572970078869414,-0.147800684010369,
-1.73669383862432));
#64689=CARTESIAN_POINT('Ctrl Pts',(0.59756570880386,-0.0524522753223972,
-1.73205729530907));
#64690=CARTESIAN_POINT('Ctrl Pts',(0.59784484288976,0.0491687030017455,
-1.72742075199382));
#64691=CARTESIAN_POINT('Ctrl Pts',(0.573773389136127,0.14465079119313,-1.72278420867856));
#64692=CARTESIAN_POINT('Ctrl Pts',(0.549701935382493,0.240132879384514,
-1.71814766536331));
#64693=CARTESIAN_POINT('Ctrl Pts',(0.501279893789324,0.329476077443143,
-1.71351112204806));
#64694=CARTESIAN_POINT('Ctrl Pts',(0.434421281630162,0.40176847006748,-1.7088745787328));
#64695=CARTESIAN_POINT('Ctrl Pts',(0.367562669471001,0.474060862691815,
-1.70423803541755));
#64696=CARTESIAN_POINT('Ctrl Pts',(0.282267486745845,0.529302449881861,
-1.6996014921023));
#64697=CARTESIAN_POINT('Ctrl Pts',(0.188953245137173,0.560746310398639,
-1.69496494878705));
#64698=CARTESIAN_POINT('Ctrl Pts',(0.0956390035284988,0.592190170915418,
-1.69032840547179));
#64699=CARTESIAN_POINT('Ctrl Pts',(-0.00569429696368506,0.599836304758928,
-1.68569186215654));
#64700=CARTESIAN_POINT('Ctrl Pts',(-0.10267033205033,0.582750852758047,
-1.68105531884129));
#64701=CARTESIAN_POINT('Ctrl Pts',(-0.199646367136978,0.565665400757165,
-1.67641877552603));
#64702=CARTESIAN_POINT('Ctrl Pts',(-0.292265136818081,0.523848362911888,
-1.67178223221078));
#64703=CARTESIAN_POINT('Ctrl Pts',(-0.369214664445686,0.462407055560158,
-1.66714568889553));
#64704=CARTESIAN_POINT('Ctrl Pts',(-0.446164192073286,0.400965748208432,
-1.66250914558028));
#64705=CARTESIAN_POINT('Ctrl Pts',(-0.507444477647392,0.319900171350254,
-1.65787260226502));
#64706=CARTESIAN_POINT('Ctrl Pts',(-0.545571064596393,0.22911125452215,
-1.65323605894977));
#64707=CARTESIAN_POINT('Ctrl Pts',(-0.575923868874289,0.156833653939345,
-1.64954487904001));
#64708=CARTESIAN_POINT('Ctrl Pts',(-0.59160221209113,0.0783935487786571,
-1.64585369913025));
#64709=CARTESIAN_POINT('Ctrl Pts',(-0.591683400125346,-1.50610791253661E-5,
-1.64216251922049));
#64710=CARTESIAN_POINT('Origin',(0.,0.,-1.97));
#64711=CARTESIAN_POINT('',(-0.591646097050001,1.31033435099431E-5,-1.44198748077951));
#64712=CARTESIAN_POINT('',(-0.591636138149344,1.03689755184515E-5,-1.46716251922049));
#64713=CARTESIAN_POINT('',(-0.591675,-7.2459289488551E-17,-1.97));
#64714=CARTESIAN_POINT('Ctrl Pts',(-0.591646097050001,1.31033435099431E-5,
-1.44198748077951));
#64715=CARTESIAN_POINT('Ctrl Pts',(-0.59167246821368,0.0326896924703124,
-1.44352549197265));
#64716=CARTESIAN_POINT('Ctrl Pts',(-0.589011448984827,0.0653620312304001,
-1.44506350316579));
#64717=CARTESIAN_POINT('Ctrl Pts',(-0.583625010676761,0.0975786958256344,
-1.44660151435893));
#64718=CARTESIAN_POINT('Ctrl Pts',(-0.567386861928784,0.194700200230078,
-1.45123805767419));
#64719=CARTESIAN_POINT('Ctrl Pts',(-0.526380028614879,0.287680525121921,
-1.45587460098944));
#64720=CARTESIAN_POINT('Ctrl Pts',(-0.465612872889403,0.365163535373068,
-1.46051114430469));
#64721=CARTESIAN_POINT('Ctrl Pts',(-0.404845717163926,0.442646545624216,
-1.46514768761995));
#64722=CARTESIAN_POINT('Ctrl Pts',(-0.324318239026884,0.50463224123467,
-1.4697842309352));
#64723=CARTESIAN_POINT('Ctrl Pts',(-0.233865647425011,0.543550010505898,
-1.47442077425045));
#64724=CARTESIAN_POINT('Ctrl Pts',(-0.143413055823141,0.582467779777125,
-1.4790573175657));
#64725=CARTESIAN_POINT('Ctrl Pts',(-0.0430353507564487,0.598317622709121,
-1.48369386088096));
#64726=CARTESIAN_POINT('Ctrl Pts',(0.0550078549600969,0.589163721608154,
-1.48833040419621));
#64727=CARTESIAN_POINT('Ctrl Pts',(0.153051060676642,0.580009820507187,
-1.49296694751146));
#64728=CARTESIAN_POINT('Ctrl Pts',(0.24875976704304,0.545852175373257,-1.49760349082671));
#64729=CARTESIAN_POINT('Ctrl Pts',(0.33044460855433,0.49086262400376,-1.50224003414197));
#64730=CARTESIAN_POINT('Ctrl Pts',(0.412129450065623,0.435873072634261,
-1.50687657745722));
#64731=CARTESIAN_POINT('Ctrl Pts',(0.479790426721806,0.360051615029195,
-1.51151312077248));
#64732=CARTESIAN_POINT('Ctrl Pts',(0.525163777402457,0.272658691170599,
-1.51614966408773));
#64733=CARTESIAN_POINT('Ctrl Pts',(0.570537128083106,0.185265767312005,
-1.52078620740298));
#64734=CARTESIAN_POINT('Ctrl Pts',(0.593622852788224,0.0863013771998743,
-1.52542275071823));
#64735=CARTESIAN_POINT('Ctrl Pts',(0.59160138071521,-0.0121474813166226,
-1.53005929403348));
#64736=CARTESIAN_POINT('Ctrl Pts',(0.589579908642197,-0.110596339833122,
-1.53469583734874));
#64737=CARTESIAN_POINT('Ctrl Pts',(0.562451239791054,-0.208529666753994,
-1.53933238066399));
#64738=CARTESIAN_POINT('Ctrl Pts',(0.513528729214872,-0.293986392946068,
-1.54396892397925));
#64739=CARTESIAN_POINT('Ctrl Pts',(0.46460621863869,-0.379443119138142,
-1.5486054672945));
#64740=CARTESIAN_POINT('Ctrl Pts',(0.393889866337471,-0.452423244601417,
-1.55324201060975));
#64741=CARTESIAN_POINT('Ctrl Pts',(0.310016601182262,-0.504013354940005,
-1.557878553925));
#64742=CARTESIAN_POINT('Ctrl Pts',(0.226143336027052,-0.555603465278593,
-1.56251509724026));
#64743=CARTESIAN_POINT('Ctrl Pts',(0.129113158017854,-0.585803560492493,
-1.56715164055551));
#64744=CARTESIAN_POINT('Ctrl Pts',(0.0307768303592042,-0.59092515742649,
-1.57178818387076));
#64745=CARTESIAN_POINT('Ctrl Pts',(-0.0675594972994458,-0.596046754360487,
-1.57642472718602));
#64746=CARTESIAN_POINT('Ctrl Pts',(-0.167201974607546,-0.576089853014582,
-1.58106127050127));
#64747=CARTESIAN_POINT('Ctrl Pts',(-0.255980785659163,-0.533491885917489,
-1.58569781381652));
#64748=CARTESIAN_POINT('Ctrl Pts',(-0.34475959671078,-0.490893918820396,
-1.59033435713178));
#64749=CARTESIAN_POINT('Ctrl Pts',(-0.422674741505912,-0.425654885972116,
-1.59497090044703));
#64750=CARTESIAN_POINT('Ctrl Pts',(-0.480210067957043,-0.345742744825069,
-1.59960744376228));
#64751=CARTESIAN_POINT('Ctrl Pts',(-0.537745394408174,-0.265830603678023,
-1.60424398707753));
#64752=CARTESIAN_POINT('Ctrl Pts',(-0.574900902515302,-0.171245354232211,
-1.60888053039279));
#64753=CARTESIAN_POINT('Ctrl Pts',(-0.58713861103016,-0.0735391487852222,
-1.61351707370804));
#64754=CARTESIAN_POINT('Ctrl Pts',(-0.590191879185685,-0.0491617708368692,
-1.6146738760652));
#64755=CARTESIAN_POINT('Ctrl Pts',(-0.59169404884925,-0.0245901177026608,
-1.61583067842235));
#64756=CARTESIAN_POINT('Ctrl Pts',(-0.591669172308873,-1.54438390886913E-5,
-1.61698748077951));
#64757=CARTESIAN_POINT('Ctrl Pts',(-0.591683400125346,-1.50610791253661E-5,
-1.64216251922049));
#64758=CARTESIAN_POINT('Ctrl Pts',(-0.591704193529728,-0.0200966155542075,
-1.641217155815));
#64759=CARTESIAN_POINT('Ctrl Pts',(-0.590701899995329,-0.0401761041119696,
-1.6402717924095));
#64760=CARTESIAN_POINT('Ctrl Pts',(-0.58866101856647,-0.0601494696056588,
-1.63932642900401));
#64761=CARTESIAN_POINT('Ctrl Pts',(-0.578651497263644,-0.158109020107328,
-1.63468988568876));
#64762=CARTESIAN_POINT('Ctrl Pts',(-0.543659566334094,-0.253515864312632,
-1.63005334237351));
#64763=CARTESIAN_POINT('Ctrl Pts',(-0.487958958919651,-0.334717504596945,
-1.62541679905825));
#64764=CARTESIAN_POINT('Ctrl Pts',(-0.43225835150521,-0.415919144881255,
-1.620780255743));
#64765=CARTESIAN_POINT('Ctrl Pts',(-0.355849067605877,-0.482915581244573,
-1.61614371242774));
#64766=CARTESIAN_POINT('Ctrl Pts',(-0.268063341261597,-0.527524216074698,
-1.61150716911249));
#64767=CARTESIAN_POINT('Ctrl Pts',(-0.180277614917312,-0.572132850904825,
-1.60687062579724));
#64768=CARTESIAN_POINT('Ctrl Pts',(-0.0811154461280793,-0.594353684201755,
-1.60223408248199));
#64769=CARTESIAN_POINT('Ctrl Pts',(0.0173120115940635,-0.59147277851827,
-1.59759753916673));
#64770=CARTESIAN_POINT('Ctrl Pts',(0.115739469316201,-0.588591872834785,
-1.59296099585148));
#64771=CARTESIAN_POINT('Ctrl Pts',(0.213432215971247,-0.560609228170888,
-1.58832445253623));
#64772=CARTESIAN_POINT('Ctrl Pts',(0.298458565653194,-0.510942499760779,
-1.58368790922097));
#64773=CARTESIAN_POINT('Ctrl Pts',(0.383484915335141,-0.46127577135067,
-1.57905136590572));
#64774=CARTESIAN_POINT('Ctrl Pts',(0.455844868043987,-0.389924959194351,
-1.57441482259047));
#64775=CARTESIAN_POINT('Ctrl Pts',(0.506700754070803,-0.305604481802273,
-1.56977827927522));
#64776=CARTESIAN_POINT('Ctrl Pts',(0.557556640097621,-0.221284004410191,
-1.56514173595996));
#64777=CARTESIAN_POINT('Ctrl Pts',(0.586908459442404,-0.123993861782351,
-1.56050519264471));
#64778=CARTESIAN_POINT('Ctrl Pts',(0.591171332969464,-0.0256165678548721,
-1.55586864932946));
#64779=CARTESIAN_POINT('Ctrl Pts',(0.595434206496523,0.0727607260726045,
-1.5512321060142));
#64780=CARTESIAN_POINT('Ctrl Pts',(0.574608134205857,0.172225171299727,
-1.54659556269895));
#64781=CARTESIAN_POINT('Ctrl Pts',(0.531236704661987,0.260628695836489,
-1.5419590193837));
#64782=CARTESIAN_POINT('Ctrl Pts',(0.487865275118117,0.349032220373248,
-1.53732247606844));
#64783=CARTESIAN_POINT('Ctrl Pts',(0.421948488321044,0.426374824219655,
-1.53268593275319));
#64784=CARTESIAN_POINT('Ctrl Pts',(0.341537079078881,0.483210282473192,
-1.52804938943794));
#64785=CARTESIAN_POINT('Ctrl Pts',(0.261125669836717,0.540045740726729,
-1.52341284612269));
#64786=CARTESIAN_POINT('Ctrl Pts',(0.166219638149465,0.576374053387396,
-1.51877630280743));
#64787=CARTESIAN_POINT('Ctrl Pts',(0.0684103149956289,0.58775826857285,
-1.51413975949218));
#64788=CARTESIAN_POINT('Ctrl Pts',(-0.02939900815821,0.599142483758304,
-1.50950321617693));
#64789=CARTESIAN_POINT('Ctrl Pts',(-0.130111622778631,0.585582601468544,
-1.50486667286167));
#64790=CARTESIAN_POINT('Ctrl Pts',(-0.221427011933022,0.548734755469315,
-1.50023012954642));
#64791=CARTESIAN_POINT('Ctrl Pts',(-0.312742401087413,0.511886909470086,
-1.49559358623117));
#64792=CARTESIAN_POINT('Ctrl Pts',(-0.394660564775773,0.451751099761389,
-1.49095704291591));
#64793=CARTESIAN_POINT('Ctrl Pts',(-0.457176442923603,0.375672002562444,
-1.48632049960066));
#64794=CARTESIAN_POINT('Ctrl Pts',(-0.519692321071433,0.2995929053635,-1.48168395628541));
#64795=CARTESIAN_POINT('Ctrl Pts',(-0.562805913678733,0.207570520674309,
-1.47704741297016));
#64796=CARTESIAN_POINT('Ctrl Pts',(-0.581251549926701,0.110843985769928,
-1.4724108696549));
#64797=CARTESIAN_POINT('Ctrl Pts',(-0.588211416105208,0.0743473461422587,
-1.4706614195101));
#64798=CARTESIAN_POINT('Ctrl Pts',(-0.591659337574339,0.0371809827961072,
-1.46891196936529));
#64799=CARTESIAN_POINT('Ctrl Pts',(-0.591636138149344,1.03689755184515E-5,
-1.46716251922049));
#64800=CARTESIAN_POINT('Origin',(0.,0.,-1.97));
#64801=CARTESIAN_POINT('',(-0.591715913879701,-8.55716902248283E-6,-1.26698748077951));
#64802=CARTESIAN_POINT('',(-0.591723545535282,-4.29287131388572E-6,-1.29216251922049));
#64803=CARTESIAN_POINT('',(-0.591675,-7.2459289488551E-17,-1.97));
#64804=CARTESIAN_POINT('Ctrl Pts',(-0.591715913879701,-8.55716902248283E-6,
-1.26698748077951));
#64805=CARTESIAN_POINT('Ctrl Pts',(-0.591652719613147,0.0898914806554165,
-1.27122030552295));
#64806=CARTESIAN_POINT('Ctrl Pts',(-0.570864102899966,0.17981974451662,
-1.27545313026639));
#64807=CARTESIAN_POINT('Ctrl Pts',(-0.53128372471532,0.260532836354837,
-1.27968595500982));
#64808=CARTESIAN_POINT('Ctrl Pts',(-0.487928247224393,0.348944185536248,
-1.28432249832508));
#64809=CARTESIAN_POINT('Ctrl Pts',(-0.422025416978272,0.426298682244433,
-1.28895904164033));
#64810=CARTESIAN_POINT('Ctrl Pts',(-0.341624264204252,0.483148649044355,
-1.29359558495558));
#64811=CARTESIAN_POINT('Ctrl Pts',(-0.261223111430231,0.539998615844276,
-1.29823212827084));
#64812=CARTESIAN_POINT('Ctrl Pts',(-0.166323636128309,0.576344052735935,
-1.30286867158609));
#64813=CARTESIAN_POINT('Ctrl Pts',(-0.0685163685140617,0.58774591637214,
-1.30750521490134));
#64814=CARTESIAN_POINT('Ctrl Pts',(0.0292908991001856,0.599147780008344,
-1.3121417582166));
#64815=CARTESIAN_POINT('Ctrl Pts',(0.13000595902676,0.585606070389094,-1.31677830153185));
#64816=CARTESIAN_POINT('Ctrl Pts',(0.221327995676024,0.548774701764317,
-1.3214148448471));
#64817=CARTESIAN_POINT('Ctrl Pts',(0.312650032325287,0.51194333313954,-1.32605138816235));
#64818=CARTESIAN_POINT('Ctrl Pts',(0.39457904569724,0.451822305509234,-1.33068793147761));
#64819=CARTESIAN_POINT('Ctrl Pts',(0.457108650593243,0.375754489686159,
-1.33532447479286));
#64820=CARTESIAN_POINT('Ctrl Pts',(0.519638255489244,0.299686673863085,
-1.33996101810811));
#64821=CARTESIAN_POINT('Ctrl Pts',(0.562768451909297,0.207672069847241,
-1.34459756142337));
#64822=CARTESIAN_POINT('Ctrl Pts',(0.58123154113094,0.110948864622555,-1.34923410473862));
#64823=CARTESIAN_POINT('Ctrl Pts',(0.599694630352582,0.0142256593978662,
-1.35387064805387));
#64824=CARTESIAN_POINT('Ctrl Pts',(0.593490612375815,-0.0872061470356578,
-1.35850719136912));
#64825=CARTESIAN_POINT('Ctrl Pts',(0.563377213811757,-0.180958199383677,
-1.36314373468438));
#64826=CARTESIAN_POINT('Ctrl Pts',(0.533263815247699,-0.274710251731697,
-1.36778027799963));
#64827=CARTESIAN_POINT('Ctrl Pts',(0.479241036096351,-0.360782549994205,
-1.37241682131488));
#64828=CARTESIAN_POINT('Ctrl Pts',(0.407906938697792,-0.42866266962342,
-1.37705336463014));
#64829=CARTESIAN_POINT('Ctrl Pts',(0.336572841299233,-0.496542789252635,
-1.38168990794539));
#64830=CARTESIAN_POINT('Ctrl Pts',(0.247927425653462,-0.546230730248557,
-1.38632645126064));
#64831=CARTESIAN_POINT('Ctrl Pts',(0.152797383533493,-0.571657864943534,
-1.3909629945759));
#64832=CARTESIAN_POINT('Ctrl Pts',(0.0576673414135263,-0.59708499963851,
-1.39559953789115));
#64833=CARTESIAN_POINT('Ctrl Pts',(-0.043947327180648,-0.598251328032543,
-1.4002360812064));
#64834=CARTESIAN_POINT('Ctrl Pts',(-0.139635933117813,-0.575014400818622,
-1.40487262452166));
#64835=CARTESIAN_POINT('Ctrl Pts',(-0.235324539054983,-0.551777473604699,
-1.40950916783691));
#64836=CARTESIAN_POINT('Ctrl Pts',(-0.325087082335145,-0.504137290782826,
-1.41414571115216));
#64837=CARTESIAN_POINT('Ctrl Pts',(-0.397960431004153,-0.437912377447213,
-1.41878225446741));
#64838=CARTESIAN_POINT('Ctrl Pts',(-0.47083377967316,-0.3716874641116,-1.42341879778267));
#64839=CARTESIAN_POINT('Ctrl Pts',(-0.526817933731005,-0.286877820262249,
-1.42805534109792));
#64840=CARTESIAN_POINT('Ctrl Pts',(-0.5590752786689,-0.193841656379048,
-1.43269188441317));
#64841=CARTESIAN_POINT('Ctrl Pts',(-0.580632376849192,-0.131666988159784,
-1.43579041653529));
#64842=CARTESIAN_POINT('Ctrl Pts',(-0.591592968764511,-0.065818316806051,
-1.4388889486574));
#64843=CARTESIAN_POINT('Ctrl Pts',(-0.591646097050001,1.31033435099431E-5,
-1.44198748077951));
#64844=CARTESIAN_POINT('Ctrl Pts',(-0.591636138149344,1.03689755184515E-5,
-1.46716251922049));
#64845=CARTESIAN_POINT('Ctrl Pts',(-0.59159785246189,-0.0613317765103333,
-1.46427542605004));
#64846=CARTESIAN_POINT('Ctrl Pts',(-0.582106163230953,-0.122685497925498,
-1.46138833287959));
#64847=CARTESIAN_POINT('Ctrl Pts',(-0.563344551531624,-0.181059851245905,
-1.45850123970914));
#64848=CARTESIAN_POINT('Ctrl Pts',(-0.533214236999943,-0.274806468237785,
-1.45386469639389));
#64849=CARTESIAN_POINT('Ctrl Pts',(-0.479175928047944,-0.360869017101977,
-1.44922815307864));
#64850=CARTESIAN_POINT('Ctrl Pts',(-0.407829583745096,-0.428736264031698,
-1.44459160976339));
#64851=CARTESIAN_POINT('Ctrl Pts',(-0.336483239442246,-0.49660351096142,
-1.43995506644813));
#64852=CARTESIAN_POINT('Ctrl Pts',(-0.247828859788544,-0.546275455956669,
-1.43531852313288));
#64853=CARTESIAN_POINT('Ctrl Pts',(-0.152694231374487,-0.571685425018436,
-1.43068197981763));
#64854=CARTESIAN_POINT('Ctrl Pts',(-0.0575596029604325,-0.597095394080203,
-1.42604543650237));
#64855=CARTESIAN_POINT('Ctrl Pts',(0.0440552742139777,-0.59824338720849,
-1.42140889318712));
#64856=CARTESIAN_POINT('Ctrl Pts',(0.139739685542633,-0.574989194470645,
-1.41677234987187));
#64857=CARTESIAN_POINT('Ctrl Pts',(0.235424096871292,-0.5517350017328,-1.41213580655661));
#64858=CARTESIAN_POINT('Ctrl Pts',(0.325178042354196,-0.504078623128823,
-1.40749926324136));
#64859=CARTESIAN_POINT('Ctrl Pts',(0.398039440127595,-0.437840561821843,
-1.40286271992611));
#64860=CARTESIAN_POINT('Ctrl Pts',(0.470900837900994,-0.371602500514862,
-1.39822617661086));
#64861=CARTESIAN_POINT('Ctrl Pts',(0.526869687964888,-0.28678275650488,
-1.3935896332956));
#64862=CARTESIAN_POINT('Ctrl Pts',(0.559110244961018,-0.193740773853068,
-1.38895308998035));
#64863=CARTESIAN_POINT('Ctrl Pts',(0.591350801957148,-0.100698791201256,
-1.3843165466651));
#64864=CARTESIAN_POINT('Ctrl Pts',(0.599863065885513,0.000565430092384633,
-1.37968000334984));
#64865=CARTESIAN_POINT('Ctrl Pts',(0.58360739293406,0.0976840027141863,
-1.37504346003459));
#64866=CARTESIAN_POINT('Ctrl Pts',(0.567351719982608,0.194802575335988,
-1.37040691671934));
#64867=CARTESIAN_POINT('Ctrl Pts',(0.526328110151338,0.28777549928595,-1.36577037340408));
#64868=CARTESIAN_POINT('Ctrl Pts',(0.465546974591508,0.365247543348685,
-1.36113383008883));
#64869=CARTESIAN_POINT('Ctrl Pts',(0.404765839031678,0.44271958741142,-1.35649728677358));
#64870=CARTESIAN_POINT('Ctrl Pts',(0.324227177743289,0.504690751586928,
-1.35186074345833));
#64871=CARTESIAN_POINT('Ctrl Pts',(0.233767565525252,0.543592198970839,
-1.34722420014307));
#64872=CARTESIAN_POINT('Ctrl Pts',(0.143307953307216,0.58249364635475,-1.34258765682782));
#64873=CARTESIAN_POINT('Ctrl Pts',(0.0429273901595324,0.598325376947065,
-1.33795111351257));
#64874=CARTESIAN_POINT('Ctrl Pts',(-0.0551141620316234,0.589153785201375,
-1.33331457019731));
#64875=CARTESIAN_POINT('Ctrl Pts',(-0.153155714222779,0.579982193455684,
-1.32867802688206));
#64876=CARTESIAN_POINT('Ctrl Pts',(-0.248858255457407,0.545807279371989,
-1.32404148356681));
#64877=CARTESIAN_POINT('Ctrl Pts',(-0.330533173207798,0.490802989887734,
-1.31940494025155));
#64878=CARTESIAN_POINT('Ctrl Pts',(-0.412208090958186,0.435798700403481,
-1.3147683969363));
#64879=CARTESIAN_POINT('Ctrl Pts',(-0.479855385224338,0.359965035518671,
-1.31013185362105));
#64880=CARTESIAN_POINT('Ctrl Pts',(-0.525212965982056,0.272563926149239,
-1.3054953103058));
#64881=CARTESIAN_POINT('Ctrl Pts',(-0.568689546648524,0.188787381669575,
-1.30105104661069));
#64882=CARTESIAN_POINT('Ctrl Pts',(-0.591686809655619,0.0943829136852825,
-1.29660678291559));
#64883=CARTESIAN_POINT('Ctrl Pts',(-0.591723545535282,-4.29287131388572E-6,
-1.29216251922049));
#64884=CARTESIAN_POINT('Origin',(0.,0.,-1.97));
#64885=CARTESIAN_POINT('',(-0.591624151837836,5.41149558302978E-7,-1.09198748077951));
#64886=CARTESIAN_POINT('',(-0.591625419221713,-3.63663382748259E-6,-1.11716251922049));
#64887=CARTESIAN_POINT('',(-0.591675,-7.2459289488551E-17,-1.97));
#64888=CARTESIAN_POINT('Ctrl Pts',(-0.591624151837836,5.41149558302978E-7,
-1.09198748077951));
#64889=CARTESIAN_POINT('Ctrl Pts',(-0.591625697888236,0.0486823199268314,
-1.09427857575799));
#64890=CARTESIAN_POINT('Ctrl Pts',(-0.585685602356747,0.0973637280149376,
-1.09656967073648));
#64891=CARTESIAN_POINT('Ctrl Pts',(-0.573799481656066,0.144547258077456,
-1.09886076571496));
#64892=CARTESIAN_POINT('Ctrl Pts',(-0.549745256930946,0.240033688345932,
-1.10349730903021));
#64893=CARTESIAN_POINT('Ctrl Pts',(-0.501339337015882,0.32938562236306,
-1.10813385234546));
#64894=CARTESIAN_POINT('Ctrl Pts',(-0.434493770166178,0.4016900778626,-1.11277039566072));
#64895=CARTESIAN_POINT('Ctrl Pts',(-0.367648203316469,0.473994533362146,
-1.11740693897597));
#64896=CARTESIAN_POINT('Ctrl Pts',(-0.282362989532117,0.5292515103441,-1.12204348229122));
#64897=CARTESIAN_POINT('Ctrl Pts',(-0.189054422940825,0.560712207940038,
-1.12668002560648));
#64898=CARTESIAN_POINT('Ctrl Pts',(-0.0957458563495401,0.592172905535974,
-1.13131656892173));
#64899=CARTESIAN_POINT('Ctrl Pts',(0.00558606304868453,0.599837323745897,
-1.13595311223698));
#64900=CARTESIAN_POINT('Ctrl Pts',(0.102565179644448,0.582769370240907,
-1.14058965555223));
#64901=CARTESIAN_POINT('Ctrl Pts',(0.199544296240211,0.565701416735917,
-1.14522619886749));
#64902=CARTESIAN_POINT('Ctrl Pts',(0.292170610033512,0.523901091516013,
-1.14986274218274));
#64903=CARTESIAN_POINT('Ctrl Pts',(0.369131222977626,0.462473669725665,
-1.15449928549799));
#64904=CARTESIAN_POINT('Ctrl Pts',(0.446091835921745,0.401046247935313,
-1.15913582881325));
#64905=CARTESIAN_POINT('Ctrl Pts',(0.507386748016674,0.319991729574514,
-1.1637723721285));
#64906=CARTESIAN_POINT('Ctrl Pts',(0.545529716283336,0.229209693552223,
-1.16840891544375));
#64907=CARTESIAN_POINT('Ctrl Pts',(0.583672684549996,0.138427657529934,
-1.17304545875901));
#64908=CARTESIAN_POINT('Ctrl Pts',(0.598663708988391,0.0379181038461522,
-1.17768200207426));
#64909=CARTESIAN_POINT('Ctrl Pts',(0.588671863545843,-0.0600432513772004,
-1.18231854538951));
#64910=CARTESIAN_POINT('Ctrl Pts',(0.578680018103295,-0.158004606600553,
-1.18695508870476));
#64911=CARTESIAN_POINT('Ctrl Pts',(0.543705302779803,-0.253417763363477,
-1.19159163202002));
#64912=CARTESIAN_POINT('Ctrl Pts',(0.488019348092275,-0.334629453058263,
-1.19622817533527));
#64913=CARTESIAN_POINT('Ctrl Pts',(0.432333393404748,-0.415841142753046,
-1.20086471865052));
#64914=CARTESIAN_POINT('Ctrl Pts',(0.355936199353185,-0.482851365379693,
-1.20550126196578));
#64915=CARTESIAN_POINT('Ctrl Pts',(0.268158523386165,-0.527475839543227,
-1.21013780528103));
#64916=CARTESIAN_POINT('Ctrl Pts',(0.180380847419145,-0.572100313706762,
-1.21477434859628));
#64917=CARTESIAN_POINT('Ctrl Pts',(0.0812226895366682,-0.594339039407184,
-1.21941089191153));
#64918=CARTESIAN_POINT('Ctrl Pts',(-0.0172052866205986,-0.591475893911818,
-1.22404743522679));
#64919=CARTESIAN_POINT('Ctrl Pts',(-0.115633262777868,-0.588612748416452,
-1.22868397854204));
#64920=CARTESIAN_POINT('Ctrl Pts',(-0.213331057209928,-0.560647731725296,
-1.2333205218573));
#64921=CARTESIAN_POINT('Ctrl Pts',(-0.298366367501436,-0.510996346083296,
-1.23795706517255));
#64922=CARTESIAN_POINT('Ctrl Pts',(-0.383401677792944,-0.461344960441296,
-1.2425936084878));
#64923=CARTESIAN_POINT('Ctrl Pts',(-0.4557745039439,-0.390007205848451,
-1.24723015180305));
#64924=CARTESIAN_POINT('Ctrl Pts',(-0.506645603949854,-0.30569590603207,
-1.25186669511831));
#64925=CARTESIAN_POINT('Ctrl Pts',(-0.557516703955809,-0.221384606215688,
-1.25650323843356));
#64926=CARTESIAN_POINT('Ctrl Pts',(-0.586886077816762,-0.124099761175768,
-1.26113978174881));
#64927=CARTESIAN_POINT('Ctrl Pts',(-0.591166702379371,-0.0257232378284896,
-1.26577632506407));
#64928=CARTESIAN_POINT('Ctrl Pts',(-0.591539429973483,-0.0171572810789546,
-1.26618004363588));
#64929=CARTESIAN_POINT('Ctrl Pts',(-0.591721941225643,-0.00858304750972869,
-1.26658376220769));
#64930=CARTESIAN_POINT('Ctrl Pts',(-0.591715913879701,-8.55716902248283E-6,
-1.26698748077951));
#64931=CARTESIAN_POINT('Ctrl Pts',(-0.591723545535282,-4.29287131388572E-6,
-1.29216251922049));
#64932=CARTESIAN_POINT('Ctrl Pts',(-0.591725134901142,-0.00408792459727398,
-1.29197023960034));
#64933=CARTESIAN_POINT('Ctrl Pts',(-0.591683746017117,-0.00817152401274099,
-1.29177795998019));
#64934=CARTESIAN_POINT('Ctrl Pts',(-0.59159917794444,-0.0122542290259055,
-1.29158568036004));
#64935=CARTESIAN_POINT('Ctrl Pts',(-0.589559941899822,-0.11070272097756,
-1.28694913704478));
#64936=CARTESIAN_POINT('Ctrl Pts',(-0.562413602561303,-0.208631151026815,
-1.28231259372953));
#64937=CARTESIAN_POINT('Ctrl Pts',(-0.513475673163749,-0.294079048119024,
-1.27767605041428));
#64938=CARTESIAN_POINT('Ctrl Pts',(-0.464537743766196,-0.37952694521123,
-1.27303950709902));
#64939=CARTESIAN_POINT('Ctrl Pts',(-0.393808224309609,-0.452494309346392,
-1.26840296378377));
#64940=CARTESIAN_POINT('Ctrl Pts',(-0.309925651833169,-0.504069284731118,
-1.26376642046852));
#64941=CARTESIAN_POINT('Ctrl Pts',(-0.226043079356727,-0.555644260115845,
-1.25912987715326));
#64942=CARTESIAN_POINT('Ctrl Pts',(-0.129007453860431,-0.585826846750134,
-1.25449333383801));
#64943=CARTESIAN_POINT('Ctrl Pts',(-0.0306702038766711,-0.590930699885967,
-1.24985679052276));
#64944=CARTESIAN_POINT('Ctrl Pts',(0.0676670461070893,-0.596034553021801,
-1.24522024720751));
#64945=CARTESIAN_POINT('Ctrl Pts',(0.167305920578315,-0.576059672659178,
-1.24058370389225));
#64946=CARTESIAN_POINT('Ctrl Pts',(0.256077043662899,-0.533445687190763,
-1.235947160577));
#64947=CARTESIAN_POINT('Ctrl Pts',(0.344848166747481,-0.490831701722349,
-1.23131061726175));
#64948=CARTESIAN_POINT('Ctrl Pts',(0.422751538445423,-0.425578611148145,
-1.22667407394649));
#64949=CARTESIAN_POINT('Ctrl Pts',(0.480272444574299,-0.345656089858378,
-1.22203753063124));
#64950=CARTESIAN_POINT('Ctrl Pts',(0.537793350703178,-0.265733568568606,
-1.21740098731599));
#64951=CARTESIAN_POINT('Ctrl Pts',(0.574931791262988,-0.17114161656327,
-1.21276444400074));
#64952=CARTESIAN_POINT('Ctrl Pts',(0.587151869547258,-0.073433204755854,
-1.20812790068548));
#64953=CARTESIAN_POINT('Ctrl Pts',(0.599371947831528,0.0242752070515565,
-1.20349135737023));
#64954=CARTESIAN_POINT('Ctrl Pts',(0.586673663840261,0.125100078661047,
-1.19885481405498));
#64955=CARTESIAN_POINT('Ctrl Pts',(0.550607920187181,0.216727182652991,
-1.19421827073972));
#64956=CARTESIAN_POINT('Ctrl Pts',(0.514542176534101,0.308354286644934,
-1.18958172742447));
#64957=CARTESIAN_POINT('Ctrl Pts',(0.455108973219207,0.390783623019332,
-1.18494518410922));
#64958=CARTESIAN_POINT('Ctrl Pts',(0.37956717375716,0.453947699718324,-1.18030864079397));
#64959=CARTESIAN_POINT('Ctrl Pts',(0.304025374295109,0.517111776417319,
-1.17567209747871));
#64960=CARTESIAN_POINT('Ctrl Pts',(0.212374978685904,0.561010593440907,
-1.17103555416346));
#64961=CARTESIAN_POINT('Ctrl Pts',(0.11580969138574,0.580282576728524,-1.1663990108482));
#64962=CARTESIAN_POINT('Ctrl Pts',(0.0192444040855797,0.59955456001614,
-1.16176246753295));
#64963=CARTESIAN_POINT('Ctrl Pts',(-0.082235774905539,0.594199709567786,
-1.1571259242177));
#64964=CARTESIAN_POINT('Ctrl Pts',(-0.176236582319707,0.564872039072412,
-1.15248938090245));
#64965=CARTESIAN_POINT('Ctrl Pts',(-0.270237389733872,0.535544368577038,
-1.14785283758719));
#64966=CARTESIAN_POINT('Ctrl Pts',(-0.356758825571087,0.482243878034646,
-1.14321629427194));
#64967=CARTESIAN_POINT('Ctrl Pts',(-0.425233609947291,0.411480413196972,
-1.13857975095669));
#64968=CARTESIAN_POINT('Ctrl Pts',(-0.493708394323496,0.340716948359297,
-1.13394320764143));
#64969=CARTESIAN_POINT('Ctrl Pts',(-0.544136527238688,0.25249050922634,
-1.12930666432618));
#64970=CARTESIAN_POINT('Ctrl Pts',(-0.570358977819315,0.157576615950659,
-1.12467012101093));
#64971=CARTESIAN_POINT('Ctrl Pts',(-0.584512317462174,0.106347667526243,
-1.12216758708078));
#64972=CARTESIAN_POINT('Ctrl Pts',(-0.591614041410101,0.0531705254529068,
-1.11966505315064));
#64973=CARTESIAN_POINT('Ctrl Pts',(-0.591625419221713,-3.63663382748259E-6,
-1.11716251922049));
#64974=CARTESIAN_POINT('Origin',(0.,0.,-1.97));
#64975=CARTESIAN_POINT('',(-0.591718276663101,7.52894403206403E-6,-0.916987480779508));
#64976=CARTESIAN_POINT('',(-0.591707850850199,1.11928198428649E-5,-0.942162519220489));
#64977=CARTESIAN_POINT('',(-0.591675,-7.2459289488551E-17,-1.97));
#64978=CARTESIAN_POINT('Ctrl Pts',(-0.591718276663101,7.52894403206403E-6,
-0.916987480779508));
#64979=CARTESIAN_POINT('Ctrl Pts',(-0.591722974652918,0.0074275342378391,
-0.917336845993036));
#64980=CARTESIAN_POINT('Ctrl Pts',(-0.591586310640105,0.0148473662541653,
-0.917686211206564));
#64981=CARTESIAN_POINT('Ctrl Pts',(-0.591307166968182,0.02226183412354,
-0.918035576420092));
#64982=CARTESIAN_POINT('Ctrl Pts',(-0.587602557362138,0.120661732295286,
-0.922672119735345));
#64983=CARTESIAN_POINT('Ctrl Pts',(-0.558803237227458,0.218116851992544,
-0.927308663050598));
#64984=CARTESIAN_POINT('Ctrl Pts',(-0.50842660630895,0.302724529834708,
-0.931945206365852));
#64985=CARTESIAN_POINT('Ctrl Pts',(-0.45804997539044,0.387332207676875,
-0.936581749681105));
#64986=CARTESIAN_POINT('Ctrl Pts',(-0.386096033688106,0.459092443663951,
-0.941218292996357));
#64987=CARTESIAN_POINT('Ctrl Pts',(-0.301352862830176,0.50924081438013,
-0.94585483631161));
#64988=CARTESIAN_POINT('Ctrl Pts',(-0.216609691972246,0.55938918509631,
-0.950491379626863));
#64989=CARTESIAN_POINT('Ctrl Pts',(-0.119077291958735,0.587925690541584,
-0.955127922942115));
#64990=CARTESIAN_POINT('Ctrl Pts',(-0.020667764787635,0.591365029795611,
-0.959764466257368));
#64991=CARTESIAN_POINT('Ctrl Pts',(0.0777417623834591,0.594804369049637,
-0.964401009572621));
#64992=CARTESIAN_POINT('Ctrl Pts',(0.177028416712141,0.573146542112413,
-0.969037552887874));
#64993=CARTESIAN_POINT('Ctrl Pts',(0.265065840667561,0.529036723751461,
-0.973674096203127));
#64994=CARTESIAN_POINT('Ctrl Pts',(0.353103264622989,0.484926905390506,
-0.97831063951838));
#64995=CARTESIAN_POINT('Ctrl Pts',(0.429891458205161,0.418365095605818,
-0.982947182833634));
#64996=CARTESIAN_POINT('Ctrl Pts',(0.486051909308696,0.337480808971196,
-0.987583726148887));
#64997=CARTESIAN_POINT('Ctrl Pts',(0.542212360412227,0.256596522336578,
-0.99222026946414));
#64998=CARTESIAN_POINT('Ctrl Pts',(0.577745069037122,0.161389758852027,
-0.996856812779392));
#64999=CARTESIAN_POINT('Ctrl Pts',(0.588310254255745,0.0634885793196063,
-1.00149335609465));
#65000=CARTESIAN_POINT('Ctrl Pts',(0.598875439474368,-0.0344126002128146,
-1.0061298994099));
#65001=CARTESIAN_POINT('Ctrl Pts',(0.584473101286718,-0.135008195793106,
-1.01076644272515));
#65002=CARTESIAN_POINT('Ctrl Pts',(0.546862266656937,-0.226011982587911,
-1.0154029860404));
#65003=CARTESIAN_POINT('Ctrl Pts',(0.509251432027154,-0.317015769382721,
-1.02003952935566));
#65004=CARTESIAN_POINT('Ctrl Pts',(0.448432100955235,-0.398427747392044,
-1.02467607267091));
#65005=CARTESIAN_POINT('Ctrl Pts',(0.371832431418214,-0.460304679437544,
-1.02931261598616));
#65006=CARTESIAN_POINT('Ctrl Pts',(0.295232761881193,-0.522181611483043,
-1.03394915930142));
#65007=CARTESIAN_POINT('Ctrl Pts',(0.202852753879069,-0.564523497564719,
-1.03858570261667));
#65008=CARTESIAN_POINT('Ctrl Pts',(0.105975222945406,-0.582158919100406,
-1.04322224593192));
#65009=CARTESIAN_POINT('Ctrl Pts',(0.00909769201174822,-0.599794340636091,
-1.04785878924718));
#65010=CARTESIAN_POINT('Ctrl Pts',(-0.0922773618534477,-0.592723297625791,
-1.05249533256243));
#65011=CARTESIAN_POINT('Ctrl Pts',(-0.185768514820475,-0.561809410625949,
-1.05713187587768));
#65012=CARTESIAN_POINT('Ctrl Pts',(-0.279259667787502,-0.530895523626107,
-1.06176841919293));
#65013=CARTESIAN_POINT('Ctrl Pts',(-0.364866919856361,-0.476138792636723,
-1.06640496250819));
#65014=CARTESIAN_POINT('Ctrl Pts',(-0.432134644811843,-0.404226921072587,
-1.07104150582344));
#65015=CARTESIAN_POINT('Ctrl Pts',(-0.499402369767325,-0.332315049508451,
-1.07567804913869));
#65016=CARTESIAN_POINT('Ctrl Pts',(-0.54833056760943,-0.243248037369564,
-1.08031459245395));
#65017=CARTESIAN_POINT('Ctrl Pts',(-0.572943401762895,-0.147904068040208,
-1.0849511357692));
#65018=CARTESIAN_POINT('Ctrl Pts',(-0.585394084740131,-0.0996732333257132,
-1.08729658410597));
#65019=CARTESIAN_POINT('Ctrl Pts',(-0.591622569109328,-0.049836151845043,
-1.08964203244274));
#65020=CARTESIAN_POINT('Ctrl Pts',(-0.591624151837836,5.41149558302978E-7,
-1.09198748077951));
#65021=CARTESIAN_POINT('Ctrl Pts',(-0.591625419221713,-3.63663382748259E-6,
-1.11716251922049));
#65022=CARTESIAN_POINT('Ctrl Pts',(-0.591635121530429,-0.0453473418964572,
-1.11502850983538));
#65023=CARTESIAN_POINT('Ctrl Pts',(-0.586488975449466,-0.0906888802184572,
-1.11289450045028));
#65024=CARTESIAN_POINT('Ctrl Pts',(-0.576162964933303,-0.134818364152742,
-1.11076049106517));
#65025=CARTESIAN_POINT('Ctrl Pts',(-0.553727733220603,-0.230698103562057,
-1.10612394774992));
#65026=CARTESIAN_POINT('Ctrl Pts',(-0.506840501549141,-0.320856234962282,
-1.10148740443466));
#65027=CARTESIAN_POINT('Ctrl Pts',(-0.441227833460853,-0.394281311315915,
-1.09685086111941));
#65028=CARTESIAN_POINT('Ctrl Pts',(-0.375615165372566,-0.467706387669546,
-1.09221431780416));
#65029=CARTESIAN_POINT('Ctrl Pts',(-0.291277060867453,-0.524398408976585,
-1.0875777744889));
#65030=CARTESIAN_POINT('Ctrl Pts',(-0.198514139053056,-0.557433305490064,
-1.08294123117365));
#65031=CARTESIAN_POINT('Ctrl Pts',(-0.105751217238654,-0.590468202003546,
-1.0783046878584));
#65032=CARTESIAN_POINT('Ctrl Pts',(-0.00456347811496688,-0.599845973723464,
-1.07366814454314));
#65033=CARTESIAN_POINT('Ctrl Pts',(0.0926905321403009,-0.584421268200519,
-1.06903160122789));
#65034=CARTESIAN_POINT('Ctrl Pts',(0.189944542395563,-0.568996562677575,
-1.06439505791264));
#65035=CARTESIAN_POINT('Ctrl Pts',(0.283264823782407,-0.52876937991177,
-1.05975851459739));
#65036=CARTESIAN_POINT('Ctrl Pts',(0.361253720647849,-0.468652859579073,
-1.05512197128213));
#65037=CARTESIAN_POINT('Ctrl Pts',(0.43924261751329,-0.408536339246375,
-1.05048542796688));
#65038=CARTESIAN_POINT('Ctrl Pts',(0.501900129857331,-0.328530481346785,
-1.04584888465163));
#65039=CARTESIAN_POINT('Ctrl Pts',(0.541573593766437,-0.238406786833893,
-1.04121234133637));
#65040=CARTESIAN_POINT('Ctrl Pts',(0.581247057675546,-0.148283092320996,
-1.03657579802112));
#65041=CARTESIAN_POINT('Ctrl Pts',(0.597936473149718,-0.048041561194797,
-1.03193925470587));
#65042=CARTESIAN_POINT('Ctrl Pts',(0.589603481454953,0.0500748253092742,
-1.02730271139062));
#65043=CARTESIAN_POINT('Ctrl Pts',(0.581270489760189,0.14819121181334,-1.02266616807536));
#65044=CARTESIAN_POINT('Ctrl Pts',(0.54791509089649,0.244182453695277,-1.01802962476011));
#65045=CARTESIAN_POINT('Ctrl Pts',(0.493611140458446,0.326324678026145,
-1.01339308144486));
#65046=CARTESIAN_POINT('Ctrl Pts',(0.439307190020401,0.408466902357016,
-1.0087565381296));
#65047=CARTESIAN_POINT('Ctrl Pts',(0.364054688008008,0.476760109136816,
-1.00411999481435));
#65048=CARTESIAN_POINT('Ctrl Pts',(0.277044585115118,0.522863319933563,
-0.999483451499097));
#65049=CARTESIAN_POINT('Ctrl Pts',(0.190034482222228,0.568966530730311,
-0.994846908183844));
#65050=CARTESIAN_POINT('Ctrl Pts',(0.0912667784488393,0.592879745544007,
-0.990210364868592));
#65051=CARTESIAN_POINT('Ctrl Pts',(-0.00719555060622232,0.591682328217624,
-0.985573821553339));
#65052=CARTESIAN_POINT('Ctrl Pts',(-0.105657879661281,0.590484910891242,
-0.980937278238086));
#65053=CARTESIAN_POINT('Ctrl Pts',(-0.203814833998013,0.564176861424783,
-0.976300734922833));
#65054=CARTESIAN_POINT('Ctrl Pts',(-0.289678031789344,0.515971308671526,
-0.97166419160758));
#65055=CARTESIAN_POINT('Ctrl Pts',(-0.37554122958068,0.467765755918267,
-0.967027648292327));
#65056=CARTESIAN_POINT('Ctrl Pts',(-0.449110670826613,0.397662699878209,
-0.962391104977074));
#65057=CARTESIAN_POINT('Ctrl Pts',(-0.501400965154952,0.314224164594702,
-0.95775456166182));
#65058=CARTESIAN_POINT('Ctrl Pts',(-0.553691259483289,0.230785629311198,
-0.953118018346567));
#65059=CARTESIAN_POINT('Ctrl Pts',(-0.584702406894033,0.134011614784245,
-0.948481475031314));
#65060=CARTESIAN_POINT('Ctrl Pts',(-0.590646866518909,0.0357215977379096,
-0.943844931716061));
#65061=CARTESIAN_POINT('Ctrl Pts',(-0.591365867181854,0.0238331180649364,
-0.94328412755087));
#65062=CARTESIAN_POINT('Ctrl Pts',(-0.591718151075332,0.0119224598117231,
-0.94272332338568));
#65063=CARTESIAN_POINT('Ctrl Pts',(-0.591707850850199,1.11928198428649E-5,
-0.942162519220489));
#65064=CARTESIAN_POINT('Origin',(0.,0.,-1.97));
#65065=CARTESIAN_POINT('',(-0.591643300061755,-1.24859503531638E-5,-0.741987480779508));
#65066=CARTESIAN_POINT('',(-0.591654968200026,-1.45109499015529E-5,-0.76716251922049));
#65067=CARTESIAN_POINT('',(-0.591675,-7.2459289488551E-17,-1.97));
#65068=CARTESIAN_POINT('Ctrl Pts',(-0.591643300061755,-1.24859503531638E-5,
-0.741987480779508));
#65069=CARTESIAN_POINT('Ctrl Pts',(-0.591593891768562,0.0646650190051903,
-0.745031659543333));
#65070=CARTESIAN_POINT('Ctrl Pts',(-0.581021510217558,0.129358282919564,
-0.748075838307159));
#65071=CARTESIAN_POINT('Ctrl Pts',(-0.560200536082961,0.190565249557322,
-0.751120017070985));
#65072=CARTESIAN_POINT('Ctrl Pts',(-0.528488420622464,0.283788668425994,
-0.755756560386238));
#65073=CARTESIAN_POINT('Ctrl Pts',(-0.473001740813173,0.368924615940348,
-0.76039310370149));
#65074=CARTESIAN_POINT('Ctrl Pts',(-0.400517352236696,0.435575028581515,
-0.765029647016743));
#65075=CARTESIAN_POINT('Ctrl Pts',(-0.328032963660219,0.502225441222683,
-0.769666190331996));
#65076=CARTESIAN_POINT('Ctrl Pts',(-0.238550866316555,0.550390318990665,
-0.77430273364725));
#65077=CARTESIAN_POINT('Ctrl Pts',(-0.142999939946241,0.5741870532691,-0.778939276962502));
#65078=CARTESIAN_POINT('Ctrl Pts',(-0.0474490135759239,0.597983787547536,
-0.783575820277755));
#65079=CARTESIAN_POINT('Ctrl Pts',(0.054170741821044,0.597412378336424,
-0.788212363593008));
#65080=CARTESIAN_POINT('Ctrl Pts',(0.149448015837724,0.572542614596196,
-0.792848906908261));
#65081=CARTESIAN_POINT('Ctrl Pts',(0.244725289854398,0.547672850855969,
-0.797485450223514));
#65082=CARTESIAN_POINT('Ctrl Pts',(0.333660082490784,0.49850473258663,-0.802121993538768));
#65083=CARTESIAN_POINT('Ctrl Pts',(0.405390358967573,0.431043399001334,
-0.806758536854021));
#65084=CARTESIAN_POINT('Ctrl Pts',(0.477120635444364,0.363582065416036,
-0.811395080169274));
#65085=CARTESIAN_POINT('Ctrl Pts',(0.531646395761552,0.27782751651479,-0.816031623484526));
#65086=CARTESIAN_POINT('Ctrl Pts',(0.562308146065541,0.184253368584715,
-0.820668166799779));
#65087=CARTESIAN_POINT('Ctrl Pts',(0.592969896369529,0.0906792206546452,
-0.825304710115031));
#65088=CARTESIAN_POINT('Ctrl Pts',(0.599767636660314,-0.0107145263042522,
-0.829941253430284));
#65089=CARTESIAN_POINT('Ctrl Pts',(0.581871126159565,-0.107544165384645,
-0.834577796745537));
#65090=CARTESIAN_POINT('Ctrl Pts',(0.563974615658815,-0.204373804465043,
-0.839214340060791));
#65091=CARTESIAN_POINT('Ctrl Pts',(0.52138385436653,-0.296639335666945,
-0.843850883376044));
#65092=CARTESIAN_POINT('Ctrl Pts',(0.459300657193611,-0.373071925060032,
-0.848487426691297));
#65093=CARTESIAN_POINT('Ctrl Pts',(0.397217460020693,-0.449504514453119,
-0.85312397000655));
#65094=CARTESIAN_POINT('Ctrl Pts',(0.315641826967143,-0.510104162037391,
-0.857760513321803));
#65095=CARTESIAN_POINT('Ctrl Pts',(0.224536983190461,-0.547469540838764,
-0.862397056637056));
#65096=CARTESIAN_POINT('Ctrl Pts',(0.13343213941378,-0.584834919640138,
-0.867033599952309));
#65097=CARTESIAN_POINT('Ctrl Pts',(0.032798084913967,-0.598966029658612,
-0.871670143267562));
#65098=CARTESIAN_POINT('Ctrl Pts',(-0.0650742583024552,-0.588136970333329,
-0.876306686582815));
#65099=CARTESIAN_POINT('Ctrl Pts',(-0.162946601518877,-0.577307911008045,
-0.880943229898068));
#65100=CARTESIAN_POINT('Ctrl Pts',(-0.258057233451909,-0.541518682339004,
-0.885579773213321));
#65101=CARTESIAN_POINT('Ctrl Pts',(-0.338789834309108,-0.485140395282941,
-0.890216316528574));
#65102=CARTESIAN_POINT('Ctrl Pts',(-0.419522435166307,-0.428762108226878,
-0.894852859843827));
#65103=CARTESIAN_POINT('Ctrl Pts',(-0.485877004947672,-0.351794762783792,
-0.89948940315908));
#65104=CARTESIAN_POINT('Ctrl Pts',(-0.529749340299652,-0.263638751739126,
-0.904125946474333));
#65105=CARTESIAN_POINT('Ctrl Pts',(-0.570315879336133,-0.182125327968706,
-0.908413124576058));
#65106=CARTESIAN_POINT('Ctrl Pts',(-0.591660626049118,-0.0910458529569786,
-0.912700302677783));
#65107=CARTESIAN_POINT('Ctrl Pts',(-0.591718276663101,7.52894403206403E-6,
-0.916987480779508));
#65108=CARTESIAN_POINT('Ctrl Pts',(-0.591707850850199,1.11928198428649E-5,
-0.942162519220489));
#65109=CARTESIAN_POINT('Ctrl Pts',(-0.591632992221397,-0.0865559552489433,
-0.938086780070427));
#65110=CARTESIAN_POINT('Ctrl Pts',(-0.572406797455186,-0.173155256294739,
-0.934011040920365));
#65111=CARTESIAN_POINT('Ctrl Pts',(-0.535615671906496,-0.25150667084932,
-0.929935301770302));
#65112=CARTESIAN_POINT('Ctrl Pts',(-0.493762245830199,-0.340638902824493,
-0.92529875845505));
#65113=CARTESIAN_POINT('Ctrl Pts',(-0.429177621838593,-0.419097347209124,
-0.920662215139797));
#65114=CARTESIAN_POINT('Ctrl Pts',(-0.349749831277004,-0.477299496118803,
-0.916025671824544));
#65115=CARTESIAN_POINT('Ctrl Pts',(-0.270322040715412,-0.535501645028483,
-0.911389128509291));
#65116=CARTESIAN_POINT('Ctrl Pts',(-0.176051083583834,-0.573447498463211,
-0.906752585194038));
#65117=CARTESIAN_POINT('Ctrl Pts',(-0.0784507261450266,-0.58650254649138,
-0.902116041878785));
#65118=CARTESIAN_POINT('Ctrl Pts',(0.0191496312937804,-0.599557594519549,
-0.897479498563532));
#65119=CARTESIAN_POINT('Ctrl Pts',(0.120079389039817,-0.587721837141161,
-0.892842955248279));
#65120=CARTESIAN_POINT('Ctrl Pts',(0.212011509424179,-0.552440832438404,
-0.888206411933026));
#65121=CARTESIAN_POINT('Ctrl Pts',(0.303943629808538,-0.517159827735649,
-0.883569868617773));
#65122=CARTESIAN_POINT('Ctrl Pts',(0.386878112831224,-0.458433575708527,
-0.87893332530252));
#65123=CARTESIAN_POINT('Ctrl Pts',(0.450685770440045,-0.383434596504304,
-0.874296781987267));
#65124=CARTESIAN_POINT('Ctrl Pts',(0.514493428048868,-0.308435617300078,
-0.869660238672014));
#65125=CARTESIAN_POINT('Ctrl Pts',(0.559174260243827,-0.217163910918747,
-0.865023695356761));
#65126=CARTESIAN_POINT('Ctrl Pts',(0.57927118168314,-0.1207669306763,-0.860387152041508));
#65127=CARTESIAN_POINT('Ctrl Pts',(0.599368103122454,-0.0243699504338505,
-0.855750608726255));
#65128=CARTESIAN_POINT('Ctrl Pts',(0.594881113806123,0.07715230366971,-0.851114065411002));
#65129=CARTESIAN_POINT('Ctrl Pts',(0.566358231361036,0.171400429530254,
-0.846477522095749));
#65130=CARTESIAN_POINT('Ctrl Pts',(0.537835348915949,0.265648555390792,
-0.841840978780496));
#65131=CARTESIAN_POINT('Ctrl Pts',(0.485276573342108,0.352622553008308,
-0.837204435465243));
#65132=CARTESIAN_POINT('Ctrl Pts',(0.415101161168002,0.421699868947729,
-0.83256789214999));
#65133=CARTESIAN_POINT('Ctrl Pts',(0.344925748993893,0.490777184887153,
-0.827931348834737));
#65134=CARTESIAN_POINT('Ctrl Pts',(0.257133700219515,0.541957819148481,
-0.823294805519484));
#65135=CARTESIAN_POINT('Ctrl Pts',(0.162447480809717,0.568990834242638,
-0.818658262204231));
#65136=CARTESIAN_POINT('Ctrl Pts',(0.0677612613999249,0.596023849336792,
-0.814021718888978));
#65137=CARTESIAN_POINT('Ctrl Pts',(-0.0338191286452886,0.598909245263779,
-0.809385175573725));
#65138=CARTESIAN_POINT('Ctrl Pts',(-0.129887186799085,0.57729461471503,
-0.804748632258472));
#65139=CARTESIAN_POINT('Ctrl Pts',(-0.225955244952882,0.555679984166281,
-0.80011208894322));
#65140=CARTESIAN_POINT('Ctrl Pts',(-0.316510971215263,0.509565327141797,
-0.795475545627967));
#65141=CARTESIAN_POINT('Ctrl Pts',(-0.390494358372299,0.444582848919031,
-0.790839002312714));
#65142=CARTESIAN_POINT('Ctrl Pts',(-0.464477745529339,0.379600370696262,
-0.78620245899746));
#65143=CARTESIAN_POINT('Ctrl Pts',(-0.521888793581034,0.295750071275207,
-0.781565915682207));
#65144=CARTESIAN_POINT('Ctrl Pts',(-0.555715614579277,0.203272991777885,
-0.776929372366954));
#65145=CARTESIAN_POINT('Ctrl Pts',(-0.579467619081906,0.13833883764249,
-0.773673754651466));
#65146=CARTESIAN_POINT('Ctrl Pts',(-0.59159176314519,0.0691513749487757,
-0.770418136935978));
#65147=CARTESIAN_POINT('Ctrl Pts',(-0.591654968200026,-1.45109499015529E-5,
-0.76716251922049));
#65148=CARTESIAN_POINT('Origin',(0.,0.,-1.97));
#65149=CARTESIAN_POINT('',(-0.59167279304111,1.54653535696381E-5,-0.566987480779507));
#65150=CARTESIAN_POINT('',(-0.591659059186468,1.49283821118909E-5,-0.59216251922049));
#65151=CARTESIAN_POINT('',(-0.591675,-7.2459289488551E-17,-1.97));
#65152=CARTESIAN_POINT('Ctrl Pts',(-0.59167279304111,1.54653535696381E-5,
-0.566987480779507));
#65153=CARTESIAN_POINT('Ctrl Pts',(-0.591696802954663,0.0234350648064659,
-0.568089929778377));
#65154=CARTESIAN_POINT('Ctrl Pts',(-0.590332828147301,0.0468518849396706,
-0.569192378777246));
#65155=CARTESIAN_POINT('Ctrl Pts',(-0.587559081074247,0.0701005079415737,
-0.570294827776116));
#65156=CARTESIAN_POINT('Ctrl Pts',(-0.575893599530016,0.167876684144606,
-0.574931371091369));
#65157=CARTESIAN_POINT('Ctrl Pts',(-0.539292473904837,0.262677838137568,
-0.579567914406623));
#65158=CARTESIAN_POINT('Ctrl Pts',(-0.48222597604303,0.342925448160133,
-0.584204457721876));
#65159=CARTESIAN_POINT('Ctrl Pts',(-0.425159478181225,0.423173058182693,
-0.588841001037129));
#65160=CARTESIAN_POINT('Ctrl Pts',(-0.347627608082795,0.488867124234858,
-0.593477544352382));
#65161=CARTESIAN_POINT('Ctrl Pts',(-0.259099706649643,0.531984113466323,
-0.598114087667635));
#65162=CARTESIAN_POINT('Ctrl Pts',(-0.170571805216496,0.575101102697786,
-0.602750630982888));
#65163=CARTESIAN_POINT('Ctrl Pts',(-0.0710478724486285,0.595641015108553,
-0.607387174298142));
#65164=CARTESIAN_POINT('Ctrl Pts',(0.0273167541639602,0.591095212219171,
-0.612023717613394));
#65165=CARTESIAN_POINT('Ctrl Pts',(0.125681380776549,0.586549409329789,
-0.616660260928647));
#65166=CARTESIAN_POINT('Ctrl Pts',(0.222886701233859,0.556917891140258,
-0.6212968042439));
#65167=CARTESIAN_POINT('Ctrl Pts',(0.307060561340197,0.505819697753977,
-0.625933347559153));
#65168=CARTESIAN_POINT('Ctrl Pts',(0.391234421446539,0.454721504367692,
-0.630569890874406));
#65169=CARTESIAN_POINT('Ctrl Pts',(0.462376821201907,0.382156635784654,
-0.635206434189659));
#65170=CARTESIAN_POINT('Ctrl Pts',(0.511798796506661,0.29698778907695,-0.639842977504912));
#65171=CARTESIAN_POINT('Ctrl Pts',(0.561220771811414,0.211818942369245,
-0.644479520820166));
#65172=CARTESIAN_POINT('Ctrl Pts',(0.588922322665554,0.114046117536873,
-0.649116064135418));
#65173=CARTESIAN_POINT('Ctrl Pts',(0.591520125176384,0.0156107808195186,
-0.653752607450672));
#65174=CARTESIAN_POINT('Ctrl Pts',(0.594117927687215,-0.0828245558978302,
-0.658389150765925));
#65175=CARTESIAN_POINT('Ctrl Pts',(0.57161198185474,-0.181922404500161,
-0.663025694081178));
#65176=CARTESIAN_POINT('Ctrl Pts',(0.52675104729403,-0.269579467209807,
-0.667662237396431));
#65177=CARTESIAN_POINT('Ctrl Pts',(0.48189011273332,-0.357236529919453,
-0.672298780711684));
#65178=CARTESIAN_POINT('Ctrl Pts',(0.414674189444375,-0.433452806736414,
-0.676935324026936));
#65179=CARTESIAN_POINT('Ctrl Pts',(0.333312682035277,-0.488919636505767,
-0.681571867342189));
#65180=CARTESIAN_POINT('Ctrl Pts',(0.251951174626179,-0.54438646627512,
-0.686208410657442));
#65181=CARTESIAN_POINT('Ctrl Pts',(0.156444083096928,-0.579103848996866,
-0.690844953972695));
#65182=CARTESIAN_POINT('Ctrl Pts',(0.0584561487608926,-0.588831583424772,
-0.695481497287948));
#65183=CARTESIAN_POINT('Ctrl Pts',(-0.039531785575143,-0.598559317852679,
-0.700118040603201));
#65184=CARTESIAN_POINT('Ctrl Pts',(-0.140000562717963,-0.583297403986747,
-0.704754583918453));
#65185=CARTESIAN_POINT('Ctrl Pts',(-0.230679446781087,-0.544909852910784,
-0.709391127233706));
#65186=CARTESIAN_POINT('Ctrl Pts',(-0.321358330844217,-0.50652230183482,
-0.71402767054896));
#65187=CARTESIAN_POINT('Ctrl Pts',(-0.402247321827649,-0.445009113548823,
-0.718664213864213));
#65188=CARTESIAN_POINT('Ctrl Pts',(-0.463467057478662,-0.367883190154907,
-0.723300757179466));
#65189=CARTESIAN_POINT('Ctrl Pts',(-0.524686793129676,-0.290757266760991,
-0.727937300494719));
#65190=CARTESIAN_POINT('Ctrl Pts',(-0.566237273448271,-0.198018608259155,
-0.732573843809972));
#65191=CARTESIAN_POINT('Ctrl Pts',(-0.583043738051716,-0.100993833896741,
-0.737210387125225));
#65192=CARTESIAN_POINT('Ctrl Pts',(-0.588815714425,-0.0676718522392664,
-0.738802751676653));
#65193=CARTESIAN_POINT('Ctrl Pts',(-0.591669144803714,-0.0338443250623759,
-0.74039511622808));
#65194=CARTESIAN_POINT('Ctrl Pts',(-0.591643300061755,-1.24859503531638E-5,
-0.741987480779508));
#65195=CARTESIAN_POINT('Ctrl Pts',(-0.591654968200026,-1.45109499015529E-5,
-0.76716251922049));
#65196=CARTESIAN_POINT('Ctrl Pts',(-0.591681777698525,-0.0293523972789734,
-0.765781593620725));
#65197=CARTESIAN_POINT('Ctrl Pts',(-0.589538611466783,-0.0586864015619183,
-0.76440066802096));
#65198=CARTESIAN_POINT('Ctrl Pts',(-0.585192419058669,-0.0876902853788226,
-0.763019742421195));
#65199=CARTESIAN_POINT('Ctrl Pts',(-0.570599808595024,-0.185072623464623,
-0.758383199105942));
#65200=CARTESIAN_POINT('Ctrl Pts',(-0.531171993722942,-0.278733440062635,
-0.753746655790689));
#65201=CARTESIAN_POINT('Ctrl Pts',(-0.471724483465576,-0.357233488313583,
-0.749110112475436));
#65202=CARTESIAN_POINT('Ctrl Pts',(-0.412276973208212,-0.435733536564528,
-0.744473569160183));
#65203=CARTESIAN_POINT('Ctrl Pts',(-0.332809767565565,-0.49907281646841,
-0.73983702584493));
#65204=CARTESIAN_POINT('Ctrl Pts',(-0.243028579295454,-0.539515396554342,
-0.735200482529677));
#65205=CARTESIAN_POINT('Ctrl Pts',(-0.15324739102534,-0.579957976640276,
-0.730563939214424));
#65206=CARTESIAN_POINT('Ctrl Pts',(-0.0531522201277623,-0.59750385690826,
-0.725927395899172));
#65207=CARTESIAN_POINT('Ctrl Pts',(0.0450318278418444,-0.590010074451935,
-0.721290852583919));
#65208=CARTESIAN_POINT('Ctrl Pts',(0.143215875811451,-0.582516291995611,
-0.716654309268665));
#65209=CARTESIAN_POINT('Ctrl Pts',(0.239488800853087,-0.549982846814977,
-0.712017765953412));
#65210=CARTESIAN_POINT('Ctrl Pts',(0.322092326716154,-0.496383205340521,
-0.707381222638159));
#65211=CARTESIAN_POINT('Ctrl Pts',(0.404695852579222,-0.442783563866064,
-0.702744679322906));
#65212=CARTESIAN_POINT('Ctrl Pts',(0.473629979263721,-0.368117726097785,
-0.698108136007653));
#65213=CARTESIAN_POINT('Ctrl Pts',(0.520475449701276,-0.281504990598408,
-0.6934715926924));
#65214=CARTESIAN_POINT('Ctrl Pts',(0.567320920138831,-0.194892255099032,
-0.688835049377147));
#65215=CARTESIAN_POINT('Ctrl Pts',(0.592077734329442,-0.0963326218685597,
-0.684198506061894));
#65216=CARTESIAN_POINT('Ctrl Pts',(0.591722223259084,0.0021363461522315,
-0.679561962746641));
#65217=CARTESIAN_POINT('Ctrl Pts',(0.591366712188726,0.100605314173023,
-0.674925419431388));
#65218=CARTESIAN_POINT('Ctrl Pts',(0.565898875857402,0.198983616984125,
-0.670288876116135));
#65219=CARTESIAN_POINT('Ctrl Pts',(0.518429223839417,0.285255838402679,
-0.665652332800882));
#65220=CARTESIAN_POINT('Ctrl Pts',(0.470959571821432,0.371528059821234,
-0.661015789485629));
#65221=CARTESIAN_POINT('Ctrl Pts',(0.40148810411678,0.445694199847239,-0.656379246170376));
#65222=CARTESIAN_POINT('Ctrl Pts',(0.318499705841953,0.498695990411137,
-0.651742702855123));
#65223=CARTESIAN_POINT('Ctrl Pts',(0.235511307567128,0.551697780975035,
-0.64710615953987));
#65224=CARTESIAN_POINT('Ctrl Pts',(0.139005978722123,0.583535222076834,
-0.642469616224617));
#65225=CARTESIAN_POINT('Ctrl Pts',(0.0407703801539367,0.590319853618069,
-0.637833072909364));
#65226=CARTESIAN_POINT('Ctrl Pts',(-0.0574652184142526,0.597104485159305,
-0.633196529594111));
#65227=CARTESIAN_POINT('Ctrl Pts',(-0.157431086705624,0.578836307139974,
-0.628559986278858));
#65228=CARTESIAN_POINT('Ctrl Pts',(-0.246917911515115,0.537746500171382,
-0.623923442963605));
#65229=CARTESIAN_POINT('Ctrl Pts',(-0.336404736324606,0.496656693202789,
-0.619286899648352));
#65230=CARTESIAN_POINT('Ctrl Pts',(-0.415412517652216,0.432745257284934,
-0.614650356333099));
#65231=CARTESIAN_POINT('Ctrl Pts',(-0.474291654445574,0.353818004059765,
-0.610013813017846));
#65232=CARTESIAN_POINT('Ctrl Pts',(-0.533170791238929,0.274890750834599,
-0.605377269702594));
#65233=CARTESIAN_POINT('Ctrl Pts',(-0.571921283498033,0.180947680302121,
-0.60074072638734));
#65234=CARTESIAN_POINT('Ctrl Pts',(-0.585810346874303,0.0834625123547343,
-0.596104183072088));
#65235=CARTESIAN_POINT('Ctrl Pts',(-0.589746182641055,0.0558374954374221,
-0.594790295121555));
#65236=CARTESIAN_POINT('Ctrl Pts',(-0.591685588338141,0.0279280399296278,
-0.593476407171022));
#65237=CARTESIAN_POINT('Ctrl Pts',(-0.591659059186468,1.49283821118909E-5,
-0.59216251922049));
#65238=CARTESIAN_POINT('Origin',(0.,0.,-1.97));
#65239=CARTESIAN_POINT('',(-0.591690521605803,-1.43942328892088E-5,-0.391987480779507));
#65240=CARTESIAN_POINT('',(-0.591703958414771,-1.21461586050568E-5,-0.417162519220489));
#65241=CARTESIAN_POINT('',(-0.591675,-7.2459289488551E-17,-1.97));
#65242=CARTESIAN_POINT('Ctrl Pts',(-0.591690521605803,-1.43942328892088E-5,
-0.391987480779507));
#65243=CARTESIAN_POINT('Ctrl Pts',(-0.591608432467092,0.0806448416080524,
-0.395784743328675));
#65244=CARTESIAN_POINT('Ctrl Pts',(-0.5749902789137,0.161336859953991,-0.399582005877842));
#65245=CARTESIAN_POINT('Ctrl Pts',(-0.542917603258004,0.235330047038208,
-0.40337926842701));
#65246=CARTESIAN_POINT('Ctrl Pts',(-0.503756142076895,0.325677399244553,
-0.408015811742263));
#65247=CARTESIAN_POINT('Ctrl Pts',(-0.441553593529191,0.40603748977217,
-0.412652355057516));
#65248=CARTESIAN_POINT('Ctrl Pts',(-0.363907054607492,0.466595553529413,
-0.417288898372769));
#65249=CARTESIAN_POINT('Ctrl Pts',(-0.286260515685798,0.527153617286652,
-0.421925441688022));
#65250=CARTESIAN_POINT('Ctrl Pts',(-0.19316998639011,0.567909654273519,
-0.426561985003275));
#65251=CARTESIAN_POINT('Ctrl Pts',(-0.0960050616434672,0.58388593329973,
-0.431198528318528));
#65252=CARTESIAN_POINT('Ctrl Pts',(0.00115986310317598,0.599862212325941,
-0.435835071633781));
#65253=CARTESIAN_POINT('Ctrl Pts',(0.102399183300774,0.591058733391496,
-0.440471614949033));
#65254=CARTESIAN_POINT('Ctrl Pts',(0.195348052926546,0.558550707800371,
-0.445108158264286));
#65255=CARTESIAN_POINT('Ctrl Pts',(0.288296922552323,0.526042682209244,
-0.449744701579539));
#65256=CARTESIAN_POINT('Ctrl Pts',(0.372955341606272,0.469830109961435,
-0.454381244894793));
#65257=CARTESIAN_POINT('Ctrl Pts',(0.438983569421467,0.396778503379994,
-0.459017788210046));
#65258=CARTESIAN_POINT('Ctrl Pts',(0.505011797236659,0.323726896798557,
-0.463654331525299));
#65259=CARTESIAN_POINT('Ctrl Pts',(0.552409833813099,0.233836255883489,
-0.468290874840552));
#65260=CARTESIAN_POINT('Ctrl Pts',(0.575388728544376,0.138085357770356,
-0.472927418155804));
#65261=CARTESIAN_POINT('Ctrl Pts',(0.598367623275652,0.0423344596572228,
-0.477563961471057));
#65262=CARTESIAN_POINT('Ctrl Pts',(0.596927376161766,-0.0592766956539763,
-0.48220050478631));
#65263=CARTESIAN_POINT('Ctrl Pts',(0.571243891522922,-0.154337848126212,
-0.486837048101563));
#65264=CARTESIAN_POINT('Ctrl Pts',(0.545560406884078,-0.249399000598452,
-0.491473591416816));
#65265=CARTESIAN_POINT('Ctrl Pts',(0.495633684720274,-0.337910150231728,
-0.496110134732069));
#65266=CARTESIAN_POINT('Ctrl Pts',(0.427561516193825,-0.409061003808133,
-0.500746678047323));
#65267=CARTESIAN_POINT('Ctrl Pts',(0.359489347667377,-0.480211857384537,
-0.505383221362576));
#65268=CARTESIAN_POINT('Ctrl Pts',(0.273271732778284,-0.534002414904071,
-0.510019764677829));
#65269=CARTESIAN_POINT('Ctrl Pts',(0.179438844294176,-0.563862976373561,
-0.514656307993082));
#65270=CARTESIAN_POINT('Ctrl Pts',(0.0856059558100742,-0.593723537843051,
-0.519292851308335));
#65271=CARTESIAN_POINT('Ctrl Pts',(-0.0158422062690415,-0.5996541032625,
-0.523929394623587));
#65272=CARTESIAN_POINT('Ctrl Pts',(-0.112515289055007,-0.580930344099315,
-0.52856593793884));
#65273=CARTESIAN_POINT('Ctrl Pts',(-0.209188371840973,-0.562206584936131,
-0.533202481254093));
#65274=CARTESIAN_POINT('Ctrl Pts',(-0.301086375333789,-0.518828501190311,
-0.537839024569346));
#65275=CARTESIAN_POINT('Ctrl Pts',(-0.376985353533273,-0.456094067257922,
-0.542475567884599));
#65276=CARTESIAN_POINT('Ctrl Pts',(-0.452884331732758,-0.393359633325533,
-0.547112111199852));
#65277=CARTESIAN_POINT('Ctrl Pts',(-0.51278428463891,-0.311268849206574,
-0.551748654515105));
#65278=CARTESIAN_POINT('Ctrl Pts',(-0.54936934236034,-0.219847857940548,
-0.556385197830358));
#65279=CARTESIAN_POINT('Ctrl Pts',(-0.5772554281287,-0.150164392551905,
-0.559919292146741));
#65280=CARTESIAN_POINT('Ctrl Pts',(-0.591595825037046,-0.0750601829560788,
-0.563453386463124));
#65281=CARTESIAN_POINT('Ctrl Pts',(-0.59167279304111,1.54653535696381E-5,
-0.566987480779507));
#65282=CARTESIAN_POINT('Ctrl Pts',(-0.591659059186468,1.49283821118909E-5,
-0.59216251922049));
#65283=CARTESIAN_POINT('Ctrl Pts',(-0.591591970339134,-0.0705737772923772,
-0.588839863855769));
#65284=CARTESIAN_POINT('Ctrl Pts',(-0.578952340615824,-0.141185864061551,
-0.585517208491049));
#65285=CARTESIAN_POINT('Ctrl Pts',(-0.554233358227024,-0.207280336988223,
-0.582194553126328));
#65286=CARTESIAN_POINT('Ctrl Pts',(-0.519739671710038,-0.299510753021489,
-0.577558009811075));
#65287=CARTESIAN_POINT('Ctrl Pts',(-0.461724664182631,-0.382944319725719,
-0.572921466495822));
#65288=CARTESIAN_POINT('Ctrl Pts',(-0.387273988074007,-0.447390893553736,
-0.568284923180568));
#65289=CARTESIAN_POINT('Ctrl Pts',(-0.312823311965386,-0.511837467381749,
-0.563648379865316));
#65290=CARTESIAN_POINT('Ctrl Pts',(-0.221936967275551,-0.55729704833355,
-0.559011836550063));
#65291=CARTESIAN_POINT('Ctrl Pts',(-0.12571534124014,-0.578217438729092,
-0.55437529323481));
#65292=CARTESIAN_POINT('Ctrl Pts',(-0.0294937152047297,-0.599137829124633,
-0.549738749919557));
#65293=CARTESIAN_POINT('Ctrl Pts',(0.072063192176254,-0.595519028963915,
-0.545102206604304));
#65294=CARTESIAN_POINT('Ctrl Pts',(0.166551746426916,-0.567803019748663,
-0.540465663289051));
#65295=CARTESIAN_POINT('Ctrl Pts',(0.261040300677573,-0.540087010533411,
-0.535829119973799));
#65296=CARTESIAN_POINT('Ctrl Pts',(0.348460501797907,-0.488273792263629,
-0.531192576658546));
#65297=CARTESIAN_POINT('Ctrl Pts',(0.418135299368905,-0.418691562961605,
-0.526556033343293));
#65298=CARTESIAN_POINT('Ctrl Pts',(0.487810096939912,-0.349109333659573,
-0.52191949002804));
#65299=CARTESIAN_POINT('Ctrl Pts',(0.539739490961578,-0.261758093325295,
-0.517282946712787));
#65300=CARTESIAN_POINT('Ctrl Pts',(0.567581094307214,-0.167306469864681,
-0.512646403397534));
#65301=CARTESIAN_POINT('Ctrl Pts',(0.595422697652849,-0.0728548464040694,
-0.508009860082281));
#65302=CARTESIAN_POINT('Ctrl Pts',(0.599176510322455,0.0286971601828845,
-0.503373316767028));
#65303=CARTESIAN_POINT('Ctrl Pts',(0.578384061086002,0.12494651397786,-0.498736773451775));
#65304=CARTESIAN_POINT('Ctrl Pts',(0.557591611849549,0.221195867772839,
-0.494100230136521));
#65305=CARTESIAN_POINT('Ctrl Pts',(0.512252900707038,0.312142568775845,
-0.489463686821268));
#65306=CARTESIAN_POINT('Ctrl Pts',(0.447905362926267,0.386678858143867,
-0.484827143506015));
#65307=CARTESIAN_POINT('Ctrl Pts',(0.3835578251455,0.461215147511885,-0.480190600190762));
#65308=CARTESIAN_POINT('Ctrl Pts',(0.300201460726476,0.519341025244921,
-0.475554056875509));
#65309=CARTESIAN_POINT('Ctrl Pts',(0.208016984129261,0.553957297801303,
-0.470917513560257));
#65310=CARTESIAN_POINT('Ctrl Pts',(0.115832507532046,0.588573570357686,
-0.466280970245004));
#65311=CARTESIAN_POINT('Ctrl Pts',(0.0148199187566409,0.599680237737416,
-0.461644426929751));
#65312=CARTESIAN_POINT('Ctrl Pts',(-0.0826836279752934,0.585920789133139,
-0.457007883614498));
#65313=CARTESIAN_POINT('Ctrl Pts',(-0.180187174707233,0.57216134052886,
-0.452371340299245));
#65314=CARTESIAN_POINT('Ctrl Pts',(-0.2741816793957,0.533535775940572,-0.447734796983991));
#65315=CARTESIAN_POINT('Ctrl Pts',(-0.353187140246972,0.474761621698427,
-0.443098253668738));
#65316=CARTESIAN_POINT('Ctrl Pts',(-0.432192601098239,0.415987467456285,
-0.438461710353485));
#65317=CARTESIAN_POINT('Ctrl Pts',(-0.496209018112312,0.337064723560289,
-0.433825167038233));
#65318=CARTESIAN_POINT('Ctrl Pts',(-0.537417757800081,0.247632605031507,
-0.42918862372298));
#65319=CARTESIAN_POINT('Ctrl Pts',(-0.573046355529395,0.170310634030099,
-0.42517992222215));
#65320=CARTESIAN_POINT('Ctrl Pts',(-0.591625916202752,0.0851327680602624,
-0.421171220721319));
#65321=CARTESIAN_POINT('Ctrl Pts',(-0.591703958414771,-1.21461586050568E-5,
-0.417162519220489));
#65322=CARTESIAN_POINT('Origin',(0.,0.,-1.97));
#65323=CARTESIAN_POINT('',(-0.591632161208708,8.69568651094832E-6,-0.216987480779508));
#65324=CARTESIAN_POINT('',(-0.591626527824809,4.92094362445281E-6,-0.24216251922049));
#65325=CARTESIAN_POINT('',(-0.591675,-7.2459289488551E-17,-1.97));
#65326=CARTESIAN_POINT('Ctrl Pts',(-0.591632161208708,8.69568651094832E-6,
-0.216987480779508));
#65327=CARTESIAN_POINT('Ctrl Pts',(-0.591652619919161,0.0394340094205286,
-0.21884301356372));
#65328=CARTESIAN_POINT('Ctrl Pts',(-0.587770808522292,0.0788553485646517,
-0.220698546347931));
#65329=CARTESIAN_POINT('Ctrl Pts',(-0.57994709302668,0.117478187578517,
-0.222554079132143));
#65330=CARTESIAN_POINT('Ctrl Pts',(-0.560397454189643,0.213987647055358,
-0.227190622447396));
#65331=CARTESIAN_POINT('Ctrl Pts',(-0.516235218791925,0.305511403920623,
-0.23182716576265));
#65332=CARTESIAN_POINT('Ctrl Pts',(-0.452854134240634,0.380871222130496,
-0.236463709077903));
#65333=CARTESIAN_POINT('Ctrl Pts',(-0.389473049689346,0.456231040340365,
-0.241100252393156));
#65334=CARTESIAN_POINT('Ctrl Pts',(-0.306873115984487,0.515426919894844,
-0.245736795708408));
#65335=CARTESIAN_POINT('Ctrl Pts',(-0.215142660653105,0.551228982051028,
-0.250373339023661));
#65336=CARTESIAN_POINT('Ctrl Pts',(-0.123412205321724,0.587031044207212,
-0.255009882338914));
#65337=CARTESIAN_POINT('Ctrl Pts',(-0.0225512283638192,0.5994392889651,
-0.259646425654167));
#65338=CARTESIAN_POINT('Ctrl Pts',(0.0751216328736339,0.586938237969985,
-0.26428296896942));
#65339=CARTESIAN_POINT('Ctrl Pts',(0.172794494111093,0.57443718697487,-0.268919512284673));
#65340=CARTESIAN_POINT('Ctrl Pts',(0.2672792396281,0.537026840226748,-0.273556055599926));
#65341=CARTESIAN_POINT('Ctrl Pts',(0.347035992262199,0.47927630345588,-0.278192598915179));
#65342=CARTESIAN_POINT('Ctrl Pts',(0.426792744896299,0.421525766685012,
-0.282829142230433));
#65343=CARTESIAN_POINT('Ctrl Pts',(0.491821504647491,0.343435039891398,
-0.287465685545686));
#65344=CARTESIAN_POINT('Ctrl Pts',(0.534179995675711,0.254541719934951,
-0.292102228860939));
#65345=CARTESIAN_POINT('Ctrl Pts',(0.576538486703928,0.16564839997851,-0.296738772176192));
#65346=CARTESIAN_POINT('Ctrl Pts',(0.596226709009175,0.0659524868592369,
-0.301375315491445));
#65347=CARTESIAN_POINT('Ctrl Pts',(0.590840045156427,-0.0323696771933723,
-0.306011858806698));
#65348=CARTESIAN_POINT('Ctrl Pts',(0.585453381303679,-0.130691841245981,
-0.31064840212195));
#65349=CARTESIAN_POINT('Ctrl Pts',(0.554991831292937,-0.227640256231927,
-0.315284945437203));
#65350=CARTESIAN_POINT('Ctrl Pts',(0.503175810999434,-0.31137414503334,
-0.319921488752456));
#65351=CARTESIAN_POINT('Ctrl Pts',(0.451359790705932,-0.395108033834752,
-0.324558032067709));
#65352=CARTESIAN_POINT('Ctrl Pts',(0.37818930012967,-0.465627396451632,
-0.329194575382962));
#65353=CARTESIAN_POINT('Ctrl Pts',(0.292601003882376,-0.5143193633253,-0.333831118698215));
#65354=CARTESIAN_POINT('Ctrl Pts',(0.207012707635082,-0.563011330198967,
-0.338467662013468));
#65355=CARTESIAN_POINT('Ctrl Pts',(0.109006605716757,-0.589875901329423,
-0.343104205328721));
#65356=CARTESIAN_POINT('Ctrl Pts',(0.010552655617975,-0.591631977184183,
-0.347740748643974));
#65357=CARTESIAN_POINT('Ctrl Pts',(-0.0879012944808124,-0.593388053038943,
-0.352377291959227));
#65358=CARTESIAN_POINT('Ctrl Pts',(-0.186803092760056,-0.570035633618004,
-0.35701383527448));
#65359=CARTESIAN_POINT('Ctrl Pts',(-0.27407338601086,-0.524426862438141,
-0.361650378589733));
#65360=CARTESIAN_POINT('Ctrl Pts',(-0.361343679261664,-0.478818091258278,
-0.366286921904986));
#65361=CARTESIAN_POINT('Ctrl Pts',(-0.436982467484029,-0.41095296831949,
-0.370923465220239));
#65362=CARTESIAN_POINT('Ctrl Pts',(-0.491751620988836,-0.329120188109687,
-0.375560008535492));
#65363=CARTESIAN_POINT('Ctrl Pts',(-0.546520774493641,-0.24728740789989,
-0.380196551850745));
#65364=CARTESIAN_POINT('Ctrl Pts',(-0.580420293280891,-0.15148697041908,
-0.384833095165998));
#65365=CARTESIAN_POINT('Ctrl Pts',(-0.589309865767258,-0.0534194447361406,
-0.389469638481251));
#65366=CARTESIAN_POINT('Ctrl Pts',(-0.590919005744876,-0.0356678176107098,
-0.390308919247336));
#65367=CARTESIAN_POINT('Ctrl Pts',(-0.591708665159043,-0.0178419066505627,
-0.391148200013422));
#65368=CARTESIAN_POINT('Ctrl Pts',(-0.591690521605803,-1.43942328892088E-5,
-0.391987480779507));
#65369=CARTESIAN_POINT('Ctrl Pts',(-0.591703958414771,-1.21461586050568E-5,
-0.417162519220489));
#65370=CARTESIAN_POINT('Ctrl Pts',(-0.591716181366265,-0.0133475210726419,
-0.416534677406066));
#65371=CARTESIAN_POINT('Ctrl Pts',(-0.591274566785637,-0.0266820876886264,
-0.415906835591644));
#65372=CARTESIAN_POINT('Ctrl Pts',(-0.590373534468136,-0.0399855383001813,
-0.415278993777221));
#65373=CARTESIAN_POINT('Ctrl Pts',(-0.583719509086956,-0.138230069941527,
-0.410642450461968));
#65374=CARTESIAN_POINT('Ctrl Pts',(-0.552010395963128,-0.234777640062649,
-0.406005907146715));
#65375=CARTESIAN_POINT('Ctrl Pts',(-0.499118981880783,-0.31783642868596,
-0.401369363831461));
#65376=CARTESIAN_POINT('Ctrl Pts',(-0.44622756779844,-0.400895217309266,
-0.396732820516209));
#65377=CARTESIAN_POINT('Ctrl Pts',(-0.372153852757582,-0.470465224434766,
-0.392096277200956));
#65378=CARTESIAN_POINT('Ctrl Pts',(-0.285944816518956,-0.518049529851638,
-0.387459733885703));
#65379=CARTESIAN_POINT('Ctrl Pts',(-0.199735780280327,-0.565633835268512,
-0.38282319057045));
#65380=CARTESIAN_POINT('Ctrl Pts',(-0.101391422843937,-0.591232438976756,
-0.378186647255197));
#65381=CARTESIAN_POINT('Ctrl Pts',(-0.00292301448043288,-0.591718860152255,
-0.373550103939944));
#65382=CARTESIAN_POINT('Ctrl Pts',(0.0955453938830743,-0.592205281327754,
-0.368913560624691));
#65383=CARTESIAN_POINT('Ctrl Pts',(0.194137853173688,-0.567579519970502,
-0.364277017309438));
#65384=CARTESIAN_POINT('Ctrl Pts',(0.280812791245678,-0.520849238980347,
-0.359640473994185));
#65385=CARTESIAN_POINT('Ctrl Pts',(0.367487729317668,-0.474118957990191,
-0.355003930678932));
#65386=CARTESIAN_POINT('Ctrl Pts',(0.442245146171034,-0.40528415736713,
-0.350367387363679));
#65387=CARTESIAN_POINT('Ctrl Pts',(0.495954558248181,-0.322751963009284,
-0.345730844048426));
#65388=CARTESIAN_POINT('Ctrl Pts',(0.549663970325325,-0.240219768651443,
-0.341094300733173));
#65389=CARTESIAN_POINT('Ctrl Pts',(0.582325377626253,-0.143990180558819,
-0.33645775741792));
#65390=CARTESIAN_POINT('Ctrl Pts',(0.589949685089932,-0.045816182031098,
-0.331821214102667));
#65391=CARTESIAN_POINT('Ctrl Pts',(0.597573992553612,0.0523578164966226,
-0.327184670787414));
#65392=CARTESIAN_POINT('Ctrl Pts',(0.580161200180044,0.15247622545944,-0.322548127472161));
#65393=CARTESIAN_POINT('Ctrl Pts',(0.53983801621007,0.242311101124062,-0.317911584156908));
#65394=CARTESIAN_POINT('Ctrl Pts',(0.499514832240094,0.332145976788689,
-0.313275040841655));
#65395=CARTESIAN_POINT('Ctrl Pts',(0.436281256673708,0.411697319155121,
-0.308638497526402));
#65396=CARTESIAN_POINT('Ctrl Pts',(0.357860310801024,0.471249139443922,
-0.304001954211149));
#65397=CARTESIAN_POINT('Ctrl Pts',(0.279439364928339,0.530800959732723,
-0.299365410895896));
#65398=CARTESIAN_POINT('Ctrl Pts',(0.185831048749355,0.570353257943894,
-0.294728867580642));
#65399=CARTESIAN_POINT('Ctrl Pts',(0.0884681969955049,0.58507532130052,
-0.290092324265389));
#65400=CARTESIAN_POINT('Ctrl Pts',(-0.00889465475833943,0.599797384657145,
-0.285455780950136));
#65401=CARTESIAN_POINT('Ctrl Pts',(-0.110012042087051,0.589689213159228,
-0.280819237634883));
#65402=CARTESIAN_POINT('Ctrl Pts',(-0.202534011219225,0.555985366507808,
-0.276182694319631));
#65403=CARTESIAN_POINT('Ctrl Pts',(-0.2950559803514,0.522281519856387,-0.271546151004378));
#65404=CARTESIAN_POINT('Ctrl Pts',(-0.37898253128704,0.464981998051463,
-0.266909607689125));
#65405=CARTESIAN_POINT('Ctrl Pts',(-0.444063309934188,0.391085067789069,
-0.262273064373872));
#65406=CARTESIAN_POINT('Ctrl Pts',(-0.509144088581336,0.317188137526676,
-0.257636521058619));
#65407=CARTESIAN_POINT('Ctrl Pts',(-0.555379094939994,0.226693798806812,
-0.252999977743366));
#65408=CARTESIAN_POINT('Ctrl Pts',(-0.577121424898413,0.13065456131464,
-0.248363434428113));
#65409=CARTESIAN_POINT('Ctrl Pts',(-0.586814158998031,0.0878402542039476,
-0.246296462692239));
#65410=CARTESIAN_POINT('Ctrl Pts',(-0.591639272973499,0.0439239662231613,
-0.244229490956364));
#65411=CARTESIAN_POINT('Ctrl Pts',(-0.591626527824809,4.92094362445281E-6,
-0.24216251922049));
#65412=CARTESIAN_POINT('Origin',(0.,0.,-1.97));
#65413=CARTESIAN_POINT('',(-0.591724346791278,-4.07989592221547E-6,-0.0419874807795086));
#65414=CARTESIAN_POINT('',(-0.591724986204225,2.85874560315911E-6,-0.0671625192204902));
#65415=CARTESIAN_POINT('',(-0.591675,-7.2459289488551E-17,-1.97));
#65416=CARTESIAN_POINT('Ctrl Pts',(-0.591724346791278,-4.07989592221547E-6,
-0.0419874807795086));
#65417=CARTESIAN_POINT('Ctrl Pts',(-0.591705292818391,0.0966334251737516,
-0.0465378271140176));
#65418=CARTESIAN_POINT('Ctrl Pts',(-0.567555912119278,0.193285312577123,
-0.0510881734485265));
#65419=CARTESIAN_POINT('Ctrl Pts',(-0.522064928224495,0.278548318802823,
-0.0556385197830354));
#65420=CARTESIAN_POINT('Ctrl Pts',(-0.475712210919869,0.365426457848211,
-0.0602750630982883));
#65421=CARTESIAN_POINT('Ctrl Pts',(-0.407201686475803,0.440480150981304,
-0.0649116064135412));
#65422=CARTESIAN_POINT('Ctrl Pts',(-0.324903331847967,0.494547117028557,
-0.069548149728794));
#65423=CARTESIAN_POINT('Ctrl Pts',(-0.242604977220127,0.548614083075814,
-0.0741846930440472));
#65424=CARTESIAN_POINT('Ctrl Pts',(-0.146518792408516,0.581694322037228,
-0.0788212363593003));
#65425=CARTESIAN_POINT('Ctrl Pts',(-0.0483789899463179,0.589745342092519,
-0.0834577796745535));
#65426=CARTESIAN_POINT('Ctrl Pts',(0.04976081251588,0.59779636214781,-0.0880943229898067));
#65427=CARTESIAN_POINT('Ctrl Pts',(0.149954232628665,0.580818163296978,
-0.0927308663050599));
#65428=CARTESIAN_POINT('Ctrl Pts',(0.239963522432172,0.540885522215563,
-0.0973674096203131));
#65429=CARTESIAN_POINT('Ctrl Pts',(0.329972812235668,0.500952881134153,
-0.102003952935566));
#65430=CARTESIAN_POINT('Ctrl Pts',(0.409797971729889,0.438065797822166,
-0.106640496250818));
#65431=CARTESIAN_POINT('Ctrl Pts',(0.469689898424806,0.359904387670641,
-0.111277039566071));
#65432=CARTESIAN_POINT('Ctrl Pts',(0.52958182511973,0.281742977519106,-0.115913582881324));
#65433=CARTESIAN_POINT('Ctrl Pts',(0.569540519015346,0.188307240528029,
-0.120550126196577));
#65434=CARTESIAN_POINT('Ctrl Pts',(0.58468546397641,0.091009233937934,-0.12518666951183));
#65435=CARTESIAN_POINT('Ctrl Pts',(0.599830408937475,-0.00628877265216127,
-0.129823212827083));
#65436=CARTESIAN_POINT('Ctrl Pts',(0.590161604963988,-0.107449048841275,
-0.134459756142337));
#65437=CARTESIAN_POINT('Ctrl Pts',(0.556860035796763,-0.200116556369054,
-0.13909629945759));
#65438=CARTESIAN_POINT('Ctrl Pts',(0.523558466629538,-0.292784063896833,
-0.143732842772843));
#65439=CARTESIAN_POINT('Ctrl Pts',(0.466624132268574,-0.376958802763277,
-0.148369386088096));
#65440=CARTESIAN_POINT('Ctrl Pts',(0.393010653253385,-0.442360027824988,
-0.153005929403349));
#65441=CARTESIAN_POINT('Ctrl Pts',(0.319397174238201,-0.507761252886696,
-0.157642472718602));
#65442=CARTESIAN_POINT('Ctrl Pts',(0.229104550568795,-0.554388964143672,
-0.162279016033855));
#65443=CARTESIAN_POINT('Ctrl Pts',(0.133160678021782,-0.576548334788175,
-0.166915559349108));
#65444=CARTESIAN_POINT('Ctrl Pts',(0.0372168054747698,-0.598707705432679,
-0.171552102664361));
#65445=CARTESIAN_POINT('Ctrl Pts',(-0.0643783159498496,-0.596398735464708,
-0.176188645979614));
#65446=CARTESIAN_POINT('Ctrl Pts',(-0.159216396050027,-0.569903409913743,
-0.180825189294867));
#65447=CARTESIAN_POINT('Ctrl Pts',(-0.254054476150203,-0.543408084362778,
-0.185461732610119));
#65448=CARTESIAN_POINT('Ctrl Pts',(-0.342135514925938,-0.492726403228817,
-0.190098275925372));
#65449=CARTESIAN_POINT('Ctrl Pts',(-0.412701744766264,-0.424048374991887,
-0.194734819240625));
#65450=CARTESIAN_POINT('Ctrl Pts',(-0.483267974606591,-0.355370346754957,
-0.199371362555878));
#65451=CARTESIAN_POINT('Ctrl Pts',(-0.536319395511509,-0.268695971415057,
-0.204007905871131));
#65452=CARTESIAN_POINT('Ctrl Pts',(-0.56537658482579,-0.174611202700902,
-0.208644449186384));
#65453=CARTESIAN_POINT('Ctrl Pts',(-0.582805161243839,-0.118178917954655,
-0.211425459717425));
#65454=CARTESIAN_POINT('Ctrl Pts',(-0.591601498377145,-0.0590806470709061,
-0.214206470248466));
#65455=CARTESIAN_POINT('Ctrl Pts',(-0.591632161208708,8.69568651094832E-6,
-0.216987480779508));
#65456=CARTESIAN_POINT('Ctrl Pts',(-0.591626527824809,4.92094362445281E-6,
-0.24216251922049));
#65457=CARTESIAN_POINT('Ctrl Pts',(-0.591610683596618,-0.0545933730654515,
-0.239592947641111));
#65458=CARTESIAN_POINT('Ctrl Pts',(-0.58411821465468,-0.109195928316423,
-0.237023376061733));
#65459=CARTESIAN_POINT('Ctrl Pts',(-0.569206298617938,-0.161690887462097,
-0.234453804482355));
#65460=CARTESIAN_POINT('Ctrl Pts',(-0.542299188820864,-0.256412962482184,
-0.229817261167102));
#65461=CARTESIAN_POINT('Ctrl Pts',(-0.491235315668536,-0.344272976257873,
-0.225180717851848));
#65462=CARTESIAN_POINT('Ctrl Pts',(-0.422251356090625,-0.414540161825823,
-0.220544174536595));
#65463=CARTESIAN_POINT('Ctrl Pts',(-0.353267396512714,-0.484807347393774,
-0.215907631221342));
#65464=CARTESIAN_POINT('Ctrl Pts',(-0.26636335050922,-0.537481704753986,
-0.211271087906089));
#65465=CARTESIAN_POINT('Ctrl Pts',(-0.172153227914291,-0.566129861023301,
-0.206634544590836));
#65466=CARTESIAN_POINT('Ctrl Pts',(-0.0779431053193665,-0.594778017292615,
-0.201998001275583));
#65467=CARTESIAN_POINT('Ctrl Pts',(0.0235730938669932,-0.599399972471034,
-0.19736145796033));
#65468=CARTESIAN_POINT('Ctrl Pts',(0.119996706913808,-0.5794312244984,-0.192724914645077));
#65469=CARTESIAN_POINT('Ctrl Pts',(0.216420319960622,-0.559462476525766,
-0.188088371329824));
#65470=CARTESIAN_POINT('Ctrl Pts',(0.307751346867891,-0.51490302540208,
-0.183451828014571));
#65471=CARTESIAN_POINT('Ctrl Pts',(0.382835089497417,-0.451195132399647,
-0.178815284699319));
#65472=CARTESIAN_POINT('Ctrl Pts',(0.457918832126947,-0.38748723939721,
-0.174178741384065));
#65473=CARTESIAN_POINT('Ctrl Pts',(0.516755290478732,-0.304630904516024,
-0.169542198068812));
#65474=CARTESIAN_POINT('Ctrl Pts',(0.552158483830049,-0.212745769664315,
-0.164905654753559));
#65475=CARTESIAN_POINT('Ctrl Pts',(0.587561677181366,-0.120860634812606,
-0.160269111438306));
#65476=CARTESIAN_POINT('Ctrl Pts',(0.599531605532214,-0.0199466999903742,
-0.155632568123053));
#65477=CARTESIAN_POINT('Ctrl Pts',(0.586606324919602,0.0776709266649116,
-0.150996024807799));
#65478=CARTESIAN_POINT('Ctrl Pts',(0.573681044306991,0.175288553320192,
-0.146359481492547));
#65479=CARTESIAN_POINT('Ctrl Pts',(0.535860554730924,0.269609871808526,
-0.141722938177294));
#65480=CARTESIAN_POINT('Ctrl Pts',(0.477764052747148,0.349114970849799,
-0.137086394862041));
#65481=CARTESIAN_POINT('Ctrl Pts',(0.419667550763372,0.428620069891072,
-0.132449851546788));
#65482=CARTESIAN_POINT('Ctrl Pts',(0.341295036371886,0.493308949485282,
-0.127813308231535));
#65483=CARTESIAN_POINT('Ctrl Pts',(0.252218526483655,0.535280833604227,
-0.123176764916282));
#65484=CARTESIAN_POINT('Ctrl Pts',(0.163142016595425,0.577252717723171,
-0.118540221601029));
#65485=CARTESIAN_POINT('Ctrl Pts',(0.0633615112104499,0.596507606366848,
-0.113903678285777));
#65486=CARTESIAN_POINT('Ctrl Pts',(-0.0349363236836362,0.590693829557053,
-0.109267134970524));
#65487=CARTESIAN_POINT('Ctrl Pts',(-0.133234158577722,0.584880052747258,
-0.104630591655271));
#65488=CARTESIAN_POINT('Ctrl Pts',(-0.23004932298092,0.553997610483989,
-0.0999940483400178));
#65489=CARTESIAN_POINT('Ctrl Pts',(-0.313557298800687,0.501818280580585,
-0.0953575050247649));
#65490=CARTESIAN_POINT('Ctrl Pts',(-0.397065274620459,0.449638950677177,
-0.0907209617095118));
#65491=CARTESIAN_POINT('Ctrl Pts',(-0.4672660618568,0.37616273313363,-0.0860844183942587));
#65492=CARTESIAN_POINT('Ctrl Pts',(-0.51558573043494,0.290363717785175,
-0.0814478750790056));
#65493=CARTESIAN_POINT('Ctrl Pts',(-0.563905399013081,0.20456470243672,
-0.0768113317637524));
#65494=CARTESIAN_POINT('Ctrl Pts',(-0.59034394893302,0.106442889283356,
-0.0721747884484991));
#65495=CARTESIAN_POINT('Ctrl Pts',(-0.591672253399873,0.00798220150416167,
-0.067538245133246));
#65496=CARTESIAN_POINT('Ctrl Pts',(-0.591708133463553,0.00532258856473375,
-0.0674130031623274));
#65497=CARTESIAN_POINT('Ctrl Pts',(-0.591725691981876,0.00266272836739514,
-0.0672877611914088));
#65498=CARTESIAN_POINT('Ctrl Pts',(-0.591724986204225,2.85874560315911E-6,
-0.0671625192204902));
#65499=CARTESIAN_POINT('Origin',(0.,0.,-4.27183905640093));
#65500=CARTESIAN_POINT('',(-0.491789390605438,7.22821825122446E-6,-0.159339056400925));
#65501=CARTESIAN_POINT('',(-0.491866550623049,2.37630884976706E-6,-0.124810943599073));
#65502=CARTESIAN_POINT('',(-0.491825,-1.07154090996976E-14,-4.27183905640093));
#65503=CARTESIAN_POINT('',(-0.416126897194384,0.262207742448202,-3.33066907387547E-16));
#65504=CARTESIAN_POINT('Ctrl Pts',(-0.491789390605438,7.22821825123801E-6,
-0.159339056400925));
#65505=CARTESIAN_POINT('Ctrl Pts',(-0.491763902377726,-0.0491103042136956,
-0.156558045869883));
#65506=CARTESIAN_POINT('Ctrl Pts',(-0.472261535530513,-0.180137132920269,
-0.149140492023589));
#65507=CARTESIAN_POINT('Ctrl Pts',(-0.357613988294798,-0.367446056440282,
-0.137086394862041));
#65508=CARTESIAN_POINT('Ctrl Pts',(-0.137964061075247,-0.493832254050675,
-0.123176764916282));
#65509=CARTESIAN_POINT('Ctrl Pts',(0.115386277850666,-0.499590191201122,
-0.109267134970524));
#65510=CARTESIAN_POINT('Ctrl Pts',(0.340551290583365,-0.383313481407925,
-0.0953575050247649));
#65511=CARTESIAN_POINT('Ctrl Pts',(0.482529888616476,-0.173404793650348,
-0.0814478750790055));
#65512=CARTESIAN_POINT('Ctrl Pts',(0.506641231064238,0.0788611606491063,
-0.0675382451332463));
#65513=CARTESIAN_POINT('Ctrl Pts',(0.406995219528124,0.311864235034375,
-0.0536286151874873));
#65514=CARTESIAN_POINT('Ctrl Pts',(0.207933188506461,0.468687354567501,
-0.0397189852417286));
#65515=CARTESIAN_POINT('Ctrl Pts',(-0.0419216921981646,0.511026320975463,
-0.0258093552959692));
#65516=CARTESIAN_POINT('Ctrl Pts',(-0.269993129330808,0.432506628936349,
-0.0125696935487264));
#65517=CARTESIAN_POINT('Ctrl Pts',(-0.3787346762928,0.321423241660421,-0.00396657511673683));
#65518=CARTESIAN_POINT('Ctrl Pts',(-0.416126897194384,0.262207742448202,
-3.5377516888202E-16));
#65519=CARTESIAN_POINT('',(0.112693552167563,0.478740006605732,0.));
#65520=CARTESIAN_POINT('Origin',(0.,0.,0.));
#65521=CARTESIAN_POINT('Ctrl Pts',(-0.491866550623049,2.37630884974928E-6,
-0.124810943599073));
#65522=CARTESIAN_POINT('Ctrl Pts',(-0.491845418300655,-0.0796391684329172,
-0.120299642254739));
#65523=CARTESIAN_POINT('Ctrl Pts',(-0.451858604081596,-0.241153864017004,
-0.111151797595152));
#65524=CARTESIAN_POINT('Ctrl Pts',(-0.283335167309922,-0.427346729913706,
-0.0973674096203128));
#65525=CARTESIAN_POINT('Ctrl Pts',(-0.0440696378965106,-0.510845571762323,
-0.0834577796745537));
#65526=CARTESIAN_POINT('Ctrl Pts',(0.205959307621291,-0.469556250960448,
-0.0695481497287949));
#65527=CARTESIAN_POINT('Ctrl Pts',(0.405681497053104,-0.313576606935647,
-0.0556385197830361));
#65528=CARTESIAN_POINT('Ctrl Pts',(0.506302444914719,-0.0809840427845483,
-0.0417288898372769));
#65529=CARTESIAN_POINT('Ctrl Pts',(0.48325998950616,0.171359585523517,-0.0278192598915182));
#65530=CARTESIAN_POINT('Ctrl Pts',(0.342150143078732,0.381908292889331,
-0.0139096299457593));
#65531=CARTESIAN_POINT('Ctrl Pts',(0.192389430706698,0.459979903999379,
-0.00463654331525315));
#65532=CARTESIAN_POINT('Ctrl Pts',(0.112693552167563,0.478740006605732,
0.));
#65533=CARTESIAN_POINT('Origin',(0.,0.,-4.27183905640093));
#65534=CARTESIAN_POINT('',(-0.491837902207756,-1.19650882245787E-5,-0.334339056400925));
#65535=CARTESIAN_POINT('',(-0.49178470790119,4.0904940728087E-6,-0.299810943599072));
#65536=CARTESIAN_POINT('',(-0.491825,-1.07154090996976E-14,-4.27183905640093));
#65537=CARTESIAN_POINT('Ctrl Pts',(-0.491837902207756,-1.19650882245553E-5,
-0.334339056400925));
#65538=CARTESIAN_POINT('Ctrl Pts',(-0.491852983887855,-0.0148309388404159,
-0.333499775634839));
#65539=CARTESIAN_POINT('Ctrl Pts',(-0.4875703651248,-0.111507530516403,
-0.3280239515535));
#65540=CARTESIAN_POINT('Ctrl Pts',(-0.426112222229761,-0.285188962782551,
-0.317911584156906));
#65541=CARTESIAN_POINT('Ctrl Pts',(-0.237489851752064,-0.454425946376765,
-0.304001954211149));
#65542=CARTESIAN_POINT('Ctrl Pts',(0.00914407872677023,-0.512660468783674,
-0.290092324265389));
#65543=CARTESIAN_POINT('Ctrl Pts',(0.253544388403441,-0.445667604307889,
-0.27618269431963));
#65544=CARTESIAN_POINT('Ctrl Pts',(0.436011502246361,-0.269811675703265,
-0.262273064373872));
#65545=CARTESIAN_POINT('Ctrl Pts',(0.511974244464808,-0.0280489468379449,
-0.248363434428113));
#65546=CARTESIAN_POINT('Ctrl Pts',(0.462877223624254,0.220565288020147,
-0.234453804482355));
#65547=CARTESIAN_POINT('Ctrl Pts',(0.300713351069406,0.41530212009148,-0.220544174536595));
#65548=CARTESIAN_POINT('Ctrl Pts',(0.0650943374357338,0.508593253514698,
-0.206634544590836));
#65549=CARTESIAN_POINT('Ctrl Pts',(-0.186425246756546,0.477650497890165,
-0.192724914645077));
#65550=CARTESIAN_POINT('Ctrl Pts',(-0.392406802818875,0.330032227073166,
-0.178815284699318));
#65551=CARTESIAN_POINT('Ctrl Pts',(-0.480516842828346,0.147429109124288,
-0.167686665284601));
#65552=CARTESIAN_POINT('Ctrl Pts',(-0.491806396741015,0.0327791975041391,
-0.161194589185136));
#65553=CARTESIAN_POINT('Ctrl Pts',(-0.491789390605438,7.22821825123801E-6,
-0.159339056400925));
#65554=CARTESIAN_POINT('Ctrl Pts',(-0.49178470790119,4.0904940727983E-6,
-0.299810943599072));
#65555=CARTESIAN_POINT('Ctrl Pts',(-0.491771537516212,-0.0453802944317873,
-0.297241372019695));
#65556=CARTESIAN_POINT('Ctrl Pts',(-0.474305564106061,-0.172666344668371,
-0.290035257125064));
#65557=CARTESIAN_POINT('Ctrl Pts',(-0.365888908126138,-0.359207010306768,
-0.278192598915179));
#65558=CARTESIAN_POINT('Ctrl Pts',(-0.149174077725999,-0.490562395317217,
-0.26428296896942));
#65559=CARTESIAN_POINT('Ctrl Pts',(0.103979450806552,-0.502088282530429,
-0.250373339023661));
#65560=CARTESIAN_POINT('Ctrl Pts',(0.331733956110991,-0.390969245649164,
-0.236463709077902));
#65561=CARTESIAN_POINT('Ctrl Pts',(0.478455929130976,-0.184348295450463,
-0.222554079132143));
#65562=CARTESIAN_POINT('Ctrl Pts',(0.508305643980286,0.067303351115353,
-0.208644449186384));
#65563=CARTESIAN_POINT('Ctrl Pts',(0.413991726952782,0.302514822609971,
-0.194734819240625));
#65564=CARTESIAN_POINT('Ctrl Pts',(0.218552193979818,0.463831127370637,
-0.180825189294866));
#65565=CARTESIAN_POINT('Ctrl Pts',(-0.0302729907633189,0.511847533035115,
-0.166915559349108));
#65566=CARTESIAN_POINT('Ctrl Pts',(-0.271703429260484,0.434835201098837,
-0.153005929403349));
#65567=CARTESIAN_POINT('Ctrl Pts',(-0.446764918333941,0.251605688139759,
-0.13909629945759));
#65568=CARTESIAN_POINT('Ctrl Pts',(-0.491312211182185,0.0862766077408699,
-0.129697970856164));
#65569=CARTESIAN_POINT('Ctrl Pts',(-0.491867137294944,0.00221337115693925,
-0.124936185569992));
#65570=CARTESIAN_POINT('Ctrl Pts',(-0.491866550623049,2.37630884974928E-6,
-0.124810943599073));
#65571=CARTESIAN_POINT('Origin',(0.,0.,-4.27183905640093));
#65572=CARTESIAN_POINT('',(-0.49182316548349,1.28554485876743E-5,-0.509339056400925));
#65573=CARTESIAN_POINT('',(-0.49184907144521,-1.00963949215827E-5,-0.474810943599073));
#65574=CARTESIAN_POINT('',(-0.491825,-1.07154090996976E-14,-4.27183905640093));
#65575=CARTESIAN_POINT('Ctrl Pts',(-0.49182316548349,1.28554485876817E-5,
-0.509339056400925));
#65576=CARTESIAN_POINT('Ctrl Pts',(-0.491759186460215,-0.0623931626016951,
-0.505804962084542));
#65577=CARTESIAN_POINT('Ctrl Pts',(-0.46420000164389,-0.206727437724254,
-0.497634324452905));
#65578=CARTESIAN_POINT('Ctrl Pts',(-0.326665047731261,-0.395214267223794,
-0.484827143506015));
#65579=CARTESIAN_POINT('Ctrl Pts',(-0.0974966584912855,-0.503387298220306,
-0.470917513560256));
#65580=CARTESIAN_POINT('Ctrl Pts',(0.155487204176033,-0.488598096357353,
-0.457007883614497));
#65581=CARTESIAN_POINT('Ctrl Pts',(0.37049026384305,-0.354459214612929,
-0.443098253668739));
#65582=CARTESIAN_POINT('Ctrl Pts',(0.494993801063038,-0.133736709005703,
-0.429188623722979));
#65583=CARTESIAN_POINT('Ctrl Pts',(0.498585381931524,0.11965361403109,-0.41527899377722));
#65584=CARTESIAN_POINT('Ctrl Pts',(0.380387692291731,0.343816192142657,
-0.401369363831462));
#65585=CARTESIAN_POINT('Ctrl Pts',(0.169272838945517,0.483994913632211,
-0.387459733885702));
#65586=CARTESIAN_POINT('Ctrl Pts',(-0.0831902294088231,0.505948373015826,
-0.373550103939943));
#65587=CARTESIAN_POINT('Ctrl Pts',(-0.315332450581861,0.404314006728254,
-0.359640473994185));
#65588=CARTESIAN_POINT('Ctrl Pts',(-0.461089117569146,0.216009520375589,
-0.346570124814512));
#65589=CARTESIAN_POINT('Ctrl Pts',(-0.491769666283222,0.0670353643873584,
-0.338136318950092));
#65590=CARTESIAN_POINT('Ctrl Pts',(-0.491837902207756,-1.19650882245553E-5,
-0.334339056400925));
#65591=CARTESIAN_POINT('Ctrl Pts',(-0.49184907144521,-1.00963949215896E-5,
-0.474810943599073));
#65592=CARTESIAN_POINT('Ctrl Pts',(-0.491859231673575,-0.0110950176221044,
-0.47418310178465));
#65593=CARTESIAN_POINT('Ctrl Pts',(-0.488781234601853,-0.104035239247785,
-0.468918716654975));
#65594=CARTESIAN_POINT('Ctrl Pts',(-0.432496181911419,-0.275411368569959,
-0.459017788210046));
#65595=CARTESIAN_POINT('Ctrl Pts',(-0.247776674242662,-0.448899865233663,
-0.445108158264288));
#65596=CARTESIAN_POINT('Ctrl Pts',(-0.0025328481751963,-0.512735754541854,
-0.431198528318528));
#65597=CARTESIAN_POINT('Ctrl Pts',(0.243329675797957,-0.451325866953922,
-0.41728889837277));
#65598=CARTESIAN_POINT('Ctrl Pts',(0.429754148070265,-0.279670773449364,
-0.40337926842701));
#65599=CARTESIAN_POINT('Ctrl Pts',(0.511202730378688,-0.0397006014952209,
-0.389469638481251));
#65600=CARTESIAN_POINT('Ctrl Pts',(0.467780007046806,0.209967221996417,
-0.375560008535492));
#65601=CARTESIAN_POINT('Ctrl Pts',(0.310092830963972,0.408346428280455,
-0.361650378589733));
#65602=CARTESIAN_POINT('Ctrl Pts',(0.0766593914673165,0.506979000559367,
-0.347740748643974));
#65603=CARTESIAN_POINT('Ctrl Pts',(-0.175499609789847,0.481771996138208,
-0.333831118698215));
#65604=CARTESIAN_POINT('Ctrl Pts',(-0.384789384990357,0.338882720885541,
-0.319921488752456));
#65605=CARTESIAN_POINT('Ctrl Pts',(-0.478787527436172,0.154903082696593,
-0.308581430386075));
#65606=CARTESIAN_POINT('Ctrl Pts',(-0.491795302201702,0.0365114373392391,
-0.301877915334947));
#65607=CARTESIAN_POINT('Ctrl Pts',(-0.49178470790119,4.0904940727983E-6,
-0.299810943599072));
#65608=CARTESIAN_POINT('Origin',(0.,0.,-4.27183905640093));
#65609=CARTESIAN_POINT('',(-0.491798649685846,-1.03788440164814E-5,-0.684339056400923));
#65610=CARTESIAN_POINT('',(-0.491811749329251,1.24090953615708E-5,-0.649810943599071));
#65611=CARTESIAN_POINT('',(-0.491825,-1.07154090996976E-14,-4.27183905640093));
#65612=CARTESIAN_POINT('Ctrl Pts',(-0.491798649685846,-1.03788440165044E-5,
-0.684339056400923));
#65613=CARTESIAN_POINT('Ctrl Pts',(-0.491820132916021,-0.0281328181413851,
-0.682746691849496));
#65614=CARTESIAN_POINT('Ctrl Pts',(-0.48254192569275,-0.138126322570039,
-0.676517783982815));
#65615=CARTESIAN_POINT('Ctrl Pts',(-0.401603104826651,-0.318777848383641,
-0.665652332800882));
#65616=CARTESIAN_POINT('Ctrl Pts',(-0.199888170155967,-0.472174850937878,
-0.651742702855122));
#65617=CARTESIAN_POINT('Ctrl Pts',(0.0506533753796834,-0.510233873815872,
-0.637833072909363));
#65618=CARTESIAN_POINT('Ctrl Pts',(0.288821839273072,-0.423658253295539,
-0.623923442963605));
#65619=CARTESIAN_POINT('Ctrl Pts',(0.45643989718452,-0.233595784817902,
-0.610013813017846));
#65620=CARTESIAN_POINT('Ctrl Pts',(0.512563546869181,0.0135270413392405,
-0.596104183072087));
#65621=CARTESIAN_POINT('Ctrl Pts',(0.443483484763275,0.257345622011976,
-0.582194553126329));
#65622=CARTESIAN_POINT('Ctrl Pts',(0.266073872596039,0.438302480883072,
-0.568284923180568));
#65623=CARTESIAN_POINT('Ctrl Pts',(0.0236704920209714,0.51219535163255,
-0.55437529323481));
#65624=CARTESIAN_POINT('Ctrl Pts',(-0.224514871059556,0.460974449508451,
-0.540465663289051));
#65625=CARTESIAN_POINT('Ctrl Pts',(-0.417858067972524,0.297151485705153,
-0.526556033343292));
#65626=CARTESIAN_POINT('Ctrl Pts',(-0.485940965058413,0.120808897856263,
-0.516180497713917));
#65627=CARTESIAN_POINT('Ctrl Pts',(-0.491843123527572,0.019480205769144,
-0.510441505399794));
#65628=CARTESIAN_POINT('Ctrl Pts',(-0.49182316548349,1.28554485876817E-5,
-0.509339056400925));
#65629=CARTESIAN_POINT('Ctrl Pts',(-0.491811749329251,1.24090953615708E-5,
-0.649810943599071));
#65630=CARTESIAN_POINT('Ctrl Pts',(-0.491755982274121,-0.058663874621788,
-0.646488288234352));
#65631=CARTESIAN_POINT('Ctrl Pts',(-0.466588151730041,-0.199265543584639,
-0.638529089554379));
#65632=CARTESIAN_POINT('Ctrl Pts',(-0.33558034712377,-0.387672800090266,
-0.625933347559152));
#65633=CARTESIAN_POINT('Ctrl Pts',(-0.108934757177873,-0.501036513623642,
-0.612023717613395));
#65634=CARTESIAN_POINT('Ctrl Pts',(0.144320286415244,-0.49201221959882,
-0.598114087667635));
#65635=CARTESIAN_POINT('Ctrl Pts',(0.362322265961503,-0.362804279045959,
-0.584204457721877));
#65636=CARTESIAN_POINT('Ctrl Pts',(0.491819916942383,-0.144974268766304,
-0.570294827776118));
#65637=CARTESIAN_POINT('Ctrl Pts',(0.501180895095398,0.108268553592046,
-0.55638519783036));
#65638=CARTESIAN_POINT('Ctrl Pts',(0.388118597680438,0.33506465561158,-0.542475567884599));
#65639=CARTESIAN_POINT('Ctrl Pts',(0.180250711102229,0.480014635665076,
-0.528565937938842));
#65640=CARTESIAN_POINT('Ctrl Pts',(-0.0716469513364315,0.507711614668931,
-0.514656307993081));
#65641=CARTESIAN_POINT('Ctrl Pts',(-0.306043438944004,0.411390061601957,
-0.500746678047323));
#65642=CARTESIAN_POINT('Ctrl Pts',(-0.45847713183902,0.223461935246029,
-0.487464889915986));
#65643=CARTESIAN_POINT('Ctrl Pts',(-0.491784199495365,0.0707659165103001,
-0.478819645099903));
#65644=CARTESIAN_POINT('Ctrl Pts',(-0.49184907144521,-1.00963949215896E-5,
-0.474810943599073));
#65645=CARTESIAN_POINT('Origin',(0.,0.,-4.27183905640093));
#65646=CARTESIAN_POINT('',(-0.491860973371918,6.25837308208287E-6,-0.859339056400924));
#65647=CARTESIAN_POINT('',(-0.491808348730261,-1.20621083624095E-5,-0.824810943599071));
#65648=CARTESIAN_POINT('',(-0.491825,-1.07154090996976E-14,-4.27183905640093));
#65649=CARTESIAN_POINT('Ctrl Pts',(-0.491860973371918,6.25837308207075E-6,
-0.859339056400924));
#65650=CARTESIAN_POINT('Ctrl Pts',(-0.491813051771,-0.0756811199232177,
-0.855051878299199));
#65651=CARTESIAN_POINT('Ctrl Pts',(-0.454881898913209,-0.233268842049668,
-0.846128156882221));
#65652=CARTESIAN_POINT('Ctrl Pts',(-0.293567896890941,-0.420383468206752,
-0.832567892149989));
#65653=CARTESIAN_POINT('Ctrl Pts',(-0.0563880943787678,-0.509631978234137,
-0.818658262204231));
#65654=CARTESIAN_POINT('Ctrl Pts',(0.194565607506746,-0.474392869678749,
-0.804748632258471));
#65655=CARTESIAN_POINT('Ctrl Pts',(0.397992838976195,-0.323273986813317,
-0.790839002312714));
#65656=CARTESIAN_POINT('Ctrl Pts',(0.504202503940466,-0.0931890843751128,
-0.776929372366952));
#65657=CARTESIAN_POINT('Ctrl Pts',(0.487250806039511,0.159659081922555,
-0.763019742421195));
#65658=CARTESIAN_POINT('Ctrl Pts',(0.351278530374647,0.373507382155073,
-0.749110112475436));
#65659=CARTESIAN_POINT('Ctrl Pts',(0.12949957543287,0.496119169544188,-0.735200482529676));
#65660=CARTESIAN_POINT('Ctrl Pts',(-0.123912193856582,0.497544107230863,
-0.721290852583919));
#65661=CARTESIAN_POINT('Ctrl Pts',(-0.347055976470588,0.377434126202911,
-0.707381222638158));
#65662=CARTESIAN_POINT('Ctrl Pts',(-0.469584188812454,0.18943305115538,
-0.695063957243828));
#65663=CARTESIAN_POINT('Ctrl Pts',(-0.49175757944661,0.0537522676675991,
-0.687383235164749));
#65664=CARTESIAN_POINT('Ctrl Pts',(-0.491798649685846,-1.03788440165044E-5,
-0.684339056400923));
#65665=CARTESIAN_POINT('Ctrl Pts',(-0.491808348730261,-1.20621083624407E-5,
-0.824810943599071));
#65666=CARTESIAN_POINT('Ctrl Pts',(-0.49183063390641,-0.0243989399446512,
-0.823430017999307));
#65667=CARTESIAN_POINT('Ctrl Pts',(-0.484067683462823,-0.130652210543813,
-0.81741254908429));
#65668=CARTESIAN_POINT('Ctrl Pts',(-0.408758323003886,-0.309549677241936,
-0.80675853685402));
#65669=CARTESIAN_POINT('Ctrl Pts',(-0.210588930608419,-0.467500450920358,
-0.792848906908262));
#65670=CARTESIAN_POINT('Ctrl Pts',(0.0390209435287369,-0.511255058920363,
-0.778939276962502));
#65671=CARTESIAN_POINT('Ctrl Pts',(0.279099185935138,-0.430125579006736,
-0.765029647016744));
#65672=CARTESIAN_POINT('Ctrl Pts',(0.45100197136601,-0.243929479828719,
-0.751120017070984));
#65673=CARTESIAN_POINT('Ctrl Pts',(0.512738668738538,0.00185118496315108,
-0.737210387125225));
#65674=CARTESIAN_POINT('Ctrl Pts',(0.449228877364958,0.247179661475123,
-0.723300757179467));
#65675=CARTESIAN_POINT('Ctrl Pts',(0.27598611096193,0.432129651680657,-0.709391127233707));
#65676=CARTESIAN_POINT('Ctrl Pts',(0.0353283172785953,0.511523488516217,
-0.695481497287949));
#65677=CARTESIAN_POINT('Ctrl Pts',(-0.213959111659945,0.46596766823807,
-0.681571867342189));
#65678=CARTESIAN_POINT('Ctrl Pts',(-0.41098282595302,0.306590094551677,
-0.667662237396431));
#65679=CARTESIAN_POINT('Ctrl Pts',(-0.484532737369335,0.128282565717192,
-0.657075262815391));
#65680=CARTESIAN_POINT('Ctrl Pts',(-0.4918338014694,0.0232149545584419,
-0.651124831549605));
#65681=CARTESIAN_POINT('Ctrl Pts',(-0.491811749329251,1.24090953615708E-5,
-0.649810943599071));
#65682=CARTESIAN_POINT('Origin',(0.,0.,-4.27183905640093));
#65683=CARTESIAN_POINT('',(-0.49178273288147,4.4982614547824E-7,-1.03433905640092));
#65684=CARTESIAN_POINT('',(-0.491852307000294,9.3039398275617E-6,-0.999810943599072));
#65685=CARTESIAN_POINT('',(-0.491825,-1.07154090996976E-14,-4.27183905640093));
#65686=CARTESIAN_POINT('Ctrl Pts',(-0.49178273288147,4.49826145484944E-7,
-1.03433905640092));
#65687=CARTESIAN_POINT('Ctrl Pts',(-0.491781417251355,-0.0414258932373119,
-1.03199360806415));
#65688=CARTESIAN_POINT('Ctrl Pts',(-0.476369267714836,-0.164745870733351,
-1.02501161641213));
#65689=CARTESIAN_POINT('Ctrl Pts',(-0.37445296760404,-0.350270389098243,
-1.01339308144486));
#65690=CARTESIAN_POINT('Ctrl Pts',(-0.160971985229762,-0.48681864220436,
-0.999483451499097));
#65691=CARTESIAN_POINT('Ctrl Pts',(0.091829565624597,-0.50445188204992,
-0.985573821553339));
#65692=CARTESIAN_POINT('Ctrl Pts',(0.322199941771856,-0.398862843529854,
-0.971664191607578));
#65693=CARTESIAN_POINT('Ctrl Pts',(0.473866654939281,-0.195843722807663,
-0.957754561661822));
#65694=CARTESIAN_POINT('Ctrl Pts',(0.509782132080318,0.0550140730918329,
-0.94384493171606));
#65695=CARTESIAN_POINT('Ctrl Pts',(0.421173312613008,0.292433601299668,
-0.929935301770304));
#65696=CARTESIAN_POINT('Ctrl Pts',(0.229684640748129,0.458420479724576,
-0.916025671824541));
#65697=CARTESIAN_POINT('Ctrl Pts',(-0.017909015052109,0.512429153743588,
-0.902116041878785));
#65698=CARTESIAN_POINT('Ctrl Pts',(-0.261128042237548,0.441266944132112,
-0.888206411933025));
#65699=CARTESIAN_POINT('Ctrl Pts',(-0.440561417203972,0.262316618035793,
-0.874296781987266));
#65700=CARTESIAN_POINT('Ctrl Pts',(-0.490243642695107,0.0941950370601843,
-0.864674330143233));
#65701=CARTESIAN_POINT('Ctrl Pts',(-0.491864878537493,0.00617407702965306,
-0.859688421614452));
#65702=CARTESIAN_POINT('Ctrl Pts',(-0.491860973371918,6.25837308207075E-6,
-0.859339056400924));
#65703=CARTESIAN_POINT('Ctrl Pts',(-0.491852307000294,9.30393982757037E-6,
-0.999810943599072));
#65704=CARTESIAN_POINT('Ctrl Pts',(-0.491790081377928,-0.0719489292099996,
-0.99573520444901));
#65705=CARTESIAN_POINT('Ctrl Pts',(-0.457627845654389,-0.225823669989117,
-0.987022921983695));
#65706=CARTESIAN_POINT('Ctrl Pts',(-0.30306494471812,-0.413589178519626,
-0.973674096203129));
#65707=CARTESIAN_POINT('Ctrl Pts',(-0.0679790606200691,-0.508215718590787,
-0.959764466257369));
#65708=CARTESIAN_POINT('Ctrl Pts',(0.183712043973384,-0.478700589308868,
-0.94585483631161));
#65709=CARTESIAN_POINT('Ctrl Pts',(0.390527874180675,-0.332253440604396,
-0.931945206365851));
#65710=CARTESIAN_POINT('Ctrl Pts',(0.501949602127359,-0.104646864404638,
-0.918035576420092));
#65711=CARTESIAN_POINT('Ctrl Pts',(0.490760282718032,0.148521763428982,
-0.904125946474333));
#65712=CARTESIAN_POINT('Ctrl Pts',(0.359693126948704,0.365411033948621,
-0.890216316528574));
#65713=CARTESIAN_POINT('Ctrl Pts',(0.140763861447594,0.493041483666333,
-0.876306686582815));
#65714=CARTESIAN_POINT('Ctrl Pts',(-0.112549741462726,0.500236868895336,
-0.862397056637057));
#65715=CARTESIAN_POINT('Ctrl Pts',(-0.338370859824982,0.385239575494054,
-0.848487426691298));
#65716=CARTESIAN_POINT('Ctrl Pts',(-0.467324823515431,0.196899023737536,
-0.835958722345302));
#65717=CARTESIAN_POINT('Ctrl Pts',(-0.491755810045864,0.0574815143180991,
-0.82806656131456));
#65718=CARTESIAN_POINT('Ctrl Pts',(-0.491808348730261,-1.20621083624407E-5,
-0.824810943599071));
#65719=CARTESIAN_POINT('Origin',(0.,0.,-4.27183905640093));
#65720=CARTESIAN_POINT('',(-0.49185900932756,-7.11307669150856E-6,-1.20933905640092));
#65721=CARTESIAN_POINT('',(-0.491783786383942,-3.02292213444355E-6,-1.17481094359907));
#65722=CARTESIAN_POINT('',(-0.491825,-1.07154090996976E-14,-4.27183905640093));
#65723=CARTESIAN_POINT('Ctrl Pts',(-0.49185900932756,-7.11307669150688E-6,
-1.20933905640092));
#65724=CARTESIAN_POINT('Ctrl Pts',(-0.491864019509531,-0.00713458797730284,
-1.20893533782911));
#65725=CARTESIAN_POINT('Ctrl Pts',(-0.489969969681151,-0.0961155435516917,
-1.20389507594204));
#65726=CARTESIAN_POINT('Ctrl Pts',(-0.439018144460899,-0.264891372567355,
-1.19421827073972));
#65727=CARTESIAN_POINT('Ctrl Pts',(-0.258540186688332,-0.442788146062732,
-1.18030864079396));
#65728=CARTESIAN_POINT('Ctrl Pts',(-0.0149087112336633,-0.512525219629101,
-1.1663990108482));
#65729=CARTESIAN_POINT('Ctrl Pts',(0.232364509709674,-0.45706794358595,
-1.15248938090245));
#65730=CARTESIAN_POINT('Ctrl Pts',(0.422878136097861,-0.289962846649199,
-1.13857975095669));
#65731=CARTESIAN_POINT('Ctrl Pts',(0.51009547347383,-0.052028630272347,
-1.12467012101093));
#65732=CARTESIAN_POINT('Ctrl Pts',(0.472711974452847,0.198614600760868,
-1.11076049106517));
#65733=CARTESIAN_POINT('Ctrl Pts',(0.319859292789327,0.400742315263586,
-1.09685086111941));
#65734=CARTESIAN_POINT('Ctrl Pts',(0.0888746976244564,0.504980849685084,
-1.08294123117365));
#65735=CARTESIAN_POINT('Ctrl Pts',(-0.163819287712257,0.485867895008465,
-1.06903160122789));
#65736=CARTESIAN_POINT('Ctrl Pts',(-0.376497195023632,0.348072165744182,
-1.05512197128213));
#65737=CARTESIAN_POINT('Ctrl Pts',(-0.476853910979439,0.16282485140757,
-1.04355778967314));
#65738=CARTESIAN_POINT('Ctrl Pts',(-0.491784018023207,0.0404667799011544,
-1.03663015137941));
#65739=CARTESIAN_POINT('Ctrl Pts',(-0.49178273288147,4.49826145484944E-7,
-1.03433905640092));
#65740=CARTESIAN_POINT('Ctrl Pts',(-0.491783786383942,-3.02292213442967E-6,
-1.17481094359907));
#65741=CARTESIAN_POINT('Ctrl Pts',(-0.491791851348631,-0.0376946067152404,
-1.17267693421397));
#65742=CARTESIAN_POINT('Ctrl Pts',(-0.478220056409159,-0.157272646410343,
-1.16590638151361));
#65743=CARTESIAN_POINT('Ctrl Pts',(-0.382332390176345,-0.341652327267911,
-1.15449928549799));
#65744=CARTESIAN_POINT('Ctrl Pts',(-0.172016313369507,-0.483026663073893,
-1.14058965555223));
#65745=CARTESIAN_POINT('Ctrl Pts',(0.0803181259485588,-0.506412250986929,
-1.12668002560648));
#65746=CARTESIAN_POINT('Ctrl Pts',(0.313033285756316,-0.406096701924727,
-1.11277039566072));
#65747=CARTESIAN_POINT('Ctrl Pts',(0.469283918326265,-0.206584058692545,
-1.09886076571496));
#65748=CARTESIAN_POINT('Ctrl Pts',(0.510902738281055,0.0433907976701933,
-1.0849511357692));
#65749=CARTESIAN_POINT('Ctrl Pts',(0.427723531557066,0.282766599615103,
-1.07104150582344));
#65750=CARTESIAN_POINT('Ctrl Pts',(0.240064452828482,0.45307110677431,-1.05713187587768));
#65751=CARTESIAN_POINT('Ctrl Pts',(-0.0062350827696745,0.512704098919047,
-1.04322224593192));
#65752=CARTESIAN_POINT('Ctrl Pts',(-0.251011576959888,0.447099046674948,
-1.02931261598616));
#65753=CARTESIAN_POINT('Ctrl Pts',(-0.434473564237258,0.27228127237199,
-1.0154029860404));
#65754=CARTESIAN_POINT('Ctrl Pts',(-0.489146988657971,0.101666277091445,
-1.00556909524471));
#65755=CARTESIAN_POINT('Ctrl Pts',(-0.491860868978114,0.00991044711519981,
-1.00037174776426));
#65756=CARTESIAN_POINT('Ctrl Pts',(-0.491852307000294,9.30393982757037E-6,
-0.999810943599072));
#65757=CARTESIAN_POINT('Origin',(0.,0.,-4.27183905640093));
#65758=CARTESIAN_POINT('',(-0.491800974659427,1.08920470272003E-5,-1.38433905640092));
#65759=CARTESIAN_POINT('',(-0.491865353078785,-3.56841417972764E-6,-1.34981094359907));
#65760=CARTESIAN_POINT('',(-0.491825,-1.07154090996976E-14,-4.27183905640093));
#65761=CARTESIAN_POINT('Ctrl Pts',(-0.491800974659428,1.08920470272104E-5,
-1.38433905640092));
#65762=CARTESIAN_POINT('Ctrl Pts',(-0.491756812207049,-0.0547109370230884,
-1.38124052427881));
#65763=CARTESIAN_POINT('Ctrl Pts',(-0.469012650190695,-0.191352540086311,
-1.37350544884145));
#65764=CARTESIAN_POINT('Ctrl Pts',(-0.344840355124436,-0.379459483876949,
-1.36113383008883));
#65765=CARTESIAN_POINT('Ctrl Pts',(-0.120997217343892,-0.498261019769301,
-1.34722420014307));
#65766=CARTESIAN_POINT('Ctrl Pts',(0.132401866856018,-0.495352516981138,
-1.33331457019731));
#65767=CARTESIAN_POINT('Ctrl Pts',(0.353459195034396,-0.371444434434203,
-1.31940494025155));
#65768=CARTESIAN_POINT('Ctrl Pts',(0.488177173769909,-0.156803754535824,
-1.30549531030579));
#65769=CARTESIAN_POINT('Ctrl Pts',(0.503648291231812,0.0961393216419958,
-1.29158568036004));
#65770=CARTESIAN_POINT('Ctrl Pts',(0.396093423165933,0.325598480572622,
-1.27767605041428));
#65771=CARTESIAN_POINT('Ctrl Pts',(0.191784958206317,0.475523816682518,
-1.26376642046852));
#65772=CARTESIAN_POINT('Ctrl Pts',(-0.0593707489727289,0.509293122467725,
-1.24985679052276));
#65773=CARTESIAN_POINT('Ctrl Pts',(-0.296023984821974,0.418657581845388,
-1.235947160577));
#65774=CARTESIAN_POINT('Ctrl Pts',(-0.45559757693874,0.231355536394371,
-1.22244124920305));
#65775=CARTESIAN_POINT('Ctrl Pts',(-0.491806479610826,0.0747215573978147,
-1.21357188114436));
#65776=CARTESIAN_POINT('Ctrl Pts',(-0.49185900932756,-7.11307669150688E-6,
-1.20933905640092));
#65777=CARTESIAN_POINT('Ctrl Pts',(-0.491865353078785,-3.56841417971767E-6,
-1.34981094359907));
#65778=CARTESIAN_POINT('Ctrl Pts',(-0.491866674226144,-0.00339805385570091,
-1.34961866397892));
#65779=CARTESIAN_POINT('Ctrl Pts',(-0.491002663521623,-0.0886449429922445,
-1.34478984104352));
#65780=CARTESIAN_POINT('Ctrl Pts',(-0.444936530586125,-0.254825142118117,
-1.33532447479286));
#65781=CARTESIAN_POINT('Ctrl Pts',(-0.268556528523827,-0.436785714387234,
-1.3214148448471));
#65782=CARTESIAN_POINT('Ctrl Pts',(-0.0265763205901719,-0.512052798536855,
-1.30750521490134));
#65783=CARTESIAN_POINT('Ctrl Pts',(0.221895675540188,-0.462240931205903,
-1.29359558495558));
#65784=CARTESIAN_POINT('Ctrl Pts',(0.416165295443046,-0.299517639170616,
-1.27968595500983));
#65785=CARTESIAN_POINT('Ctrl Pts',(0.508778369487043,-0.063631281989616,
-1.26577632506407));
#65786=CARTESIAN_POINT('Ctrl Pts',(0.477112335647494,0.187798265376785,
-1.25186669511831));
#65787=CARTESIAN_POINT('Ctrl Pts',(0.328902244531517,0.393354398536063,
-1.23795706517255));
#65788=CARTESIAN_POINT('Ctrl Pts',(0.100351321370171,0.502825995355051,
-1.22404743522679));
#65789=CARTESIAN_POINT('Ctrl Pts',(-0.15271238268513,0.489472468561989,
-1.21013780528103));
#65790=CARTESIAN_POINT('Ctrl Pts',(-0.368473088379839,0.356555679305995,
-1.19622817533527));
#65791=CARTESIAN_POINT('Ctrl Pts',(-0.474933894869138,0.170297388134082,
-1.18445255477462));
#65792=CARTESIAN_POINT('Ctrl Pts',(-0.491774328671187,0.0441975640019624,
-1.17731347752922));
#65793=CARTESIAN_POINT('Ctrl Pts',(-0.491783786383942,-3.02292213442967E-6,
-1.17481094359907));
#65794=CARTESIAN_POINT('Origin',(0.,0.,-4.27183905640093));
#65795=CARTESIAN_POINT('',(-0.491820155779459,-1.28375648062008E-5,-1.55933905640092));
#65796=CARTESIAN_POINT('',(-0.491792696404785,8.61912597031889E-6,-1.52481094359907));
#65797=CARTESIAN_POINT('',(-0.491825,-1.07154090996976E-14,-4.27183905640093));
#65798=CARTESIAN_POINT('Ctrl Pts',(-0.491820155779459,-1.28375648062243E-5,
-1.55933905640092));
#65799=CARTESIAN_POINT('Ctrl Pts',(-0.491840834199996,-0.0204403340332267,
-1.55818225404377));
#65800=CARTESIAN_POINT('Ctrl Pts',(-0.485587427915056,-0.122730064592817,
-1.55238890837136));
#65801=CARTESIAN_POINT('Ctrl Pts',(-0.416111244906428,-0.299592727363217,
-1.5419590193837));
#65802=CARTESIAN_POINT('Ctrl Pts',(-0.221812266131596,-0.462280963289723,
-1.52804938943794));
#65803=CARTESIAN_POINT('Ctrl Pts',(0.0266687144847388,-0.512047995889291,
-1.51413975949218));
#65804=CARTESIAN_POINT('Ctrl Pts',(0.268635337881236,-0.436737250149265,
-1.50023012954642));
#65805=CARTESIAN_POINT('Ctrl Pts',(0.44498250467321,-0.254744854631581,
-1.48632049960066));
#65806=CARTESIAN_POINT('Ctrl Pts',(0.512633956353846,-0.0105260258174941,
-1.4724108696549));
#65807=CARTESIAN_POINT('Ctrl Pts',(0.455064497344623,0.23626399150737,-1.45850123970914));
#65808=CARTESIAN_POINT('Ctrl Pts',(0.286336598528917,0.425341889271909,
-1.44459160976338));
#65809=CARTESIAN_POINT('Ctrl Pts',(0.047665362586952,0.510521677929509,
-1.43068197981763));
#65810=CARTESIAN_POINT('Ctrl Pts',(-0.202649074195538,0.47099652138227,
-1.41677234987187));
#65811=CARTESIAN_POINT('Ctrl Pts',(-0.403462495084136,0.316421215292198,
-1.40286271992611));
#65812=CARTESIAN_POINT('Ctrl Pts',(-0.482942720425566,0.136204978692006,
-1.39205162210246));
#65813=CARTESIAN_POINT('Ctrl Pts',(-0.491822895473348,0.0271730392516382,
-1.38587706759407));
#65814=CARTESIAN_POINT('Ctrl Pts',(-0.491800974659428,1.08920470272104E-5,
-1.38433905640092));
#65815=CARTESIAN_POINT('Ctrl Pts',(-0.491792696404785,8.61912597030848E-6,
-1.52481094359907));
#65816=CARTESIAN_POINT('Ctrl Pts',(-0.49176087174051,-0.0509815371313851,
-1.52192385042862));
#65817=CARTESIAN_POINT('Ctrl Pts',(-0.471200171751201,-0.183884693624623,
-1.51440021394292));
#65818=CARTESIAN_POINT('Ctrl Pts',(-0.353392165482507,-0.371508205402143,
-1.50224003414197));
#65819=CARTESIAN_POINT('Ctrl Pts',(-0.132312483529502,-0.495376398315253,
-1.48833040419621));
#65820=CARTESIAN_POINT('Ctrl Pts',(0.121087120812267,-0.498239177984762,
-1.47442077425045));
#65821=CARTESIAN_POINT('Ctrl Pts',(0.344908818047041,-0.379397254258554,
-1.46051114430469));
#65822=CARTESIAN_POINT('Ctrl Pts',(0.484479763326162,-0.167880100765288,
-1.44660151435893));
#65823=CARTESIAN_POINT('Ctrl Pts',(0.505707012440461,0.0846450640857451,
-1.43269188441317));
#65824=CARTESIAN_POINT('Ctrl Pts',(0.40340539294362,0.316494009816205,-1.41878225446742));
#65825=CARTESIAN_POINT('Ctrl Pts',(0.202564084346017,0.47103307849725,-1.40487262452166));
#65826=CARTESIAN_POINT('Ctrl Pts',(-0.0477574797057481,0.510513067842236,
-1.3909629945759));
#65827=CARTESIAN_POINT('Ctrl Pts',(-0.28641334150177,0.425290215165276,
-1.37705336463014));
#65828=CARTESIAN_POINT('Ctrl Pts',(-0.452775183555581,0.238796012894704,
-1.36333601430453));
#65829=CARTESIAN_POINT('Ctrl Pts',(-0.49183481667956,0.0784550243347217,
-1.35425520729417));
#65830=CARTESIAN_POINT('Ctrl Pts',(-0.491865353078785,-3.56841417971767E-6,
-1.34981094359907));
#65831=CARTESIAN_POINT('Origin',(0.,0.,-4.27183905640093));
#65832=CARTESIAN_POINT('',(-0.491840877697987,1.15800763210497E-5,-1.73433905640093));
#65833=CARTESIAN_POINT('',(-0.491831982535426,-1.2519398762012E-5,-1.69981094359907));
#65834=CARTESIAN_POINT('',(-0.491825,-1.07154090996976E-14,-4.27183905640093));
#65835=CARTESIAN_POINT('Ctrl Pts',(-0.491840877697987,1.1580076321056E-5,
-1.73433905640093));
#65836=CARTESIAN_POINT('Ctrl Pts',(-0.491772846092899,-0.0679942662770046,
-1.73048744049347));
#65837=CARTESIAN_POINT('Ctrl Pts',(-0.46042730279502,-0.217925740442619,
-1.72199928127076));
#65838=CARTESIAN_POINT('Ctrl Pts',(-0.312960005664294,-0.406153179577745,
-1.70887457873281));
#65839=CARTESIAN_POINT('Ctrl Pts',(-0.0802267483162252,-0.506426736341114,
-1.69496494878705));
#65840=CARTESIAN_POINT('Ctrl Pts',(0.172103467761028,-0.482995617797032,
-1.68105531884129));
#65841=CARTESIAN_POINT('Ctrl Pts',(0.38239403215543,-0.341583334778529,
-1.66714568889553));
#65842=CARTESIAN_POINT('Ctrl Pts',(0.499277344932229,-0.116732614396888,
-1.65323605894977));
#65843=CARTESIAN_POINT('Ctrl Pts',(0.494202361649382,0.136632339388161,
-1.63932642900401));
#65844=CARTESIAN_POINT('Ctrl Pts',(0.36840874663372,0.35662216115979,-1.62541679905825));
#65845=CARTESIAN_POINT('Ctrl Pts',(0.152624060625208,0.489500016899674,
-1.61150716911249));
#65846=CARTESIAN_POINT('Ctrl Pts',(-0.100442049346334,0.502807880954164,
-1.59759753916673));
#65847=CARTESIAN_POINT('Ctrl Pts',(-0.328973216334069,0.393295046194743,
-1.58368790922097));
#65848=CARTESIAN_POINT('Ctrl Pts',(-0.464823322547969,0.20480959069708,
-1.57093508163237));
#65849=CARTESIAN_POINT('Ctrl Pts',(-0.491757953669959,0.0614344751008574,
-1.56281879735902));
#65850=CARTESIAN_POINT('Ctrl Pts',(-0.491820155779459,-1.28375648062243E-5,
-1.55933905640092));
#65851=CARTESIAN_POINT('Ctrl Pts',(-0.491831982535426,-1.25193987619981E-5,
-1.69981094359907));
#65852=CARTESIAN_POINT('Ctrl Pts',(-0.491849266882592,-0.016705147158428,
-1.69886558019358));
#65853=CARTESIAN_POINT('Ctrl Pts',(-0.486929935288758,-0.115256778052977,
-1.69328367347283));
#65854=CARTESIAN_POINT('Ctrl Pts',(-0.422825807720183,-0.290039144998243,
-1.68306522343684));
#65855=CARTESIAN_POINT('Ctrl Pts',(-0.232282032571033,-0.457109862779405,
-1.66915559349108));
#65856=CARTESIAN_POINT('Ctrl Pts',(0.0150011904725086,-0.51252252008077,
-1.65524596354532));
#65857=CARTESIAN_POINT('Ctrl Pts',(0.25862007815723,-0.442741487190307,
-1.64133633359956));
#65858=CARTESIAN_POINT('Ctrl Pts',(0.439065933099701,-0.264812151716694,
-1.6274267036538));
#65859=CARTESIAN_POINT('Ctrl Pts',(0.512261311724355,-0.0221972479370705,
-1.61351707370804));
#65860=CARTESIAN_POINT('Ctrl Pts',(0.46032680542771,0.225839769549687,-1.59960744376228));
#65861=CARTESIAN_POINT('Ctrl Pts',(0.295948437236704,0.418710988394965,
-1.58569781381652));
#65862=CARTESIAN_POINT('Ctrl Pts',(0.0592788515625552,0.509303825886828,
-1.57178818387076));
#65863=CARTESIAN_POINT('Ctrl Pts',(-0.191870757694326,0.475489202450847,
-1.55787855392501));
#65864=CARTESIAN_POINT('Ctrl Pts',(-0.396152166521947,0.325527003895996,
-1.54396892397925));
#65865=CARTESIAN_POINT('Ctrl Pts',(-0.481350054693306,0.143679183617523,
-1.53294638720394));
#65866=CARTESIAN_POINT('Ctrl Pts',(-0.491811980736892,0.0309063875669545,
-1.52656039374388));
#65867=CARTESIAN_POINT('Ctrl Pts',(-0.491792696404785,8.61912597030848E-6,
-1.52481094359907));
#65868=CARTESIAN_POINT('Origin',(0.,0.,-4.27183905640093));
#65869=CARTESIAN_POINT('',(-0.491787937416117,-6.46297745255268E-6,-1.90933905640093));
#65870=CARTESIAN_POINT('',(-0.491829112982424,1.26920333077193E-5,-1.87481094359907));
#65871=CARTESIAN_POINT('',(-0.491825,-1.07154090996976E-14,-4.27183905640093));
#65872=CARTESIAN_POINT('Ctrl Pts',(-0.491787937416117,-6.46297745255861E-6,
-1.90933905640093));
#65873=CARTESIAN_POINT('Ctrl Pts',(-0.491803529803698,-0.0337386931560804,
-1.90742917025843));
#65874=CARTESIAN_POINT('Ctrl Pts',(-0.480081042180642,-0.149350430953692,
-1.90088274080068));
#65875=CARTESIAN_POINT('Ctrl Pts',(-0.390467917193037,-0.332323902344444,
-1.88969976802767));
#65876=CARTESIAN_POINT('Ctrl Pts',(-0.183625665141514,-0.478733731345353,
-1.87579013808191));
#65877=CARTESIAN_POINT('Ctrl Pts',(0.0680707615702241,-0.508203445330468,
-1.86188050813615));
#65878=CARTESIAN_POINT('Ctrl Pts',(0.303139568028706,-0.413534487947351,
-1.8479708781904));
#65879=CARTESIAN_POINT('Ctrl Pts',(0.464160582092247,-0.217851611098688,
-1.83406124824463));
#65880=CARTESIAN_POINT('Ctrl Pts',(0.511801259025317,0.0310457998223131,
-1.82015161829888));
#65881=CARTESIAN_POINT('Ctrl Pts',(0.43442442794312,0.272359664474753,-1.80624198835312));
#65882=CARTESIAN_POINT('Ctrl Pts',(0.250930899325168,0.447144332615734,
-1.79233235840736));
#65883=CARTESIAN_POINT('Ctrl Pts',(0.00614257089095992,0.512705216717518,
-1.7784227284616));
#65884=CARTESIAN_POINT('Ctrl Pts',(-0.240146201108115,0.453027783386239,
-1.76451309851584));
#65885=CARTESIAN_POINT('Ctrl Pts',(-0.427774547614985,0.282689417628787,
-1.75060346857008));
#65886=CARTESIAN_POINT('Ctrl Pts',(-0.487889963149149,0.109586602519485,
-1.74054545453178));
#65887=CARTESIAN_POINT('Ctrl Pts',(-0.4918547419754,0.0138706080728537,
-1.73512398380873));
#65888=CARTESIAN_POINT('Ctrl Pts',(-0.491840877697987,1.1580076321056E-5,
-1.73433905640093));
#65889=CARTESIAN_POINT('Ctrl Pts',(-0.491829112982424,1.26920333077315E-5,
-1.87481094359907));
#65890=CARTESIAN_POINT('Ctrl Pts',(-0.491762475705567,-0.064264325262914,
-1.87117076664328));
#65891=CARTESIAN_POINT('Ctrl Pts',(-0.462964584526037,-0.210469807830858,
-1.86289404637224));
#65892=CARTESIAN_POINT('Ctrl Pts',(-0.322127965446493,-0.398920973606101,
-1.84998078278594));
#65893=CARTESIAN_POINT('Ctrl Pts',(-0.0917385411651713,-0.504468442393003,
-1.83607115284018));
#65894=CARTESIAN_POINT('Ctrl Pts',(0.161059823311547,-0.48678958762528,
-1.82216152289443));
#65895=CARTESIAN_POINT('Ctrl Pts',(0.37451616313179,-0.350202816748494,
-1.80825189294867));
#65896=CARTESIAN_POINT('Ctrl Pts',(0.496489575545123,-0.128072130772313,
-1.79434226300291));
#65897=CARTESIAN_POINT('Ctrl Pts',(0.497185659316439,0.125342688161754,
-1.78043263305715));
#65898=CARTESIAN_POINT('Ctrl Pts',(0.376434382315248,0.348140094094997,
-1.76652300311139));
#65899=CARTESIAN_POINT('Ctrl Pts',(0.163731615202558,0.485897445443685,
-1.75261337316563));
#65900=CARTESIAN_POINT('Ctrl Pts',(-0.088965814203307,0.504964803930609,
-1.73870374321987));
#65901=CARTESIAN_POINT('Ctrl Pts',(-0.319931596423644,0.40068459281005,
-1.72479411327411));
#65902=CARTESIAN_POINT('Ctrl Pts',(-0.462361700510878,0.212268719064823,
-1.71182984673385));
#65903=CARTESIAN_POINT('Ctrl Pts',(-0.491764495646635,0.0651639956531007,
-1.70350212350883));
#65904=CARTESIAN_POINT('Ctrl Pts',(-0.491831982535426,-1.25193987619981E-5,
-1.69981094359907));
#65905=CARTESIAN_POINT('Origin',(0.,0.,-4.27183905640093));
#65906=CARTESIAN_POINT('',(-0.491867427628364,6.00722023146672E-7,-2.08433905640092));
#65907=CARTESIAN_POINT('',(-0.491794496945441,-9.2326743954263E-6,-2.04981094359907));
#65908=CARTESIAN_POINT('',(-0.491825,-1.07154090996976E-14,-4.27183905640093));
#65909=CARTESIAN_POINT('Ctrl Pts',(-0.491867398827384,6.00314237376911E-7,
-2.08433905640092));
#65910=CARTESIAN_POINT('Ctrl Pts',(-0.491861574474256,-0.0812893295483687,
-2.07973435670813));
#65911=CARTESIAN_POINT('Ctrl Pts',(-0.45056433286084,-0.244437046519258,
-2.07049311370008));
#65912=CARTESIAN_POINT('Ctrl Pts',(-0.279021570577783,-0.430175933286389,
-2.05661532737678));
#65913=CARTESIAN_POINT('Ctrl Pts',(-0.0389286926494526,-0.511262092585704,
-2.04270569743102));
#65914=CARTESIAN_POINT('Ctrl Pts',(0.210673282920791,-0.467462445860503,
-2.02879606748526));
#65915=CARTESIAN_POINT('Ctrl Pts',(0.408814172040582,-0.309475916939077,
-2.0148864375395));
#65916=CARTESIAN_POINT('Ctrl Pts',(0.507094171550263,-0.0758938179712873,
-2.00097680759374));
#65917=CARTESIAN_POINT('Ctrl Pts',(0.481506461595899,0.176226836401005,
-1.98706717764799));
#65918=CARTESIAN_POINT('Ctrl Pts',(0.338301342812545,0.385300625327465,
-1.97315754770222));
#65919=CARTESIAN_POINT('Ctrl Pts',(0.112459477653878,0.500257170175825,
-1.95924791775647));
#65920=CARTESIAN_POINT('Ctrl Pts',(-0.140852823344986,0.493016077407475,
-1.94533828781071));
#65921=CARTESIAN_POINT('Ctrl Pts',(-0.359759056244216,0.365346126128058,
-1.93142865786495));
#65922=CARTESIAN_POINT('Ctrl Pts',(-0.472796042913746,0.178216817683005,
-1.91942891406169));
#65923=CARTESIAN_POINT('Ctrl Pts',(-0.491765676876868,0.0481515006429693,
-1.91206571357368));
#65924=CARTESIAN_POINT('Ctrl Pts',(-0.491787937416117,-6.46297745255861E-6,
-1.90933905640093));
#65925=CARTESIAN_POINT('Ctrl Pts',(-0.491794496945441,-9.23267439544018E-6,
-2.04981094359907));
#65926=CARTESIAN_POINT('Ctrl Pts',(-0.491814648737398,-0.0300059021629562,
-2.04811249640824));
#65927=CARTESIAN_POINT('Ctrl Pts',(-0.481742510538666,-0.141876266339579,
-2.04177750590215));
#65928=CARTESIAN_POINT('Ctrl Pts',(-0.397934500429466,-0.32334579427215,
-2.03080597208081));
#65929=CARTESIAN_POINT('Ctrl Pts',(-0.194480004972519,-0.474427968158946,
-2.01689634213505));
#65930=CARTESIAN_POINT('Ctrl Pts',(0.0564800508004891,-0.509621794242663,
-2.00298671218929));
#65931=CARTESIAN_POINT('Ctrl Pts',(0.293643745038357,-0.420330489383515,
-1.98907708224353));
#65932=CARTESIAN_POINT('Ctrl Pts',(0.459079188120922,-0.228365208251544,
-1.97516745229777));
#65933=CARTESIAN_POINT('Ctrl Pts',(0.512375524336397,0.0193827595181383,
-1.96125782235201));
#65934=CARTESIAN_POINT('Ctrl Pts',(0.440514076957236,0.262396107646534,
-1.94734819240626));
#65935=CARTESIAN_POINT('Ctrl Pts',(0.261048415685123,0.441314053678131,
-1.9334385624605));
#65936=CARTESIAN_POINT('Ctrl Pts',(0.0178165525430863,0.512432375793154,
-1.91952893251474));
#65937=CARTESIAN_POINT('Ctrl Pts',(-0.229767353430185,0.458379027228804,
-1.90561930256898));
#65938=CARTESIAN_POINT('Ctrl Pts',(-0.421226071271232,0.292357599844676,
-1.89170967262322));
#65939=CARTESIAN_POINT('Ctrl Pts',(-0.486614162270651,0.117059418554486,
-1.88144021963325));
#65940=CARTESIAN_POINT('Ctrl Pts',(-0.49184735251906,0.0176061932554664,
-1.87580730995854));
#65941=CARTESIAN_POINT('Ctrl Pts',(-0.491829112982424,1.26920333077315E-5,
-1.87481094359907));
#65942=CARTESIAN_POINT('Origin',(0.,0.,-4.27183905640093));
#65943=CARTESIAN_POINT('',(-0.491786451319463,5.52690589573186E-6,-2.25933905640092));
#65944=CARTESIAN_POINT('',(-0.491864161604618,4.47272762704037E-6,-2.22481094359907));
#65945=CARTESIAN_POINT('',(-0.491825,-1.07154090996976E-14,-4.27183905640093));
#65946=CARTESIAN_POINT('Ctrl Pts',(-0.491786451319463,5.52690589572871E-6,
-2.25933905640092));
#65947=CARTESIAN_POINT('Ctrl Pts',(-0.491767929113347,-0.0470280052530091,
-2.25667608647308));
#65948=CARTESIAN_POINT('Ctrl Pts',(-0.473414348620751,-0.175966592201857,
-2.24937657322999));
#65949=CARTESIAN_POINT('Ctrl Pts',(-0.362256796811613,-0.362869650963398,
-2.23744051667165));
#65950=CARTESIAN_POINT('Ctrl Pts',(-0.144231506204031,-0.492038253639516,
-2.22353088672589));
#65951=CARTESIAN_POINT('Ctrl Pts',(0.1090251621404,-0.501016850461905,-2.20962125678013));
#65952=CARTESIAN_POINT('Ctrl Pts',(0.33565029365018,-0.387612242839485,
-2.19571162683437));
#65953=CARTESIAN_POINT('Ctrl Pts',(0.480286249602533,-0.179525733167259,
-2.18180199688861));
#65954=CARTESIAN_POINT('Ctrl Pts',(0.507602857467195,0.0724134622680479,
-2.16789236694285));
#65955=CARTESIAN_POINT('Ctrl Pts',(0.410927499343277,0.306664247524861,
-2.15398273699709));
#65956=CARTESIAN_POINT('Ctrl Pts',(0.213875029915099,0.466006268203898,
-2.14007310705133));
#65957=CARTESIAN_POINT('Ctrl Pts',(-0.0354206155412066,0.511517106675026,
-2.12616347710558));
#65958=CARTESIAN_POINT('Ctrl Pts',(-0.276064080079156,0.432079846922483,
-2.11225384715981));
#65959=CARTESIAN_POINT('Ctrl Pts',(-0.449273471848797,0.247098599590194,
-2.09834421721406));
#65960=CARTESIAN_POINT('Ctrl Pts',(-0.491729113979008,0.0829769823530704,
-2.08903928696109));
#65961=CARTESIAN_POINT('Ctrl Pts',(-0.491867439105472,0.000562757677112689,
-2.08437090002338));
#65962=CARTESIAN_POINT('Ctrl Pts',(-0.491867398827384,6.00314237376911E-7,
-2.08433905640092));
#65963=CARTESIAN_POINT('Ctrl Pts',(-0.491864161604618,4.47272762705338E-6,
-2.22481094359907));
#65964=CARTESIAN_POINT('Ctrl Pts',(-0.491827285582898,-0.0775542653706536,
-2.22041768285794));
#65965=CARTESIAN_POINT('Ctrl Pts',(-0.453465461486664,-0.237001846569603,
-2.21138787880155));
#65966=CARTESIAN_POINT('Ctrl Pts',(-0.288745389504487,-0.423710360205458,
-2.19772153142992));
#65967=CARTESIAN_POINT('Ctrl Pts',(-0.0505613083818057,-0.510243004263906,
-2.18381190148416));
#65968=CARTESIAN_POINT('Ctrl Pts',(0.199973365210935,-0.472138774632788,
-2.1699022715384));
#65969=CARTESIAN_POINT('Ctrl Pts',(0.401660617373509,-0.318705377671398,
-2.15599264159264));
#65970=CARTESIAN_POINT('Ctrl Pts',(0.505234376131355,-0.0874219336362221,
-2.14208301164688));
#65971=CARTESIAN_POINT('Ctrl Pts',(0.485394716977961,0.165216034438012,
-2.12817338170112));
#65972=CARTESIAN_POINT('Ctrl Pts',(0.346987866262887,0.377496741670528,
-2.11426375175536));
#65973=CARTESIAN_POINT('Ctrl Pts',(0.123822415238128,0.49756645665693,-2.10035412180961));
#65974=CARTESIAN_POINT('Ctrl Pts',(-0.129589092271495,0.496095793642505,
-2.08644449186384));
#65975=CARTESIAN_POINT('Ctrl Pts',(-0.351345919187724,0.37344399094867,
-2.07253486191809));
#65976=CARTESIAN_POINT('Ctrl Pts',(-0.470681307409857,0.185686283826414,
-2.06032367916316));
#65977=CARTESIAN_POINT('Ctrl Pts',(-0.491759636926143,0.0518811639451681,
-2.05274903972349));
#65978=CARTESIAN_POINT('Ctrl Pts',(-0.491794496945441,-9.23267439544018E-6,
-2.04981094359907));
#65979=CARTESIAN_POINT('Origin',(0.,0.,-4.27183905640093));
#65980=CARTESIAN_POINT('',(-0.49184428547454,-1.10437734740307E-5,-2.43433905640093));
#65981=CARTESIAN_POINT('',(-0.491783273045562,2.19569279796827E-6,-2.39981094359907));
#65982=CARTESIAN_POINT('',(-0.491825,-1.07154090996976E-14,-4.27183905640093));
#65983=CARTESIAN_POINT('Ctrl Pts',(-0.49184428547454,-1.1043773474018E-5,
-2.43433905640093));
#65984=CARTESIAN_POINT('Ctrl Pts',(-0.491856670524148,-0.0127453266690652,
-2.43361781623804));
#65985=CARTESIAN_POINT('Ctrl Pts',(-0.488257104721263,-0.1073358620036,
-2.4282600327599));
#65986=CARTESIAN_POINT('Ctrl Pts',(-0.429703678489127,-0.279748313881283,
-2.41826570596651));
#65987=CARTESIAN_POINT('Ctrl Pts',(-0.243248235588849,-0.451369766720613,
-2.40435607602075));
#65988=CARTESIAN_POINT('Ctrl Pts',(0.00262536564176082,-0.512735290263655,
-2.39044644607499));
#65989=CARTESIAN_POINT('Ctrl Pts',(0.247857669758745,-0.448855150319423,
-2.37653681612923));
#65990=CARTESIAN_POINT('Ctrl Pts',(0.432545870731629,-0.275333325515683,
-2.36262718618348));
#65991=CARTESIAN_POINT('Ctrl Pts',(0.511576248657834,-0.0345559290959576,
-2.34871755623772));
#65992=CARTESIAN_POINT('Ctrl Pts',(0.46564408176967,0.214662431597587,-2.33480792629196));
#65993=CARTESIAN_POINT('Ctrl Pts',(0.305969203822596,0.411445277939455,
-2.3208982963462));
#65994=CARTESIAN_POINT('Ctrl Pts',(0.0715553393709438,0.507724535387071,
-2.30698866640044));
#65995=CARTESIAN_POINT('Ctrl Pts',(-0.180337321890193,0.479982104624726,
-2.29307903645468));
#65996=CARTESIAN_POINT('Ctrl Pts',(-0.388179050905097,0.334994619158167,
-2.27916940650892));
#65997=CARTESIAN_POINT('Ctrl Pts',(-0.479562715419935,0.151601669956443,
-2.267922746491));
#65998=CARTESIAN_POINT('Ctrl Pts',(-0.491800178448968,0.0348628966472575,
-2.26131262978834));
#65999=CARTESIAN_POINT('Ctrl Pts',(-0.491786451319463,5.52690589572871E-6,
-2.25933905640092));
#66000=CARTESIAN_POINT('Ctrl Pts',(-0.491783273045562,2.19569279793705E-6,
-2.39981094359907));
#66001=CARTESIAN_POINT('Ctrl Pts',(-0.491776551894691,-0.0432976893620342,
-2.3973594126229));
#66002=CARTESIAN_POINT('Ctrl Pts',(-0.475405604406094,-0.168494975390873,
-2.39027133833147));
#66003=CARTESIAN_POINT('Ctrl Pts',(-0.370426298772862,-0.354526058961786,
-2.37854672072478));
#66004=CARTESIAN_POINT('Ctrl Pts',(-0.155399039185073,-0.488626143309885,
-2.36463709077902));
#66005=CARTESIAN_POINT('Ctrl Pts',(0.0975874873726366,-0.503369696757594,
-2.35072746083327));
#66006=CARTESIAN_POINT('Ctrl Pts',(0.326736353765087,-0.395155316848746,
-2.3368178308875));
#66007=CARTESIAN_POINT('Ctrl Pts',(0.476073449464557,-0.190416490936197,
-2.32290820094175));
#66008=CARTESIAN_POINT('Ctrl Pts',(0.509120256238909,0.060835302191775,
-2.30899857099599));
#66009=CARTESIAN_POINT('Ctrl Pts',(0.417804442576766,0.297226878106026,
-2.29508894105023));
#66010=CARTESIAN_POINT('Ctrl Pts',(0.224431689179598,0.461014952249414,
-2.28117931110447));
#66011=CARTESIAN_POINT('Ctrl Pts',(-0.0237629115774706,0.512191071123753,
-2.26726968115871));
#66012=CARTESIAN_POINT('Ctrl Pts',(-0.266152954537513,0.438254462722844,
-2.25336005121295));
#66013=CARTESIAN_POINT('Ctrl Pts',(-0.443529911772546,0.257265595578916,
-2.23945042126719));
#66014=CARTESIAN_POINT('Ctrl Pts',(-0.49076141250102,0.0904469082399701,
-2.22993405206257));
#66015=CARTESIAN_POINT('Ctrl Pts',(-0.491866203662674,0.00429938954725858,
-2.22505422617319));
#66016=CARTESIAN_POINT('Ctrl Pts',(-0.491864161604618,4.47272762705338E-6,
-2.22481094359907));
#66017=CARTESIAN_POINT('Origin',(0.,0.,-4.27183905640093));
#66018=CARTESIAN_POINT('',(-0.49181668614067,1.27304208609013E-5,-2.60933905640093));
#66019=CARTESIAN_POINT('',(-0.491854631260498,-8.64168429531853E-6,-2.57481094359907));
#66020=CARTESIAN_POINT('',(-0.491825,-1.07154090996976E-14,-4.27183905640093));
#66021=CARTESIAN_POINT('Ctrl Pts',(-0.49181668614067,1.27304208609111E-5,
-2.60933905640093));
#66022=CARTESIAN_POINT('Ctrl Pts',(-0.491756878388132,-0.0603111785225525,
-2.60592300268774));
#66023=CARTESIAN_POINT('Ctrl Pts',(-0.46554538245605,-0.202562094355018,
-2.59787040565931));
#66024=CARTESIAN_POINT('Ctrl Pts',(-0.331663405555064,-0.391029098459597,
-2.58518126531562));
#66025=CARTESIAN_POINT('Ctrl Pts',(-0.103888852940067,-0.502107037056149,
-2.57127163536986));
#66026=CARTESIAN_POINT('Ctrl Pts',(0.149262592123117,-0.490535471723703,
-2.5573620054241));
#66027=CARTESIAN_POINT('Ctrl Pts',(0.365953717915752,-0.359140984531349,
-2.54345237547834));
#66028=CARTESIAN_POINT('Ctrl Pts',(0.49325346169053,-0.140019259235349,
-2.52954274553259));
#66029=CARTESIAN_POINT('Ctrl Pts',(0.500066361181473,0.113304919757393,
-2.51563311558682));
#66030=CARTESIAN_POINT('Ctrl Pts',(0.384728231899584,0.338952147073784,
-2.50172348564107));
#66031=CARTESIAN_POINT('Ctrl Pts',(0.175412676874732,0.481803656293877,
-2.48781385569531));
#66032=CARTESIAN_POINT('Ctrl Pts',(-0.0767508691435963,0.506965161043843,
-2.47390422574955));
#66033=CARTESIAN_POINT('Ctrl Pts',(-0.310166508178242,0.4082904696794,-2.45999459580379));
#66034=CARTESIAN_POINT('Ctrl Pts',(-0.459643369733334,0.220170619003029,
-2.44680620602092));
#66035=CARTESIAN_POINT('Ctrl Pts',(-0.491777052358209,0.0691179101173199,
-2.43825435955329));
#66036=CARTESIAN_POINT('Ctrl Pts',(-0.49184428547454,-1.1043773474018E-5,
-2.43433905640093));
#66037=CARTESIAN_POINT('Ctrl Pts',(-0.491854631260498,-8.64168429529598E-6,
-2.57481094359907));
#66038=CARTESIAN_POINT('Ctrl Pts',(-0.491861998545963,-0.00900919132475913,
-2.57430114238785));
#66039=CARTESIAN_POINT('Ctrl Pts',(-0.489419424958644,-0.0998640001557114,
-2.56915479786138));
#66040=CARTESIAN_POINT('Ctrl Pts',(-0.435962809677364,-0.269890344183994,
-2.55937191001965));
#66041=CARTESIAN_POINT('Ctrl Pts',(-0.253463967943028,-0.445713345391533,
-2.54546228007389));
#66042=CARTESIAN_POINT('Ctrl Pts',(-0.00905157463938524,-0.512662109290402,
-2.53155265012813));
#66043=CARTESIAN_POINT('Ctrl Pts',(0.237571843520245,-0.454383085591805,
-2.51764302018238));
#66044=CARTESIAN_POINT('Ctrl Pts',(0.426163673582462,-0.285112070288575,
-2.50373339023661));
#66045=CARTESIAN_POINT('Ctrl Pts',(0.510656657582095,-0.0461968329284603,
-2.48982376029085));
#66046=CARTESIAN_POINT('Ctrl Pts',(0.470411724946076,0.204002888064838,
-2.4759141303451));
#66047=CARTESIAN_POINT('Ctrl Pts',(0.315259490780706,0.404370897541139,
-2.46200450039934));
#66048=CARTESIAN_POINT('Ctrl Pts',(0.083098935083214,0.505963374458638,
-2.44809487045358));
#66049=CARTESIAN_POINT('Ctrl Pts',(-0.169360167363873,0.48396436130775,
-2.43418524050782));
#66050=CARTESIAN_POINT('Ctrl Pts',(-0.380449723121679,0.343747549056243,
-2.42027561056206));
#66051=CARTESIAN_POINT('Ctrl Pts',(-0.477782100252891,0.159075394567747,
-2.40881751159248));
#66052=CARTESIAN_POINT('Ctrl Pts',(-0.491789263505291,0.0385947258483526,
-2.40199595593815));
#66053=CARTESIAN_POINT('Ctrl Pts',(-0.491783273045562,2.19569279793705E-6,
-2.39981094359907));
#66054=CARTESIAN_POINT('Origin',(0.,0.,-4.27183905640093));
#66055=CARTESIAN_POINT('',(-0.491803854275335,-1.14244199510044E-5,-2.78433905640093));
#66056=CARTESIAN_POINT('',(-0.491805856046874,1.17355489448745E-5,-2.74981094359907));
#66057=CARTESIAN_POINT('',(-0.491825,-1.07154090996976E-14,-4.27183905640093));
#66058=CARTESIAN_POINT('Ctrl Pts',(-0.491803854275335,-1.14244199509762E-5,
-2.78433905640093));
#66059=CARTESIAN_POINT('Ctrl Pts',(-0.491826081341972,-0.02604838175069,
-2.7828647324527));
#66060=CARTESIAN_POINT('Ctrl Pts',(-0.483404780242388,-0.133953703491761,
-2.77675386518922));
#66061=CARTESIAN_POINT('Ctrl Pts',(-0.405623591737084,-0.313646093954341,
-2.76600645461048));
#66062=CARTESIAN_POINT('Ctrl Pts',(-0.205875253078692,-0.469595305125906,
-2.75209682466473));
#66063=CARTESIAN_POINT('Ctrl Pts',(0.0441621590199009,-0.510836641341642,
-2.73818719471897));
#66064=CARTESIAN_POINT('Ctrl Pts',(0.283412096543389,-0.427296096354025,
-2.72427756477321));
#66065=CARTESIAN_POINT('Ctrl Pts',(0.453433063980492,-0.239380088803917,
-2.71036793482745));
#66066=CARTESIAN_POINT('Ctrl Pts',(0.512694101247579,0.00700920626356338,
-2.69645830488169));
#66067=CARTESIAN_POINT('Ctrl Pts',(0.446719536253416,0.251686365057864,
-2.68254867493593));
#66068=CARTESIAN_POINT('Ctrl Pts',(0.271624952073492,0.434884186695241,
-2.66863904499017));
#66069=CARTESIAN_POINT('Ctrl Pts',(0.0301806393140316,0.511853005693142,
-2.65472941504441));
#66070=CARTESIAN_POINT('Ctrl Pts',(-0.218635887270253,0.463791676535983,
-2.64081978509866));
#66071=CARTESIAN_POINT('Ctrl Pts',(-0.414046304926066,0.302440122674851,
-2.6269101551529));
#66072=CARTESIAN_POINT('Ctrl Pts',(-0.485165733168298,0.124981187180373,
-2.61641657892032));
#66073=CARTESIAN_POINT('Ctrl Pts',(-0.491838054288311,0.0215652907150948,
-2.610559546003));
#66074=CARTESIAN_POINT('Ctrl Pts',(-0.49181668614067,1.27304208609111E-5,
-2.60933905640093));
#66075=CARTESIAN_POINT('Ctrl Pts',(-0.491805856046874,1.1735548944871E-5,
-2.74981094359907));
#66076=CARTESIAN_POINT('Ctrl Pts',(-0.491755926810843,-0.05658196160197,
-2.74660632883756));
#66077=CARTESIAN_POINT('Ctrl Pts',(-0.467878716857623,-0.195098347367542,
-2.73876517076078));
#66078=CARTESIAN_POINT('Ctrl Pts',(-0.340482102013575,-0.383374891606055,
-2.72628746936876));
#66079=CARTESIAN_POINT('Ctrl Pts',(-0.115296139210803,-0.499611018281843,
-2.712377839423));
#66080=CARTESIAN_POINT('Ctrl Pts',(0.138053169722395,-0.493807342629832,
-2.69846820947724));
#66081=CARTESIAN_POINT('Ctrl Pts',(0.357680280931475,-0.367381526397719,
-2.68455857953148));
#66082=CARTESIAN_POINT('Ctrl Pts',(0.489936959575747,-0.151215557887439,
-2.67064894958572));
#66083=CARTESIAN_POINT('Ctrl Pts',(0.502516914705533,0.101887780132694,
-2.65673931963996));
#66084=CARTESIAN_POINT('Ctrl Pts',(0.392347245241488,0.330103027033912,
-2.64282968969421));
#66085=CARTESIAN_POINT('Ctrl Pts',(0.186339056407328,0.477684127183188,
-2.62892005974845));
#66086=CARTESIAN_POINT('Ctrl Pts',(-0.0651861061879488,0.508581498744882,
-2.61501042980269));
#66087=CARTESIAN_POINT('Ctrl Pts',(-0.300788282254515,0.415247851967851,
-2.60110079985693));
#66088=CARTESIAN_POINT('Ctrl Pts',(-0.456974840927703,0.227620125942558,
-2.58770097112239));
#66089=CARTESIAN_POINT('Ctrl Pts',(-0.491794994511007,0.0728490650907621,
-2.57893768570311));
#66090=CARTESIAN_POINT('Ctrl Pts',(-0.491854631260498,-8.64168429529598E-6,
-2.57481094359907));
#66091=CARTESIAN_POINT('Origin',(0.,0.,-4.27183905640093));
#66092=CARTESIAN_POINT('',(-0.491856460957234,8.05430276504716E-6,-2.95933905640093));
#66093=CARTESIAN_POINT('',(-0.491814419211658,-1.26084172522301E-5,-2.92481094359907));
#66094=CARTESIAN_POINT('',(-0.491825,-1.07154090996976E-14,-4.27183905640093));
#66095=CARTESIAN_POINT('Ctrl Pts',(-0.491856460957234,8.0543027650452E-6,
-2.95933905640093));
#66096=CARTESIAN_POINT('Ctrl Pts',(-0.491799376571172,-0.0735973513096081,
-2.9551699189024));
#66097=CARTESIAN_POINT('Ctrl Pts',(-0.456427518232039,-0.229113145239056,
-2.94636423808863));
#66098=CARTESIAN_POINT('Ctrl Pts',(-0.29888893149109,-0.416617062851034,
-2.93292201395959));
#66099=CARTESIAN_POINT('Ctrl Pts',(-0.0628630064529875,-0.5088738673249,
-2.91901238401384));
#66100=CARTESIAN_POINT('Ctrl Pts',(0.188518442383684,-0.476828236692982,
-2.90510275406808));
#66101=CARTESIAN_POINT('Ctrl Pts',(0.393850559636817,-0.328307945533265,
-2.89119312412232));
#66102=CARTESIAN_POINT('Ctrl Pts',(0.502976943457436,-0.0995919915290553,
-2.87728349417656));
#66103=CARTESIAN_POINT('Ctrl Pts',(0.489241331627754,0.153451262144076,
-2.8633738642308));
#66104=CARTESIAN_POINT('Ctrl Pts',(0.35599891707028,0.369011031639022,-2.84946423428504));
#66105=CARTESIAN_POINT('Ctrl Pts',(0.135796776088882,0.494432610201203,
-2.83555460433928));
#66106=CARTESIAN_POINT('Ctrl Pts',(-0.117576394161712,0.499079314300279,
-2.82164497439352));
#66107=CARTESIAN_POINT('Ctrl Pts',(-0.342229221231611,0.381816095210394,
-2.80773534444777));
#66108=CARTESIAN_POINT('Ctrl Pts',(-0.468334820753547,0.193601437055532,
-2.79530003845023));
#66109=CARTESIAN_POINT('Ctrl Pts',(-0.491756180315567,0.0558342198353221,
-2.78750127576795));
#66110=CARTESIAN_POINT('Ctrl Pts',(-0.491803854275335,-1.14244199509762E-5,
-2.78433905640093));
#66111=CARTESIAN_POINT('Ctrl Pts',(-0.491814419211658,-1.26084172522266E-5,
-2.92481094359907));
#66112=CARTESIAN_POINT('Ctrl Pts',(-0.491836147905159,-0.0223141218257271,
-2.92354805860251));
#66113=CARTESIAN_POINT('Ctrl Pts',(-0.48488055383623,-0.126479739420017,
-2.91764863029069));
#66114=CARTESIAN_POINT('Ctrl Pts',(-0.412660904457599,-0.304327697125603,
-2.90711265866362));
#66115=CARTESIAN_POINT('Ctrl Pts',(-0.216515718225303,-0.464785233271151,
-2.89320302871787));
#66116=CARTESIAN_POINT('Ctrl Pts',(0.0325176840114124,-0.511709848969189,
-2.87929339877211));
#66117=CARTESIAN_POINT('Ctrl Pts',(0.273608003362249,-0.43363928535323,
-2.86538376882635));
#66118=CARTESIAN_POINT('Ctrl Pts',(0.447864194914093,-0.249643810697336,
-2.85147413888059));
#66119=CARTESIAN_POINT('Ctrl Pts',(0.51272076192407,-0.00466793289774274,
-2.83756450893483));
#66120=CARTESIAN_POINT('Ctrl Pts',(0.452335214279015,0.241448179178668,
-2.82365487898907));
#66121=CARTESIAN_POINT('Ctrl Pts',(0.281457907812556,0.428585832051545,
-2.80974524904331));
#66122=CARTESIAN_POINT('Ctrl Pts',(0.0418289802326045,0.511032979090623,
-2.79583561909755));
#66123=CARTESIAN_POINT('Ctrl Pts',(-0.208017497185851,0.468650285575578,
-2.78192598915179));
#66124=CARTESIAN_POINT('Ctrl Pts',(-0.40705161597261,0.311790556687697,
-2.76801635920603));
#66125=CARTESIAN_POINT('Ctrl Pts',(-0.483707850118771,0.13245508266619,
-2.7573113440218));
#66126=CARTESIAN_POINT('Ctrl Pts',(-0.491828166091625,0.0252996833812049,
-2.75124287215281));
#66127=CARTESIAN_POINT('Ctrl Pts',(-0.491805856046874,1.1735548944871E-5,
-2.74981094359907));
#66128=CARTESIAN_POINT('Origin',(0.,0.,-4.27183905640093));
#66129=CARTESIAN_POINT('',(-0.491782972158755,-1.50095741644205E-6,-3.13433905640093));
#66130=CARTESIAN_POINT('',(-0.491846492690184,1.06369834088973E-5,-3.09981094359907));
#66131=CARTESIAN_POINT('',(-0.491825,-1.07154090996976E-14,-4.27183905640093));
#66132=CARTESIAN_POINT('Ctrl Pts',(-0.491782972158755,-1.50095741644624E-6,
-3.13433905640093));
#66133=CARTESIAN_POINT('Ctrl Pts',(-0.491787143576006,-0.0393429040773888,
-3.13211164866736));
#66134=CARTESIAN_POINT('Ctrl Pts',(-0.477413957249408,-0.160573869922756,
-3.12524769761854));
#66135=CARTESIAN_POINT('Ctrl Pts',(-0.378876045665121,-0.345481276551521,
-3.11374720325446));
#66136=CARTESIAN_POINT('Ctrl Pts',(-0.167148395020481,-0.484732693830926,
-3.0998375733087));
#66137=CARTESIAN_POINT('Ctrl Pts',(0.0854085334848828,-0.505578631702793,
-3.08592794336294));
#66138=CARTESIAN_POINT('Ctrl Pts',(0.317102750476299,-0.402927060479777,
-3.07201831341718));
#66139=CARTESIAN_POINT('Ctrl Pts',(0.47133839355793,-0.201852642253547,
-3.05810868347143));
#66140=CARTESIAN_POINT('Ctrl Pts',(0.510440378104306,0.0485282477248127,
-3.04419905352566));
#66141=CARTESIAN_POINT('Ctrl Pts',(0.424857276524671,0.287055160222818,
-3.03028942357991));
#66142=CARTESIAN_POINT('Ctrl Pts',(0.235494442018191,0.455463212790065,
-3.01637979363415));
#66143=CARTESIAN_POINT('Ctrl Pts',(-0.0113925344738468,0.512615431473507,
-3.00247016368839));
#66144=CARTESIAN_POINT('Ctrl Pts',(-0.255496660699727,0.444551264532895,
-2.98856053374263));
#66145=CARTESIAN_POINT('Ctrl Pts',(-0.437190710233471,0.267896721353699,
-2.97465090379687));
#66146=CARTESIAN_POINT('Ctrl Pts',(-0.489642054774299,0.0983659229714609,
-2.96491041134964));
#66147=CARTESIAN_POINT('Ctrl Pts',(-0.491862860739947,0.00826002362209832,
-2.95980646221765));
#66148=CARTESIAN_POINT('Ctrl Pts',(-0.491856460957234,8.0543027650452E-6,
-2.95933905640093));
#66149=CARTESIAN_POINT('Ctrl Pts',(-0.491846492690184,1.06369834089078E-5,
-3.09981094359907));
#66150=CARTESIAN_POINT('Ctrl Pts',(-0.4917801485058,-0.0698659474040416,
-3.09585324505221));
#66151=CARTESIAN_POINT('Ctrl Pts',(-0.459116439411713,-0.221664739361114,
-3.0872590031901));
#66152=CARTESIAN_POINT('Ctrl Pts',(-0.308298828990521,-0.409702576692666,
-3.07402821801273));
#66153=CARTESIAN_POINT('Ctrl Pts',(-0.0744350294889845,-0.507310354408927,
-3.06011858806697));
#66154=CARTESIAN_POINT('Ctrl Pts',(0.177610987683289,-0.480997615752618,
-3.04620895812121));
#66155=CARTESIAN_POINT('Ctrl Pts',(0.386272033277762,-0.337191763857008,
-3.03229932817546));
#66156=CARTESIAN_POINT('Ctrl Pts',(0.500578549326249,-0.111020202035327,
-3.0183896982297));
#66157=CARTESIAN_POINT('Ctrl Pts',(0.492608924589448,0.142270224292942,
-3.00448006828394));
#66158=CARTESIAN_POINT('Ctrl Pts',(0.364309896412847,0.360808354505819,
-2.99057043833818));
#66159=CARTESIAN_POINT('Ctrl Pts',(0.147021021901026,0.491211958755805,
-2.97666080839242));
#66160=CARTESIAN_POINT('Ctrl Pts',(-0.10618062433576,0.501627395903777,
-2.96275117844666));
#66161=CARTESIAN_POINT('Ctrl Pts',(-0.333445567956295,0.389510490893173,
-2.9488415485009));
#66162=CARTESIAN_POINT('Ctrl Pts',(-0.46602109057202,0.201065803521883,
-2.93619480355171));
#66163=CARTESIAN_POINT('Ctrl Pts',(-0.491756373397683,0.0595634309169782,
-2.92818460191776));
#66164=CARTESIAN_POINT('Ctrl Pts',(-0.491814419211658,-1.26084172522266E-5,
-2.92481094359907));
#66165=CARTESIAN_POINT('Origin',(0.,0.,-4.27183905640093));
#66166=CARTESIAN_POINT('',(-0.491862997454019,-5.20327585691352E-6,-3.30933905640093));
#66167=CARTESIAN_POINT('',(-0.491785594053212,-4.88331669762365E-6,-3.27481094359907));
#66168=CARTESIAN_POINT('',(-0.491825,-1.07154090996976E-14,-4.27183905640093));
#66169=CARTESIAN_POINT('Ctrl Pts',(-0.491862997454019,-5.20327585694629E-6,
-3.30933905640093));
#66170=CARTESIAN_POINT('Ctrl Pts',(-0.491865730726733,-0.00504860421699772,
-3.30905337843231));
#66171=CARTESIAN_POINT('Ctrl Pts',(-0.490557081626144,-0.0919448026840877,
-3.30413115714845));
#66172=CARTESIAN_POINT('Ctrl Pts',(-0.442350493670444,-0.259288278130775,
-3.29457239254933));
#66173=CARTESIAN_POINT('Ctrl Pts',(-0.264148905910468,-0.439465272726765,
-3.28066276260357));
#66174=CARTESIAN_POINT('Ctrl Pts',(-0.0214237606571462,-0.512294244458996,
-3.26675313265781));
#66175=CARTESIAN_POINT('Ctrl Pts',(0.226534558845831,-0.459985286802776,
-3.25284350271205));
#66176=CARTESIAN_POINT('Ctrl Pts',(0.419157363777824,-0.295315889882908,
-3.2389338727663));
#66177=CARTESIAN_POINT('Ctrl Pts',(0.509392751403437,-0.0585097875927088,
-3.22502424282053));
#66178=CARTESIAN_POINT('Ctrl Pts',(0.475198956297498,0.192588479303088,
-3.21111461287478));
#66179=CARTESIAN_POINT('Ctrl Pts',(0.324928484395358,0.396643228172426,
-3.19720498292901));
#66180=CARTESIAN_POINT('Ctrl Pts',(0.0952878493958325,0.503810079478394,
-3.18329535298326));
#66181=CARTESIAN_POINT('Ctrl Pts',(-0.157628714033977,0.487911425300231,
-3.1693857230375));
#66182=CARTESIAN_POINT('Ctrl Pts',(-0.372041368626771,0.35283082413081,
-3.15547609309174));
#66183=CARTESIAN_POINT('Ctrl Pts',(-0.475793553181783,0.166996697092384,
-3.14379387087955));
#66184=CARTESIAN_POINT('Ctrl Pts',(-0.49177846040746,0.042549655106789,
-3.13674819198261));
#66185=CARTESIAN_POINT('Ctrl Pts',(-0.491782972158755,-1.50095741644624E-6,
-3.13433905640093));
#66186=CARTESIAN_POINT('Ctrl Pts',(-0.491785594053212,-4.88331669762365E-6,
-3.27481094359907));
#66187=CARTESIAN_POINT('Ctrl Pts',(-0.49179795679528,-0.0356112203065527,
-3.27279497481717));
#66188=CARTESIAN_POINT('Ctrl Pts',(-0.479213063431929,-0.153100258346796,
-3.26614246272001));
#66189=CARTESIAN_POINT('Ctrl Pts',(-0.386645261186138,-0.336763732174116,
-3.2548534073076));
#66190=CARTESIAN_POINT('Ctrl Pts',(-0.178143619199366,-0.480800603414854,
-3.24094377736184));
#66191=CARTESIAN_POINT('Ctrl Pts',(0.0738731000725598,-0.507392485548619,
-3.22703414741608));
#66192=CARTESIAN_POINT('Ctrl Pts',(0.307844863968601,-0.410043789166097,
-3.21312451747032));
#66193=CARTESIAN_POINT('Ctrl Pts',(0.466619474536125,-0.212533845043952,
-3.19921488752456));
#66194=CARTESIAN_POINT('Ctrl Pts',(0.511413115207255,0.0368916643640206,
-3.18530525757881));
#66195=CARTESIAN_POINT('Ctrl Pts',(0.431284059612851,0.277305660290942,
-3.17139562763304));
#66196=CARTESIAN_POINT('Ctrl Pts',(0.245805403116349,0.449982303101295,
-3.15748599768729));
#66197=CARTESIAN_POINT('Ctrl Pts',(0.000283949904538727,0.5127419318507,
-3.14357636774152));
#66198=CARTESIAN_POINT('Ctrl Pts',(-0.24530686364752,0.450254274774769,
-3.12966673779577));
#66199=CARTESIAN_POINT('Ctrl Pts',(-0.430976658539604,0.277783169215801,
-3.11575710785));
#66200=CARTESIAN_POINT('Ctrl Pts',(-0.488497120387308,0.105837624003322,
-3.10580517645111));
#66201=CARTESIAN_POINT('Ctrl Pts',(-0.491857872385214,0.0119962273922986,
-3.10048978836747));
#66202=CARTESIAN_POINT('Ctrl Pts',(-0.491846492690184,1.06369834089078E-5,
-3.09981094359907));
#66203=CARTESIAN_POINT('Origin',(0.,0.,-4.27183905640093));
#66204=CARTESIAN_POINT('',(-0.49179609326986,9.71264568225073E-6,-3.48433905640093));
#66205=CARTESIAN_POINT('',(-0.491867129348278,-1.39672308571703E-6,-3.44981094359908));
#66206=CARTESIAN_POINT('',(-0.491825,-1.07154090996976E-14,-4.27183905640093));
#66207=CARTESIAN_POINT('Ctrl Pts',(-0.49179609326986,9.71264568224578E-6,
-3.48433905640093));
#66208=CARTESIAN_POINT('Ctrl Pts',(-0.491758729881948,-0.0526289498675229,
-3.48135856488202));
#66209=CARTESIAN_POINT('Ctrl Pts',(-0.470245757754536,-0.187183730626312,
-3.47374153004786));
#66210=CARTESIAN_POINT('Ctrl Pts',(-0.349636937317957,-0.3750445073447,
-3.46148795189843));
#66211=CARTESIAN_POINT('Ctrl Pts',(-0.127322336735289,-0.496682386435005,
-3.44757832195268));
#66212=CARTESIAN_POINT('Ctrl Pts',(0.12609324488764,-0.496995839037123,
-3.43366869200692));
#66213=CARTESIAN_POINT('Ctrl Pts',(0.348708075290391,-0.375908298197551,
-3.41975906206116));
#66214=CARTESIAN_POINT('Ctrl Pts',(0.486144110547877,-0.162997773623204,
-3.4058494321154));
#66215=CARTESIAN_POINT('Ctrl Pts',(0.504829900148016,0.0897281580277445,
-3.39193980216964));
#66216=CARTESIAN_POINT('Ctrl Pts',(0.40020107303874,0.320536225043519,-3.37803017222388));
#66217=CARTESIAN_POINT('Ctrl Pts',(0.197815274890308,0.473047024561597,
-3.36412054227812));
#66218=CARTESIAN_POINT('Ctrl Pts',(-0.0528907887479718,0.51000679886853,
-3.35021091233236));
#66219=CARTESIAN_POINT('Ctrl Pts',(-0.29067723859158,0.422387397292203,
-3.3363012823866));
#66220=CARTESIAN_POINT('Ctrl Pts',(-0.4540346552045,0.235510171083702,-3.32267733040946));
#66221=CARTESIAN_POINT('Ctrl Pts',(-0.491821369807362,0.0768056144799782,
-3.31368992174757));
#66222=CARTESIAN_POINT('Ctrl Pts',(-0.491862997454019,-5.20327585694629E-6,
-3.30933905640093));
#66223=CARTESIAN_POINT('Ctrl Pts',(-0.491867129348278,-1.39672308572809E-6,
-3.44981094359908));
#66224=CARTESIAN_POINT('Ctrl Pts',(-0.491867342373088,-0.00131199121913817,
-3.44973670458213));
#66225=CARTESIAN_POINT('Ctrl Pts',(-0.491541924711959,-0.0844746968207473,
-3.44502592224992));
#66226=CARTESIAN_POINT('Ctrl Pts',(-0.448140419207187,-0.24914761483575,
-3.43567859660246));
#66227=CARTESIAN_POINT('Ctrl Pts',(-0.274088123141906,-0.433335978264076,
-3.42176896665671));
#66228=CARTESIAN_POINT('Ctrl Pts',(-0.0330844205931006,-0.511673519365186,
-3.40785933671095));
#66229=CARTESIAN_POINT('Ctrl Pts',(0.216000801380951,-0.4650247553715,-3.39394970676519));
#66230=CARTESIAN_POINT('Ctrl Pts',(0.412323585901499,-0.304784562953681,
-3.38004007681943));
#66231=CARTESIAN_POINT('Ctrl Pts',(0.50792823756029,-0.0700947558269063,
-3.36613044687367));
#66232=CARTESIAN_POINT('Ctrl Pts',(0.479461442753112,0.18171707189651,-3.35222081692791));
#66233=CARTESIAN_POINT('Ctrl Pts',(0.33387677512836,0.38914093633981,-3.33831118698215));
#66234=CARTESIAN_POINT('Ctrl Pts',(0.106736148672607,0.501509485326126,
-3.3244015570364));
#66235=CARTESIAN_POINT('Ctrl Pts',(-0.146476878127779,0.491374494127927,
-3.31049192709063));
#66236=CARTESIAN_POINT('Ctrl Pts',(-0.363910051005443,0.361211633371286,
-3.29658229714488));
#66237=CARTESIAN_POINT('Ctrl Pts',(-0.473821174853051,0.174468579041008,
-3.28468863598102));
#66238=CARTESIAN_POINT('Ctrl Pts',(-0.491769523622302,0.0462800893370987,
-3.27743151813242));
#66239=CARTESIAN_POINT('Ctrl Pts',(-0.491785594053212,-4.88331669762365E-6,
-3.27481094359907));
#66240=CARTESIAN_POINT('Origin',(0.,0.,-4.27183905640093));
#66241=CARTESIAN_POINT('',(-0.491826729621748,-1.27889840308831E-5,-3.65933905640093));
#66242=CARTESIAN_POINT('',(-0.491789055620677,7.06292780691675E-6,-3.62481094359907));
#66243=CARTESIAN_POINT('',(-0.491825,-1.07154090996976E-14,-4.27183905640093));
#66244=CARTESIAN_POINT('Ctrl Pts',(-0.491826729621748,-1.27889840308929E-5,
-3.65933905640093));
#66245=CARTESIAN_POINT('Ctrl Pts',(-0.491845702227525,-0.018355149817109,
-3.65830029464697));
#66246=CARTESIAN_POINT('Ctrl Pts',(-0.486347785408333,-0.11855786198984,
-3.65262498957776));
#66247=CARTESIAN_POINT('Ctrl Pts',(-0.419886639219421,-0.294278066833141,
-3.6423131411933));
#66248=CARTESIAN_POINT('Ctrl Pts',(-0.227671785951002,-0.459423473843918,
-3.62840351124754));
#66249=CARTESIAN_POINT('Ctrl Pts',(0.0201563719388868,-0.512345675389839,
-3.61449388130178));
#66250=CARTESIAN_POINT('Ctrl Pts',(0.263060940163059,-0.440117384557558,
-3.60058425135602));
#66251=CARTESIAN_POINT('Ctrl Pts',(0.441707707892028,-0.260381779728162,
-3.58667462141027));
#66252=CARTESIAN_POINT('Ctrl Pts',(0.512458693932598,-0.0170428119589638,
-3.57276499146451));
#66253=CARTESIAN_POINT('Ctrl Pts',(0.458031580571258,0.230459197312829,
-3.55885536151875));
#66254=CARTESIAN_POINT('Ctrl Pts',(0.291721259059309,0.421667021996254,
-3.54494573157299));
#66255=CARTESIAN_POINT('Ctrl Pts',(0.0541522913452231,0.509874396070913,
-3.53103610162723));
#66256=CARTESIAN_POINT('Ctrl Pts',(-0.196644436945652,0.473534936245239,
-3.51712647168147));
#66257=CARTESIAN_POINT('Ctrl Pts',(-0.399406899907004,0.321525269198555,
-3.50321684173571));
#66258=CARTESIAN_POINT('Ctrl Pts',(-0.482064722644773,0.140377619227812,
-3.49228770330886));
#66259=CARTESIAN_POINT('Ctrl Pts',(-0.491816853505303,0.0292573555458383,
-3.48599510819727));
#66260=CARTESIAN_POINT('Ctrl Pts',(-0.49179609326986,9.71264568224578E-6,
-3.48433905640093));
#66261=CARTESIAN_POINT('Ctrl Pts',(-0.491789055620677,7.06292780690287E-6,
-3.62481094359907));
#66262=CARTESIAN_POINT('Ctrl Pts',(-0.491764279731792,-0.0488993655234134,
-3.62204189103183));
#66263=CARTESIAN_POINT('Ctrl Pts',(-0.472379668665207,-0.179714664337686,
-3.61463629514933));
#66264=CARTESIAN_POINT('Ctrl Pts',(-0.358086963773074,-0.366985143679068,
-3.60259415595158));
#66265=CARTESIAN_POINT('Ctrl Pts',(-0.13860001322218,-0.493654135646059,
-3.58868452600581));
#66266=CARTESIAN_POINT('Ctrl Pts',(0.114742712316349,-0.499738410846886,
-3.57477489606006));
#66267=CARTESIAN_POINT('Ctrl Pts',(0.340057277111318,-0.383751765584462,
-3.5608652661143));
#66268=CARTESIAN_POINT('Ctrl Pts',(0.482306174096344,-0.174026215651783,
-3.54695563616854));
#66269=CARTESIAN_POINT('Ctrl Pts',(0.506742316769786,0.0782086548939713,
-3.53304600622278));
#66270=CARTESIAN_POINT('Ctrl Pts',(0.407396697418865,0.311339525659273,
-3.51913637627702));
#66271=CARTESIAN_POINT('Ctrl Pts',(0.208536434469852,0.46841960335167,-3.50522674633126));
#66272=CARTESIAN_POINT('Ctrl Pts',(-0.041262947733106,0.511078994334449,
-3.4913171163855));
#66273=CARTESIAN_POINT('Ctrl Pts',(-0.280983044651029,0.428897304636174,
-3.47740748643975));
#66274=CARTESIAN_POINT('Ctrl Pts',(-0.451154396430177,0.242946813420274,
-3.46357209551093));
#66275=CARTESIAN_POINT('Ctrl Pts',(-0.491854038064979,0.0805402261099205,
-3.45437324789738));
#66276=CARTESIAN_POINT('Ctrl Pts',(-0.491867129348278,-1.39672308572809E-6,
-3.44981094359908));
#66277=CARTESIAN_POINT('Origin',(0.,0.,-4.27183905640093));
#66278=CARTESIAN_POINT('',(-0.491834365111822,1.2415361585749E-5,-3.83433905640093));
#66279=CARTESIAN_POINT('',(-0.491838560105423,-1.18860308867263E-5,-3.79981094359907));
#66280=CARTESIAN_POINT('',(-0.491825,-1.07154090996976E-14,-4.27183905640093));
#66281=CARTESIAN_POINT('Ctrl Pts',(-0.491834365111822,1.24153615857388E-5,
-3.83433905640092));
#66282=CARTESIAN_POINT('Ctrl Pts',(-0.491766406376123,-0.0659117740156114,
-3.83060548109667));
#66283=CARTESIAN_POINT('Ctrl Pts',(-0.461856136979431,-0.213763970312948,
-3.82223536247717));
#66284=CARTESIAN_POINT('Ctrl Pts',(-0.318098551972822,-0.402141302407426,
-3.80922870054241));
#66285=CARTESIAN_POINT('Ctrl Pts',(-0.086658980441776,-0.505365835465607,
-3.79531907059665));
#66286=CARTESIAN_POINT('Ctrl Pts',(0.165948741836808,-0.485144687019642,
-3.7814094406509));
#66287=CARTESIAN_POINT('Ctrl Pts',(0.378020228680476,-0.346417499554377,
-3.76749981070513));
#66288=CARTESIAN_POINT('Ctrl Pts',(0.497752849465234,-0.123070995229855,
-3.75359018075938));
#66289=CARTESIAN_POINT('Ctrl Pts',(0.495899563082201,0.130337996110901,
-3.73968055081361));
#66290=CARTESIAN_POINT('Ctrl Pts',(0.372913069708243,0.351909382815266,
-3.72577092086785));
#66291=CARTESIAN_POINT('Ctrl Pts',(0.158835236222117,0.487519986810459,
-3.7118612909221));
#66292=CARTESIAN_POINT('Ctrl Pts',(-0.0940412229640735,0.504044263082503,
-3.69795166097634));
#66293=CARTESIAN_POINT('Ctrl Pts',(-0.323946266642341,0.397445828529313,
-3.68404203103058));
#66294=CARTESIAN_POINT('Ctrl Pts',(-0.463461312679454,0.208974308740659,
-3.67117116283877));
#66295=CARTESIAN_POINT('Ctrl Pts',(-0.49176101744956,0.0635165114976635,
-3.66293683796222));
#66296=CARTESIAN_POINT('Ctrl Pts',(-0.491826729621748,-1.27889840308929E-5,
-3.65933905640093));
#66297=CARTESIAN_POINT('Ctrl Pts',(-0.491838560105423,-1.18860308867142E-5,
-3.79981094359907));
#66298=CARTESIAN_POINT('Ctrl Pts',(-0.491853378270322,-0.0146196642867341,
-3.79898362079678));
#66299=CARTESIAN_POINT('Ctrl Pts',(-0.48764117239995,-0.111084912717674,
-3.79351975467924));
#66300=CARTESIAN_POINT('Ctrl Pts',(-0.426479195061789,-0.284639888869293,
-3.78341934524644));
#66301=CARTESIAN_POINT('Ctrl Pts',(-0.238074960618299,-0.454119677846183,
-3.76950971530068));
#66302=CARTESIAN_POINT('Ctrl Pts',(0.00848375782171881,-0.512671820463746,
-3.75560008535492));
#66303=CARTESIAN_POINT('Ctrl Pts',(0.252970151983937,-0.445993801941228,
-3.74169045540916));
#66304=CARTESIAN_POINT('Ctrl Pts',(0.435663618735166,-0.270373039805825,
-3.72778082546341));
#66305=CARTESIAN_POINT('Ctrl Pts',(0.511937691309605,-0.0287083528804346,
-3.71387119551764));
#66306=CARTESIAN_POINT('Ctrl Pts',(0.46316092958135,0.219968912808865,-3.69996156557189));
#66307=CARTESIAN_POINT('Ctrl Pts',(0.301248015490757,0.414914452000562,
-3.68605193562613));
#66308=CARTESIAN_POINT('Ctrl Pts',(0.0657493578520152,0.508508988358545,
-3.67214230568037));
#66309=CARTESIAN_POINT('Ctrl Pts',(-0.185809871592183,0.477890218488734,
-3.65823267573461));
#66310=CARTESIAN_POINT('Ctrl Pts',(-0.391981391059797,0.330537378169973,
-3.64432304578885));
#66311=CARTESIAN_POINT('Ctrl Pts',(-0.480421481164107,0.147851808358191,
-3.63318246841034));
#66312=CARTESIAN_POINT('Ctrl Pts',(-0.491805764853219,0.0329902947129077,
-3.62667843434708));
#66313=CARTESIAN_POINT('Ctrl Pts',(-0.491789055620677,7.06292780690287E-6,
-3.62481094359907));
#66314=CARTESIAN_POINT('Ctrl Pts',(-0.214786219406509,0.442446279878201,
-4.00597342437858));
#66315=CARTESIAN_POINT('Ctrl Pts',(-0.288440279010312,0.406690804635878,
-4.00133688106333));
#66316=CARTESIAN_POINT('Ctrl Pts',(-0.417471723369089,0.297721387833798,
-3.99206379443282));
#66317=CARTESIAN_POINT('Ctrl Pts',(-0.509054350485474,0.0613839821133976,
-3.97815416448707));
#66318=CARTESIAN_POINT('Ctrl Pts',(-0.476283132556506,-0.189881432885139,
-3.9642445345413));
#66319=CARTESIAN_POINT('Ctrl Pts',(-0.327174291768812,-0.394797097600903,
-3.95033490459555));
#66320=CARTESIAN_POINT('Ctrl Pts',(-0.0981447036446028,-0.503259303300383,
-3.93642527464979));
#66321=CARTESIAN_POINT('Ctrl Pts',(0.154857629827177,-0.488798982873136,
-3.92251564470403));
#66322=CARTESIAN_POINT('Ctrl Pts',(0.37003347141403,-0.354935592235777,
-3.90860601475827));
#66323=CARTESIAN_POINT('Ctrl Pts',(0.494821102216335,-0.134374424279909,
-3.89469638481251));
#66324=CARTESIAN_POINT('Ctrl Pts',(0.498739099375933,0.119011467407269,
-3.88078675486675));
#66325=CARTESIAN_POINT('Ctrl Pts',(0.380830207075808,0.343325891736714,
-3.86687712492099));
#66326=CARTESIAN_POINT('Ctrl Pts',(0.169896094203756,0.483776521506451,
-3.85296749497524));
#66327=CARTESIAN_POINT('Ctrl Pts',(-0.0825384944710284,0.506055083932911,
-3.83905786502947));
#66328=CARTESIAN_POINT('Ctrl Pts',(-0.314811425572855,0.404719832155649,
-3.82514823508372));
#66329=CARTESIAN_POINT('Ctrl Pts',(-0.47018548870497,0.204523773912369,
-3.81123860513796));
#66330=CARTESIAN_POINT('Ctrl Pts',(-0.510707510476629,-0.0456312120848563,
-3.7973289751922));
#66331=CARTESIAN_POINT('Ctrl Pts',(-0.426479195061789,-0.284639888869293,
-3.78341934524644));
#66332=CARTESIAN_POINT('Ctrl Pts',(-0.238074960618299,-0.454119677846183,
-3.76950971530068));
#66333=CARTESIAN_POINT('Ctrl Pts',(0.00848375782171881,-0.512671820463746,
-3.75560008535492));
#66334=CARTESIAN_POINT('Ctrl Pts',(0.252970151983937,-0.445993801941228,
-3.74169045540916));
#66335=CARTESIAN_POINT('Ctrl Pts',(0.435663618735166,-0.270373039805825,
-3.72778082546341));
#66336=CARTESIAN_POINT('Ctrl Pts',(0.511937691309605,-0.0287083528804346,
-3.71387119551764));
#66337=CARTESIAN_POINT('Ctrl Pts',(0.46316092958135,0.219968912808865,-3.69996156557189));
#66338=CARTESIAN_POINT('Ctrl Pts',(0.301248015490757,0.414914452000562,
-3.68605193562613));
#66339=CARTESIAN_POINT('Ctrl Pts',(0.0657493578520152,0.508508988358545,
-3.67214230568037));
#66340=CARTESIAN_POINT('Ctrl Pts',(-0.185809871592183,0.477890218488734,
-3.65823267573461));
#66341=CARTESIAN_POINT('Ctrl Pts',(-0.391981391059797,0.330537378169973,
-3.64432304578885));
#66342=CARTESIAN_POINT('Ctrl Pts',(-0.502403758224836,0.102444292311302,
-3.63041341584309));
#66343=CARTESIAN_POINT('Ctrl Pts',(-0.490104141488973,-0.15067282369779,
-3.61650378589733));
#66344=CARTESIAN_POINT('Ctrl Pts',(-0.358086963773074,-0.366985143679068,
-3.60259415595158));
#66345=CARTESIAN_POINT('Ctrl Pts',(-0.13860001322218,-0.493654135646059,
-3.58868452600581));
#66346=CARTESIAN_POINT('Ctrl Pts',(0.114742712316349,-0.499738410846886,
-3.57477489606006));
#66347=CARTESIAN_POINT('Ctrl Pts',(0.340057277111318,-0.383751765584462,
-3.5608652661143));
#66348=CARTESIAN_POINT('Ctrl Pts',(0.482306174096344,-0.174026215651783,
-3.54695563616854));
#66349=CARTESIAN_POINT('Ctrl Pts',(0.506742316769786,0.0782086548939713,
-3.53304600622278));
#66350=CARTESIAN_POINT('Ctrl Pts',(0.407396697418865,0.311339525659273,
-3.51913637627702));
#66351=CARTESIAN_POINT('Ctrl Pts',(0.208536434469852,0.46841960335167,-3.50522674633126));
#66352=CARTESIAN_POINT('Ctrl Pts',(-0.041262947733106,0.511078994334449,
-3.4913171163855));
#66353=CARTESIAN_POINT('Ctrl Pts',(-0.280983044651029,0.428897304636174,
-3.47740748643975));
#66354=CARTESIAN_POINT('Ctrl Pts',(-0.452067515107786,0.24194902580876,
-3.46349785649398));
#66355=CARTESIAN_POINT('Ctrl Pts',(-0.512725617522656,-0.00410005384696384,
-3.44958822654823));
#66356=CARTESIAN_POINT('Ctrl Pts',(-0.448140419207187,-0.24914761483575,
-3.43567859660246));
#66357=CARTESIAN_POINT('Ctrl Pts',(-0.274088123141906,-0.433335978264076,
-3.42176896665671));
#66358=CARTESIAN_POINT('Ctrl Pts',(-0.0330844205931006,-0.511673519365186,
-3.40785933671095));
#66359=CARTESIAN_POINT('Ctrl Pts',(0.216000801380951,-0.4650247553715,-3.39394970676519));
#66360=CARTESIAN_POINT('Ctrl Pts',(0.412323585901499,-0.304784562953681,
-3.38004007681943));
#66361=CARTESIAN_POINT('Ctrl Pts',(0.50792823756029,-0.0700947558269063,
-3.36613044687367));
#66362=CARTESIAN_POINT('Ctrl Pts',(0.479461442753112,0.18171707189651,-3.35222081692791));
#66363=CARTESIAN_POINT('Ctrl Pts',(0.33387677512836,0.38914093633981,-3.33831118698215));
#66364=CARTESIAN_POINT('Ctrl Pts',(0.106736148672607,0.501509485326126,
-3.3244015570364));
#66365=CARTESIAN_POINT('Ctrl Pts',(-0.146476878127779,0.491374494127927,
-3.31049192709063));
#66366=CARTESIAN_POINT('Ctrl Pts',(-0.363910051005443,0.361211633371286,
-3.29658229714488));
#66367=CARTESIAN_POINT('Ctrl Pts',(-0.492451047640611,0.142815737869471,
-3.28267266719911));
#66368=CARTESIAN_POINT('Ctrl Pts',(-0.500701205381039,-0.110465706151326,
-3.26876303725336));
#66369=CARTESIAN_POINT('Ctrl Pts',(-0.386645261186138,-0.336763732174116,
-3.2548534073076));
#66370=CARTESIAN_POINT('Ctrl Pts',(-0.178143619199366,-0.480800603414854,
-3.24094377736184));
#66371=CARTESIAN_POINT('Ctrl Pts',(0.0738731000725598,-0.507392485548619,
-3.22703414741608));
#66372=CARTESIAN_POINT('Ctrl Pts',(0.307844863968601,-0.410043789166097,
-3.21312451747032));
#66373=CARTESIAN_POINT('Ctrl Pts',(0.466619474536125,-0.212533845043952,
-3.19921488752456));
#66374=CARTESIAN_POINT('Ctrl Pts',(0.511413115207255,0.0368916643640206,
-3.18530525757881));
#66375=CARTESIAN_POINT('Ctrl Pts',(0.431284059612851,0.277305660290942,
-3.17139562763304));
#66376=CARTESIAN_POINT('Ctrl Pts',(0.245805403116349,0.449982303101295,
-3.15748599768729));
#66377=CARTESIAN_POINT('Ctrl Pts',(0.000283949904538727,0.5127419318507,
-3.14357636774152));
#66378=CARTESIAN_POINT('Ctrl Pts',(-0.24530686364752,0.450254274774769,
-3.12966673779577));
#66379=CARTESIAN_POINT('Ctrl Pts',(-0.430976658539604,0.277783169215801,
-3.11575710785));
#66380=CARTESIAN_POINT('Ctrl Pts',(-0.51137194127832,0.0374580696082845,
-3.10184747790425));
#66381=CARTESIAN_POINT('Ctrl Pts',(-0.466854585292198,-0.212016899083981,
-3.08793784795849));
#66382=CARTESIAN_POINT('Ctrl Pts',(-0.308298828990521,-0.409702576692666,
-3.07402821801273));
#66383=CARTESIAN_POINT('Ctrl Pts',(-0.0744350294889845,-0.507310354408927,
-3.06011858806697));
#66384=CARTESIAN_POINT('Ctrl Pts',(0.177610987683289,-0.480997615752618,
-3.04620895812121));
#66385=CARTESIAN_POINT('Ctrl Pts',(0.386272033277762,-0.337191763857008,
-3.03229932817546));
#66386=CARTESIAN_POINT('Ctrl Pts',(0.500578549326249,-0.111020202035327,
-3.0183896982297));
#66387=CARTESIAN_POINT('Ctrl Pts',(0.492608924589448,0.142270224292942,
-3.00448006828394));
#66388=CARTESIAN_POINT('Ctrl Pts',(0.364309896412847,0.360808354505819,
-2.99057043833818));
#66389=CARTESIAN_POINT('Ctrl Pts',(0.147021021901026,0.491211958755805,
-2.97666080839242));
#66390=CARTESIAN_POINT('Ctrl Pts',(-0.10618062433576,0.501627395903777,
-2.96275117844666));
#66391=CARTESIAN_POINT('Ctrl Pts',(-0.333445567956295,0.389510490893173,
-2.9488415485009));
#66392=CARTESIAN_POINT('Ctrl Pts',(-0.479259883565437,0.1822479994688,-2.93493191855514));
#66393=CARTESIAN_POINT('Ctrl Pts',(-0.508005561146717,-0.0695321447213124,
-2.92102228860938));
#66394=CARTESIAN_POINT('Ctrl Pts',(-0.412660904457599,-0.304327697125603,
-2.90711265866362));
#66395=CARTESIAN_POINT('Ctrl Pts',(-0.216515718225303,-0.464785233271151,
-2.89320302871787));
#66396=CARTESIAN_POINT('Ctrl Pts',(0.0325176840114124,-0.511709848969189,
-2.87929339877211));
#66397=CARTESIAN_POINT('Ctrl Pts',(0.273608003362249,-0.43363928535323,
-2.86538376882635));
#66398=CARTESIAN_POINT('Ctrl Pts',(0.447864194914093,-0.249643810697336,
-2.85147413888059));
#66399=CARTESIAN_POINT('Ctrl Pts',(0.51272076192407,-0.00466793289774274,
-2.83756450893483));
#66400=CARTESIAN_POINT('Ctrl Pts',(0.452335214279015,0.241448179178668,
-2.82365487898907));
#66401=CARTESIAN_POINT('Ctrl Pts',(0.281457907812556,0.428585832051545,
-2.80974524904331));
#66402=CARTESIAN_POINT('Ctrl Pts',(0.0418289802326045,0.511032979090623,
-2.79583561909755));
#66403=CARTESIAN_POINT('Ctrl Pts',(-0.208017497185851,0.468650285575578,
-2.78192598915179));
#66404=CARTESIAN_POINT('Ctrl Pts',(-0.40705161597261,0.311790556687697,
-2.76801635920603));
#66405=CARTESIAN_POINT('Ctrl Pts',(-0.506655384081065,0.0787698615411085,
-2.75410672926028));
#66406=CARTESIAN_POINT('Ctrl Pts',(-0.482498625181512,-0.17349191913022,
-2.74019709931452));
#66407=CARTESIAN_POINT('Ctrl Pts',(-0.340482102013575,-0.383374891606055,
-2.72628746936876));
#66408=CARTESIAN_POINT('Ctrl Pts',(-0.115296139210803,-0.499611018281843,
-2.712377839423));
#66409=CARTESIAN_POINT('Ctrl Pts',(0.138053169722395,-0.493807342629832,
-2.69846820947724));
#66410=CARTESIAN_POINT('Ctrl Pts',(0.357680280931475,-0.367381526397719,
-2.68455857953148));
#66411=CARTESIAN_POINT('Ctrl Pts',(0.489936959575747,-0.151215557887439,
-2.67064894958572));
#66412=CARTESIAN_POINT('Ctrl Pts',(0.502516914705533,0.101887780132694,
-2.65673931963996));
#66413=CARTESIAN_POINT('Ctrl Pts',(0.392347245241488,0.330103027033912,
-2.64282968969421));
#66414=CARTESIAN_POINT('Ctrl Pts',(0.186339056407328,0.477684127183188,
-2.62892005974845));
#66415=CARTESIAN_POINT('Ctrl Pts',(-0.0651861061879488,0.508581498744882,
-2.61501042980269));
#66416=CARTESIAN_POINT('Ctrl Pts',(-0.300788282254515,0.415247851967851,
-2.60110079985693));
#66417=CARTESIAN_POINT('Ctrl Pts',(-0.46291701364987,0.220481762917078,
-2.58719116991117));
#66418=CARTESIAN_POINT('Ctrl Pts',(-0.511969173927383,-0.028141326437292,
-2.57328153996541));
#66419=CARTESIAN_POINT('Ctrl Pts',(-0.435962809677364,-0.269890344183994,
-2.55937191001965));
#66420=CARTESIAN_POINT('Ctrl Pts',(-0.253463967943028,-0.445713345391533,
-2.54546228007389));
#66421=CARTESIAN_POINT('Ctrl Pts',(-0.00905157463938524,-0.512662109290402,
-2.53155265012813));
#66422=CARTESIAN_POINT('Ctrl Pts',(0.237571843520245,-0.454383085591805,
-2.51764302018238));
#66423=CARTESIAN_POINT('Ctrl Pts',(0.426163673582462,-0.285112070288575,
-2.50373339023661));
#66424=CARTESIAN_POINT('Ctrl Pts',(0.510656657582095,-0.0461968329284603,
-2.48982376029085));
#66425=CARTESIAN_POINT('Ctrl Pts',(0.470411724946076,0.204002888064838,
-2.4759141303451));
#66426=CARTESIAN_POINT('Ctrl Pts',(0.315259490780706,0.404370897541139,
-2.46200450039934));
#66427=CARTESIAN_POINT('Ctrl Pts',(0.083098935083214,0.505963374458638,
-2.44809487045358));
#66428=CARTESIAN_POINT('Ctrl Pts',(-0.169360167363873,0.48396436130775,
-2.43418524050782));
#66429=CARTESIAN_POINT('Ctrl Pts',(-0.380449723121679,0.343747549056243,
-2.42027561056206));
#66430=CARTESIAN_POINT('Ctrl Pts',(-0.498606962924748,0.119563647604509,
-2.4063659806163));
#66431=CARTESIAN_POINT('Ctrl Pts',(-0.494969660638129,-0.133826022706017,
-2.39245635067054));
#66432=CARTESIAN_POINT('Ctrl Pts',(-0.370426298772862,-0.354526058961786,
-2.37854672072478));
#66433=CARTESIAN_POINT('Ctrl Pts',(-0.155399039185073,-0.488626143309885,
-2.36463709077902));
#66434=CARTESIAN_POINT('Ctrl Pts',(0.0975874873726366,-0.503369696757594,
-2.35072746083327));
#66435=CARTESIAN_POINT('Ctrl Pts',(0.326736353765087,-0.395155316848746,
-2.3368178308875));
#66436=CARTESIAN_POINT('Ctrl Pts',(0.476073449464557,-0.190416490936197,
-2.32290820094175));
#66437=CARTESIAN_POINT('Ctrl Pts',(0.509120256238909,0.060835302191775,
-2.30899857099599));
#66438=CARTESIAN_POINT('Ctrl Pts',(0.417804442576766,0.297226878106026,
-2.29508894105023));
#66439=CARTESIAN_POINT('Ctrl Pts',(0.224431689179598,0.461014952249414,
-2.28117931110447));
#66440=CARTESIAN_POINT('Ctrl Pts',(-0.0237629115774706,0.512191071123753,
-2.26726968115871));
#66441=CARTESIAN_POINT('Ctrl Pts',(-0.266152954537513,0.438254462722844,
-2.25336005121295));
#66442=CARTESIAN_POINT('Ctrl Pts',(-0.443529911772546,0.257265595578916,
-2.23945042126719));
#66443=CARTESIAN_POINT('Ctrl Pts',(-0.512565978237527,0.013434554661145,
-2.22554079132144));
#66444=CARTESIAN_POINT('Ctrl Pts',(-0.456397739002481,-0.233678140053707,
-2.21163116137568));
#66445=CARTESIAN_POINT('Ctrl Pts',(-0.288745389504487,-0.423710360205458,
-2.19772153142992));
#66446=CARTESIAN_POINT('Ctrl Pts',(-0.0505613083818057,-0.510243004263906,
-2.18381190148416));
#66447=CARTESIAN_POINT('Ctrl Pts',(0.199973365210935,-0.472138774632788,
-2.1699022715384));
#66448=CARTESIAN_POINT('Ctrl Pts',(0.401660617373509,-0.318705377671398,
-2.15599264159264));
#66449=CARTESIAN_POINT('Ctrl Pts',(0.505234376131355,-0.0874219336362221,
-2.14208301164688));
#66450=CARTESIAN_POINT('Ctrl Pts',(0.485394716977961,0.165216034438012,
-2.12817338170112));
#66451=CARTESIAN_POINT('Ctrl Pts',(0.346987866262887,0.377496741670528,
-2.11426375175536));
#66452=CARTESIAN_POINT('Ctrl Pts',(0.123822415238128,0.49756645665693,-2.10035412180961));
#66453=CARTESIAN_POINT('Ctrl Pts',(-0.129589092271495,0.496095793642505,
-2.08644449186384));
#66454=CARTESIAN_POINT('Ctrl Pts',(-0.351345919187724,0.37344399094867,
-2.07253486191809));
#66455=CARTESIAN_POINT('Ctrl Pts',(-0.487279605786099,0.159571159958436,
-2.05862523197233));
#66456=CARTESIAN_POINT('Ctrl Pts',(-0.504185679716899,-0.0932800604306441,
-2.04471560202657));
#66457=CARTESIAN_POINT('Ctrl Pts',(-0.397934500429466,-0.32334579427215,
-2.03080597208081));
#66458=CARTESIAN_POINT('Ctrl Pts',(-0.194480004972519,-0.474427968158946,
-2.01689634213505));
#66459=CARTESIAN_POINT('Ctrl Pts',(0.0564800508004891,-0.509621794242663,
-2.00298671218929));
#66460=CARTESIAN_POINT('Ctrl Pts',(0.293643745038357,-0.420330489383515,
-1.98907708224353));
#66461=CARTESIAN_POINT('Ctrl Pts',(0.459079188120922,-0.228365208251544,
-1.97516745229777));
#66462=CARTESIAN_POINT('Ctrl Pts',(0.512375524336397,0.0193827595181383,
-1.96125782235201));
#66463=CARTESIAN_POINT('Ctrl Pts',(0.440514076957236,0.262396107646534,
-1.94734819240626));
#66464=CARTESIAN_POINT('Ctrl Pts',(0.261048415685123,0.441314053678131,
-1.9334385624605));
#66465=CARTESIAN_POINT('Ctrl Pts',(0.0178165525430863,0.512432375793154,
-1.91952893251474));
#66466=CARTESIAN_POINT('Ctrl Pts',(-0.229767353430185,0.458379027228804,
-1.90561930256898));
#66467=CARTESIAN_POINT('Ctrl Pts',(-0.421226071271232,0.292357599844676,
-1.89170967262322));
#66468=CARTESIAN_POINT('Ctrl Pts',(-0.50979204937639,0.0549220875254831,
-1.87780004267746));
#66469=CARTESIAN_POINT('Ctrl Pts',(-0.473831308378887,-0.195929223204422,
-1.8638904127317));
#66470=CARTESIAN_POINT('Ctrl Pts',(-0.322127965446493,-0.398920973606101,
-1.84998078278594));
#66471=CARTESIAN_POINT('Ctrl Pts',(-0.0917385411651713,-0.504468442393003,
-1.83607115284018));
#66472=CARTESIAN_POINT('Ctrl Pts',(0.161059823311547,-0.48678958762528,
-1.82216152289443));
#66473=CARTESIAN_POINT('Ctrl Pts',(0.37451616313179,-0.350202816748494,
-1.80825189294867));
#66474=CARTESIAN_POINT('Ctrl Pts',(0.496489575545123,-0.128072130772313,
-1.79434226300291));
#66475=CARTESIAN_POINT('Ctrl Pts',(0.497185659316439,0.125342688161754,
-1.78043263305715));
#66476=CARTESIAN_POINT('Ctrl Pts',(0.376434382315248,0.348140094094997,
-1.76652300311139));
#66477=CARTESIAN_POINT('Ctrl Pts',(0.163731615202558,0.485897445443685,
-1.75261337316563));
#66478=CARTESIAN_POINT('Ctrl Pts',(-0.088965814203307,0.504964803930609,
-1.73870374321987));
#66479=CARTESIAN_POINT('Ctrl Pts',(-0.319931596423644,0.40068459281005,
-1.72479411327411));
#66480=CARTESIAN_POINT('Ctrl Pts',(-0.472747803560086,0.198529301451072,
-1.71088448332836));
#66481=CARTESIAN_POINT('Ctrl Pts',(-0.510086076090958,-0.0521206704069183,
-1.69697485338259));
#66482=CARTESIAN_POINT('Ctrl Pts',(-0.422825807720183,-0.290039144998243,
-1.68306522343684));
#66483=CARTESIAN_POINT('Ctrl Pts',(-0.232282032571033,-0.457109862779405,
-1.66915559349108));
#66484=CARTESIAN_POINT('Ctrl Pts',(0.0150011904725086,-0.51252252008077,
-1.65524596354532));
#66485=CARTESIAN_POINT('Ctrl Pts',(0.25862007815723,-0.442741487190307,
-1.64133633359956));
#66486=CARTESIAN_POINT('Ctrl Pts',(0.439065933099701,-0.264812151716694,
-1.6274267036538));
#66487=CARTESIAN_POINT('Ctrl Pts',(0.512261311724355,-0.0221972479370705,
-1.61351707370804));
#66488=CARTESIAN_POINT('Ctrl Pts',(0.46032680542771,0.225839769549687,-1.59960744376228));
#66489=CARTESIAN_POINT('Ctrl Pts',(0.295948437236704,0.418710988394965,
-1.58569781381652));
#66490=CARTESIAN_POINT('Ctrl Pts',(0.0592788515625552,0.509303825886828,
-1.57178818387076));
#66491=CARTESIAN_POINT('Ctrl Pts',(-0.191870757694326,0.475489202450847,
-1.55787855392501));
#66492=CARTESIAN_POINT('Ctrl Pts',(-0.396152166521947,0.325527003895996,
-1.54396892397925));
#66493=CARTESIAN_POINT('Ctrl Pts',(-0.503665629237551,0.0960484421023013,
-1.53005929403349));
#66494=CARTESIAN_POINT('Ctrl Pts',(-0.488148871276991,-0.15689183782637,
-1.51614966408773));
#66495=CARTESIAN_POINT('Ctrl Pts',(-0.353392165482507,-0.371508205402143,
-1.50224003414197));
#66496=CARTESIAN_POINT('Ctrl Pts',(-0.132312483529502,-0.495376398315253,
-1.48833040419621));
#66497=CARTESIAN_POINT('Ctrl Pts',(0.121087120812267,-0.498239177984762,
-1.47442077425045));
#66498=CARTESIAN_POINT('Ctrl Pts',(0.344908818047041,-0.379397254258554,
-1.46051114430469));
#66499=CARTESIAN_POINT('Ctrl Pts',(0.484479763326162,-0.167880100765288,
-1.44660151435893));
#66500=CARTESIAN_POINT('Ctrl Pts',(0.505707012440461,0.0846450640857451,
-1.43269188441317));
#66501=CARTESIAN_POINT('Ctrl Pts',(0.40340539294362,0.316494009816205,-1.41878225446742));
#66502=CARTESIAN_POINT('Ctrl Pts',(0.202564084346017,0.47103307849725,-1.40487262452166));
#66503=CARTESIAN_POINT('Ctrl Pts',(-0.0477574797057481,0.510513067842236,
-1.3909629945759));
#66504=CARTESIAN_POINT('Ctrl Pts',(-0.28641334150177,0.425290215165276,
-1.37705336463014));
#66505=CARTESIAN_POINT('Ctrl Pts',(-0.455107120193369,0.236181875796673,
-1.36314373468438));
#66506=CARTESIAN_POINT('Ctrl Pts',(-0.512632047610675,-0.0106185247573672,
-1.34923410473862));
#66507=CARTESIAN_POINT('Ctrl Pts',(-0.444936530586125,-0.254825142118117,
-1.33532447479286));
#66508=CARTESIAN_POINT('Ctrl Pts',(-0.268556528523827,-0.436785714387234,
-1.3214148448471));
#66509=CARTESIAN_POINT('Ctrl Pts',(-0.0265763205901719,-0.512052798536855,
-1.30750521490134));
#66510=CARTESIAN_POINT('Ctrl Pts',(0.221895675540188,-0.462240931205903,
-1.29359558495558));
#66511=CARTESIAN_POINT('Ctrl Pts',(0.416165295443046,-0.299517639170616,
-1.27968595500983));
#66512=CARTESIAN_POINT('Ctrl Pts',(0.508778369487043,-0.063631281989616,
-1.26577632506407));
#66513=CARTESIAN_POINT('Ctrl Pts',(0.477112335647494,0.187798265376785,
-1.25186669511831));
#66514=CARTESIAN_POINT('Ctrl Pts',(0.328902244531517,0.393354398536063,
-1.23795706517255));
#66515=CARTESIAN_POINT('Ctrl Pts',(0.100351321370171,0.502825995355051,
-1.22404743522679));
#66516=CARTESIAN_POINT('Ctrl Pts',(-0.15271238268513,0.489472468561989,
-1.21013780528103));
#66517=CARTESIAN_POINT('Ctrl Pts',(-0.368473088379839,0.356555679305995,
-1.19622817533527));
#66518=CARTESIAN_POINT('Ctrl Pts',(-0.494227006346698,0.136543163516585,
-1.18231854538951));
#66519=CARTESIAN_POINT('Ctrl Pts',(-0.499256272629466,-0.116822701328421,
-1.16840891544375));
#66520=CARTESIAN_POINT('Ctrl Pts',(-0.382332390176345,-0.341652327267911,
-1.15449928549799));
#66521=CARTESIAN_POINT('Ctrl Pts',(-0.172016313369507,-0.483026663073893,
-1.14058965555223));
#66522=CARTESIAN_POINT('Ctrl Pts',(0.0803181259485588,-0.506412250986929,
-1.12668002560648));
#66523=CARTESIAN_POINT('Ctrl Pts',(0.313033285756316,-0.406096701924727,
-1.11277039566072));
#66524=CARTESIAN_POINT('Ctrl Pts',(0.469283918326265,-0.206584058692545,
-1.09886076571496));
#66525=CARTESIAN_POINT('Ctrl Pts',(0.510902738281055,0.0433907976701933,
-1.0849511357692));
#66526=CARTESIAN_POINT('Ctrl Pts',(0.427723531557066,0.282766599615103,
-1.07104150582344));
#66527=CARTESIAN_POINT('Ctrl Pts',(0.240064452828482,0.45307110677431,-1.05713187587768));
#66528=CARTESIAN_POINT('Ctrl Pts',(-0.0062350827696745,0.512704098919047,
-1.04322224593192));
#66529=CARTESIAN_POINT('Ctrl Pts',(-0.251011576959888,0.447099046674948,
-1.02931261598616));
#66530=CARTESIAN_POINT('Ctrl Pts',(-0.434473564237258,0.27228127237199,
-1.0154029860404));
#66531=CARTESIAN_POINT('Ctrl Pts',(-0.511806851474115,0.0309534503680939,
-1.00149335609465));
#66532=CARTESIAN_POINT('Ctrl Pts',(-0.464121264630259,-0.217935359736655,
-0.987583726148886));
#66533=CARTESIAN_POINT('Ctrl Pts',(-0.30306494471812,-0.413589178519626,
-0.973674096203129));
#66534=CARTESIAN_POINT('Ctrl Pts',(-0.0679790606200691,-0.508215718590787,
-0.959764466257369));
#66535=CARTESIAN_POINT('Ctrl Pts',(0.183712043973384,-0.478700589308868,
-0.94585483631161));
#66536=CARTESIAN_POINT('Ctrl Pts',(0.390527874180675,-0.332253440604396,
-0.931945206365851));
#66537=CARTESIAN_POINT('Ctrl Pts',(0.501949602127359,-0.104646864404638,
-0.918035576420092));
#66538=CARTESIAN_POINT('Ctrl Pts',(0.490760282718032,0.148521763428982,
-0.904125946474333));
#66539=CARTESIAN_POINT('Ctrl Pts',(0.359693126948704,0.365411033948621,
-0.890216316528574));
#66540=CARTESIAN_POINT('Ctrl Pts',(0.140763861447594,0.493041483666333,
-0.876306686582815));
#66541=CARTESIAN_POINT('Ctrl Pts',(-0.112549741462726,0.500236868895336,
-0.862397056637057));
#66542=CARTESIAN_POINT('Ctrl Pts',(-0.338370859824982,0.385239575494054,
-0.848487426691298));
#66543=CARTESIAN_POINT('Ctrl Pts',(-0.481538250916493,0.176139950635345,
-0.834577796745538));
#66544=CARTESIAN_POINT('Ctrl Pts',(-0.507080468013198,-0.0759853161147112,
-0.820668166799779));
#66545=CARTESIAN_POINT('Ctrl Pts',(-0.408758323003886,-0.309549677241936,
-0.80675853685402));
#66546=CARTESIAN_POINT('Ctrl Pts',(-0.210588930608419,-0.467500450920358,
-0.792848906908262));
#66547=CARTESIAN_POINT('Ctrl Pts',(0.0390209435287369,-0.511255058920363,
-0.778939276962502));
#66548=CARTESIAN_POINT('Ctrl Pts',(0.279099185935138,-0.430125579006736,
-0.765029647016744));
#66549=CARTESIAN_POINT('Ctrl Pts',(0.45100197136601,-0.243929479828719,
-0.751120017070984));
#66550=CARTESIAN_POINT('Ctrl Pts',(0.512738668738538,0.00185118496315108,
-0.737210387125225));
#66551=CARTESIAN_POINT('Ctrl Pts',(0.449228877364958,0.247179661475123,
-0.723300757179467));
#66552=CARTESIAN_POINT('Ctrl Pts',(0.27598611096193,0.432129651680657,-0.709391127233707));
#66553=CARTESIAN_POINT('Ctrl Pts',(0.0353283172785953,0.511523488516217,
-0.695481497287949));
#66554=CARTESIAN_POINT('Ctrl Pts',(-0.213959111659945,0.46596766823807,
-0.681571867342189));
#66555=CARTESIAN_POINT('Ctrl Pts',(-0.41098282595302,0.306590094551677,
-0.667662237396431));
#66556=CARTESIAN_POINT('Ctrl Pts',(-0.507615914330933,0.0723218696073868,
-0.653752607450671));
#66557=CARTESIAN_POINT('Ctrl Pts',(-0.480253847324892,-0.179612392209383,
-0.639842977504913));
#66558=CARTESIAN_POINT('Ctrl Pts',(-0.33558034712377,-0.387672800090266,
-0.625933347559152));
#66559=CARTESIAN_POINT('Ctrl Pts',(-0.108934757177873,-0.501036513623642,
-0.612023717613395));
#66560=CARTESIAN_POINT('Ctrl Pts',(0.144320286415244,-0.49201221959882,
-0.598114087667635));
#66561=CARTESIAN_POINT('Ctrl Pts',(0.362322265961503,-0.362804279045959,
-0.584204457721877));
#66562=CARTESIAN_POINT('Ctrl Pts',(0.491819916942383,-0.144974268766304,
-0.570294827776118));
#66563=CARTESIAN_POINT('Ctrl Pts',(0.501180895095398,0.108268553592046,
-0.55638519783036));
#66564=CARTESIAN_POINT('Ctrl Pts',(0.388118597680438,0.33506465561158,-0.542475567884599));
#66565=CARTESIAN_POINT('Ctrl Pts',(0.180250711102229,0.480014635665076,
-0.528565937938842));
#66566=CARTESIAN_POINT('Ctrl Pts',(-0.0716469513364315,0.507711614668931,
-0.514656307993081));
#66567=CARTESIAN_POINT('Ctrl Pts',(-0.306043438944004,0.411390061601957,
-0.500746678047323));
#66568=CARTESIAN_POINT('Ctrl Pts',(-0.46568280666081,0.214578407315484,
-0.486837048101564));
#66569=CARTESIAN_POINT('Ctrl Pts',(-0.511570004003579,-0.0346482367417505,
-0.472927418155805));
#66570=CARTESIAN_POINT('Ctrl Pts',(-0.432496181911419,-0.275411368569959,
-0.459017788210046));
#66571=CARTESIAN_POINT('Ctrl Pts',(-0.247776674242662,-0.448899865233663,
-0.445108158264288));
#66572=CARTESIAN_POINT('Ctrl Pts',(-0.0025328481751963,-0.512735754541854,
-0.431198528318528));
#66573=CARTESIAN_POINT('Ctrl Pts',(0.243329675797957,-0.451325866953922,
-0.41728889837277));
#66574=CARTESIAN_POINT('Ctrl Pts',(0.429754148070265,-0.279670773449364,
-0.40337926842701));
#66575=CARTESIAN_POINT('Ctrl Pts',(0.511202730378688,-0.0397006014952209,
-0.389469638481251));
#66576=CARTESIAN_POINT('Ctrl Pts',(0.467780007046806,0.209967221996417,
-0.375560008535492));
#66577=CARTESIAN_POINT('Ctrl Pts',(0.310092830963972,0.408346428280455,
-0.361650378589733));
#66578=CARTESIAN_POINT('Ctrl Pts',(0.0766593914673165,0.506979000559367,
-0.347740748643974));
#66579=CARTESIAN_POINT('Ctrl Pts',(-0.175499609789847,0.481771996138208,
-0.333831118698215));
#66580=CARTESIAN_POINT('Ctrl Pts',(-0.384789384990357,0.338882720885541,
-0.319921488752456));
#66581=CARTESIAN_POINT('Ctrl Pts',(-0.500086796588008,0.113214686199793,
-0.306011858806698));
#66582=CARTESIAN_POINT('Ctrl Pts',(-0.493228187695886,-0.140108258752822,
-0.292102228860939));
#66583=CARTESIAN_POINT('Ctrl Pts',(-0.365888908126138,-0.359207010306768,
-0.278192598915179));
#66584=CARTESIAN_POINT('Ctrl Pts',(-0.149174077725999,-0.490562395317217,
-0.26428296896942));
#66585=CARTESIAN_POINT('Ctrl Pts',(0.103979450806552,-0.502088282530429,
-0.250373339023661));
#66586=CARTESIAN_POINT('Ctrl Pts',(0.331733956110991,-0.390969245649164,
-0.236463709077902));
#66587=CARTESIAN_POINT('Ctrl Pts',(0.478455929130976,-0.184348295450463,
-0.222554079132143));
#66588=CARTESIAN_POINT('Ctrl Pts',(0.508305643980286,0.067303351115353,
-0.208644449186384));
#66589=CARTESIAN_POINT('Ctrl Pts',(0.413991726952782,0.302514822609971,
-0.194734819240625));
#66590=CARTESIAN_POINT('Ctrl Pts',(0.218552193979818,0.463831127370637,
-0.180825189294866));
#66591=CARTESIAN_POINT('Ctrl Pts',(-0.0302729907633189,0.511847533035115,
-0.166915559349108));
#66592=CARTESIAN_POINT('Ctrl Pts',(-0.271703429260484,0.434835201098837,
-0.153005929403349));
#66593=CARTESIAN_POINT('Ctrl Pts',(-0.446764918333941,0.251605688139759,
-0.13909629945759));
#66594=CARTESIAN_POINT('Ctrl Pts',(-0.51269540287887,0.006916826412533,
-0.12518666951183));
#66595=CARTESIAN_POINT('Ctrl Pts',(-0.453389771617352,-0.23946215586583,
-0.111277039566072));
#66596=CARTESIAN_POINT('Ctrl Pts',(-0.283335167309922,-0.427346729913706,
-0.0973674096203128));
#66597=CARTESIAN_POINT('Ctrl Pts',(-0.0440696378965106,-0.510845571762323,
-0.0834577796745537));
#66598=CARTESIAN_POINT('Ctrl Pts',(0.205959307621291,-0.469556250960448,
-0.0695481497287949));
#66599=CARTESIAN_POINT('Ctrl Pts',(0.405681497053104,-0.313576606935647,
-0.0556385197830361));
#66600=CARTESIAN_POINT('Ctrl Pts',(0.506302444914719,-0.0809840427845483,
-0.0417288898372769));
#66601=CARTESIAN_POINT('Ctrl Pts',(0.48325998950616,0.171359585523517,-0.0278192598915182));
#66602=CARTESIAN_POINT('Ctrl Pts',(0.342150143078732,0.381908292889331,
-0.0139096299457593));
#66603=CARTESIAN_POINT('Ctrl Pts',(0.192389430706698,0.459979903999379,
-0.00463654331525315));
#66604=CARTESIAN_POINT('Ctrl Pts',(0.112693552167563,0.478740006605732,
0.));
#66605=CARTESIAN_POINT('Ctrl Pts',(-0.229321473482477,0.472388001049917,
-3.98675728291905));
#66606=CARTESIAN_POINT('Ctrl Pts',(-0.30795993326347,0.43421284116167,-3.9821207396038));
#66607=CARTESIAN_POINT('Ctrl Pts',(-0.445723338325901,0.317869123698659,
-3.9728476529733));
#66608=CARTESIAN_POINT('Ctrl Pts',(-0.543503647759894,0.0655380278369941,
-3.95893802302754));
#66609=CARTESIAN_POINT('Ctrl Pts',(-0.508514699194888,-0.202731302299111,
-3.94502839308177));
#66610=CARTESIAN_POINT('Ctrl Pts',(-0.34931519760125,-0.421514249836929,
-3.93111876313602));
#66611=CARTESIAN_POINT('Ctrl Pts',(-0.104786462169088,-0.537316431638404,
-3.91720913319026));
#66612=CARTESIAN_POINT('Ctrl Pts',(0.165337329136378,-0.52187753617962,
-3.9032995032445));
#66613=CARTESIAN_POINT('Ctrl Pts',(0.395074791748627,-0.37895519194756,
-3.88938987329874));
#66614=CARTESIAN_POINT('Ctrl Pts',(0.528307191141123,-0.143467961116758,
-3.87548024335298));
#66615=CARTESIAN_POINT('Ctrl Pts',(0.53249033140134,0.127065344986093,-3.86157061340723));
#66616=CARTESIAN_POINT('Ctrl Pts',(0.406602176222368,0.366559826767745,
-3.84766098346146));
#66617=CARTESIAN_POINT('Ctrl Pts',(0.181393493350638,0.516515189171047,
-3.83375135351571));
#66618=CARTESIAN_POINT('Ctrl Pts',(-0.0881241320947979,0.540301411475365,
-3.81984172356994));
#66619=CARTESIAN_POINT('Ctrl Pts',(-0.336115697650287,0.432108486819904,
-3.80593209362419));
#66620=CARTESIAN_POINT('Ctrl Pts',(-0.502004408745765,0.21836453626019,
-3.79202246367843));
#66621=CARTESIAN_POINT('Ctrl Pts',(-0.545268682249171,-0.0487192186770869,
-3.77811283373267));
#66622=CARTESIAN_POINT('Ctrl Pts',(-0.455340373751309,-0.303902358855974,
-3.76420320378691));
#66623=CARTESIAN_POINT('Ctrl Pts',(-0.254186236524524,-0.484851374305249,
-3.75029357384116));
#66624=CARTESIAN_POINT('Ctrl Pts',(0.00905788020162857,-0.547365923226114,
-3.73638394389539));
#66625=CARTESIAN_POINT('Ctrl Pts',(0.270089431995863,-0.476175595007076,
-3.72247431394964));
#66626=CARTESIAN_POINT('Ctrl Pts',(0.465146336050408,-0.288670027572214,
-3.70856468400387));
#66627=CARTESIAN_POINT('Ctrl Pts',(0.546582113260003,-0.030651136753501,
-3.69465505405812));
#66628=CARTESIAN_POINT('Ctrl Pts',(0.494504475774067,0.234854895928853,
-3.68074542411236));
#66629=CARTESIAN_POINT('Ctrl Pts',(0.321634409260054,0.442993008419515,
-3.6668357941666));
#66630=CARTESIAN_POINT('Ctrl Pts',(0.0701988221814853,0.542921379275098,
-3.65292616422084));
#66631=CARTESIAN_POINT('Ctrl Pts',(-0.198384205741171,0.510230541649818,
-3.63901653427508));
#66632=CARTESIAN_POINT('Ctrl Pts',(-0.418507995642945,0.352905874559456,
-3.62510690432932));
#66633=CARTESIAN_POINT('Ctrl Pts',(-0.536402989156401,0.109377017425102,
-3.61119727438356));
#66634=CARTESIAN_POINT('Ctrl Pts',(-0.523271018953975,-0.160869324110351,
-3.59728764443781));
#66635=CARTESIAN_POINT('Ctrl Pts',(-0.382319826636045,-0.391820174158306,
-3.58337801449204));
#66636=CARTESIAN_POINT('Ctrl Pts',(-0.147979508855949,-0.527061252299515,
-3.56946838454629));
#66637=CARTESIAN_POINT('Ctrl Pts',(0.122507709910199,-0.533557269399598,
-3.55555875460053));
#66638=CARTESIAN_POINT('Ctrl Pts',(0.363070014785332,-0.409721445717036,
-3.54164912465477));
#66639=CARTESIAN_POINT('Ctrl Pts',(0.514945338760956,-0.18580311301218,
-3.52773949470901));
#66640=CARTESIAN_POINT('Ctrl Pts',(0.541035151503999,0.0835012787548714,
-3.51382986476325));
#66641=CARTESIAN_POINT('Ctrl Pts',(0.43496650391323,0.332408843429535,-3.49992023481749));
#66642=CARTESIAN_POINT('Ctrl Pts',(0.222648746085987,0.500119020417133,
-3.48601060487173));
#66643=CARTESIAN_POINT('Ctrl Pts',(-0.0440553402379942,0.545665305579503,
-3.47210097492598));
#66644=CARTESIAN_POINT('Ctrl Pts',(-0.299998044572006,0.45792212435045,
-3.45819134498021));
#66645=CARTESIAN_POINT('Ctrl Pts',(-0.482660335307052,0.258322471802089,
-3.44428171503446));
#66646=CARTESIAN_POINT('Ctrl Pts',(-0.547423360899966,-0.00437751729203636,
-3.43037208508869));
#66647=CARTESIAN_POINT('Ctrl Pts',(-0.478467480565623,-0.266008211824075,
-3.41646245514294));
#66648=CARTESIAN_POINT('Ctrl Pts',(-0.292636522196936,-0.462661176881245,
-3.40255282519718));
#66649=CARTESIAN_POINT('Ctrl Pts',(-0.0353233466313068,-0.546300063975303,
-3.38864319525142));
#66650=CARTESIAN_POINT('Ctrl Pts',(0.230618250011315,-0.496494432474701,
-3.37473356530566));
#66651=CARTESIAN_POINT('Ctrl Pts',(0.440226810322289,-0.325410285931654,
-3.3608239353599));
#66652=CARTESIAN_POINT('Ctrl Pts',(0.542301327257096,-0.0748382868046036,
-3.34691430541414));
#66653=CARTESIAN_POINT('Ctrl Pts',(0.511908095565866,0.194014433511492,
-3.33300467546839));
#66654=CARTESIAN_POINT('Ctrl Pts',(0.356471258936331,0.415475318483546,
-3.31909504552262));
#66655=CARTESIAN_POINT('Ctrl Pts',(0.113959317106475,0.535448198018523,
-3.30518541557687));
#66656=CARTESIAN_POINT('Ctrl Pts',(-0.156389425802974,0.524627340322321,
-3.2912757856311));
#66657=CARTESIAN_POINT('Ctrl Pts',(-0.388536980362357,0.385655952381858,
-3.27736615568535));
#66658=CARTESIAN_POINT('Ctrl Pts',(-0.52577674757244,0.152480524752521,
-3.26345652573959));
#66659=CARTESIAN_POINT('Ctrl Pts',(-0.534585219245928,-0.117941265384257,
-3.24954689579383));
#66660=CARTESIAN_POINT('Ctrl Pts',(-0.412810753200192,-0.359553585379074,
-3.23563726584807));
#66661=CARTESIAN_POINT('Ctrl Pts',(-0.190199154113247,-0.513337881410735,
-3.22172763590231));
#66662=CARTESIAN_POINT('Ctrl Pts',(0.0788723234021615,-0.541729319234063,
-3.20781800595655));
#66663=CARTESIAN_POINT('Ctrl Pts',(0.328677687071171,-0.437792732623787,
-3.1939083760108));
#66664=CARTESIAN_POINT('Ctrl Pts',(0.498197071264252,-0.226916673914411,
-3.17999874606503));
#66665=CARTESIAN_POINT('Ctrl Pts',(0.546022037454967,0.0393882384752367,
-3.16608911611928));
#66666=CARTESIAN_POINT('Ctrl Pts',(0.460470398488362,0.296071800130688,
-3.15217948617351));
#66667=CARTESIAN_POINT('Ctrl Pts',(0.26243982220252,0.480434010493602,-3.13826985622776));
#66668=CARTESIAN_POINT('Ctrl Pts',(0.000303165681132534,0.547440779269527,
-3.124360226282));
#66669=CARTESIAN_POINT('Ctrl Pts',(-0.261907545011288,0.480724387339375,
-3.11045059633624));
#66670=CARTESIAN_POINT('Ctrl Pts',(-0.460142194624714,0.296581623575379,
-3.09654096639048));
#66671=CARTESIAN_POINT('Ctrl Pts',(-0.545978077157708,0.0399929741308204,
-3.08263133644472));
#66672=CARTESIAN_POINT('Ctrl Pts',(-0.498448092699254,-0.22636474460731,
-3.06872170649896));
#66673=CARTESIAN_POINT('Ctrl Pts',(-0.329162373323501,-0.43742842923694,
-3.0548120765532));
#66674=CARTESIAN_POINT('Ctrl Pts',(-0.0794722803366616,-0.541641630023716,
-3.04090244660745));
#66675=CARTESIAN_POINT('Ctrl Pts',(0.189630477759485,-0.513548226188511,
-3.02699281666168));
#66676=CARTESIAN_POINT('Ctrl Pts',(0.412412267793957,-0.360010583302355,
-3.01308318671593));
#66677=CARTESIAN_POINT('Ctrl Pts',(0.534454262672952,-0.118533285735985,
-2.99917355677017));
#66678=CARTESIAN_POINT('Ctrl Pts',(0.525945308547331,0.151898094569056,
-2.98526392682441));
#66679=CARTESIAN_POINT('Ctrl Pts',(0.388963884556884,0.385225382376441,
-2.97135429687865));
#66680=CARTESIAN_POINT('Ctrl Pts',(0.156970393484291,0.524453805674097,
-2.9574446669329));
#66681=CARTESIAN_POINT('Ctrl Pts',(-0.113366198703285,0.535574087973106,
-2.94353503698713));
#66682=CARTESIAN_POINT('Ctrl Pts',(-0.356010870628611,0.415869881947366,
-2.92962540704138));
#66683=CARTESIAN_POINT('Ctrl Pts',(-0.51169289623865,0.19458129061027,-2.91571577709561));
#66684=CARTESIAN_POINT('Ctrl Pts',(-0.542383883572038,-0.0742376020488999,
-2.90180614714986));
#66685=CARTESIAN_POINT('Ctrl Pts',(-0.440586956278262,-0.324922502566556,
-2.8878965172041));
#66686=CARTESIAN_POINT('Ctrl Pts',(-0.231168012886207,-0.496238701165981,
-2.87398688725834));
#66687=CARTESIAN_POINT('Ctrl Pts',(0.034718257215661,-0.54633885211704,
-2.86007725731258));
#66688=CARTESIAN_POINT('Ctrl Pts',(0.292123911212751,-0.462985009708113,
-2.84616762736682));
#66689=CARTESIAN_POINT('Ctrl Pts',(0.478172563312183,-0.266537986808846,
-2.83225799742106));
#66690=CARTESIAN_POINT('Ctrl Pts',(0.547418176707864,-0.00498382649122336,
-2.8183483674753));
#66691=CARTESIAN_POINT('Ctrl Pts',(0.482946150517014,0.257787731316786,
-2.80443873752954));
#66692=CARTESIAN_POINT('Ctrl Pts',(0.3005050432063,0.457589573443535,-2.79052910758379));
#66693=CARTESIAN_POINT('Ctrl Pts',(0.0446596779240103,0.545616176340457,
-2.77661947763802));
#66694=CARTESIAN_POINT('Ctrl Pts',(-0.222094690695742,0.500365313627373,
-2.76270984769227));
#66695=CARTESIAN_POINT('Ctrl Pts',(-0.434598069728088,0.332890397135869,
-2.7488002177465));
#66696=CARTESIAN_POINT('Ctrl Pts',(-0.54094233580881,0.0841004640080302,
-2.73489058780075));
#66697=CARTESIAN_POINT('Ctrl Pts',(-0.515150813611932,-0.185232658976813,
-2.72098095785499));
#66698=CARTESIAN_POINT('Ctrl Pts',(-0.36352358891512,-0.409319067499827,
-2.70707132790923));
#66699=CARTESIAN_POINT('Ctrl Pts',(-0.12309858893052,-0.533421255781931,
-2.69316169796347));
#66700=CARTESIAN_POINT('Ctrl Pts',(0.147395658749169,-0.527224827278226,
-2.67925206801771));
#66701=CARTESIAN_POINT('Ctrl Pts',(0.381885622296803,-0.392243381333121,
-2.66534243807195));
#66702=CARTESIAN_POINT('Ctrl Pts',(0.523092523318703,-0.161448786817147,
-2.6514328081262));
#66703=CARTESIAN_POINT('Ctrl Pts',(0.536523803289445,0.108782844329816,
-2.63752317818043));
#66704=CARTESIAN_POINT('Ctrl Pts',(0.418898608319388,0.35244212952588,-2.62361354823468));
#66705=CARTESIAN_POINT('Ctrl Pts',(0.198949202144987,0.510010503502163,
-2.60970391828892));
#66706=CARTESIAN_POINT('Ctrl Pts',(-0.0695974535187176,0.542998796665671,
-2.59579428834316));
#66707=CARTESIAN_POINT('Ctrl Pts',(-0.321143564440328,0.443348970603538,
-2.5818846583974));
#66708=CARTESIAN_POINT('Ctrl Pts',(-0.494244053289945,0.235402452205118,
-2.56797502845164));
#66709=CARTESIAN_POINT('Ctrl Pts',(-0.546615726404821,-0.0300457378605709,
-2.55406539850588));
#66710=CARTESIAN_POINT('Ctrl Pts',(-0.465465774177804,-0.288154666430573,
-2.54015576856012));
#66711=CARTESIAN_POINT('Ctrl Pts',(-0.270616666022705,-0.475876159087017,
-2.52624613861436));
#66712=CARTESIAN_POINT('Ctrl Pts',(-0.00966412295619432,-0.547355554867349,
-2.5123365086686));
#66713=CARTESIAN_POINT('Ctrl Pts',(0.253649071921605,-0.485132607675433,
-2.49842687872285));
#66714=CARTESIAN_POINT('Ctrl Pts',(0.45500349994835,-0.304406494266152,
-2.48451724877709));
#66715=CARTESIAN_POINT('Ctrl Pts',(0.54521438798049,-0.049323116849169,
-2.47060761883133));
#66716=CARTESIAN_POINT('Ctrl Pts',(0.502245955099664,0.217808400441037,
-2.45669798888557));
#66717=CARTESIAN_POINT('Ctrl Pts',(0.33659408482971,0.431735938710581,-2.44278835893981));
#66718=CARTESIAN_POINT('Ctrl Pts',(0.0887224994730275,0.54020349573463,
-2.42887872899405));
#66719=CARTESIAN_POINT('Ctrl Pts',(-0.18082129866822,0.516715740678176,
-2.41496909904829));
#66720=CARTESIAN_POINT('Ctrl Pts',(-0.40619594373111,0.367010018954592,
-2.40105946910253));
#66721=CARTESIAN_POINT('Ctrl Pts',(-0.532349252863944,0.127654892941306,
-2.38714983915677));
#66722=CARTESIAN_POINT('Ctrl Pts',(-0.528465802975152,-0.142882447496131,
-2.37324020921101));
#66723=CARTESIAN_POINT('Ctrl Pts',(-0.395494202961323,-0.378517944278266,
-2.35933057926526));
#66724=CARTESIAN_POINT('Ctrl Pts',(-0.165915377355921,-0.52169300002348,
-2.3454209493195));
#66725=CARTESIAN_POINT('Ctrl Pts',(0.104191537332248,-0.537434295765537,
-2.33151131937374));
#66726=CARTESIAN_POINT('Ctrl Pts',(0.348847622965475,-0.421896710899712,
-2.31760168942798));
#66727=CARTESIAN_POINT('Ctrl Pts',(0.508290826193431,-0.203302569399051,
-2.30369205948222));
#66728=CARTESIAN_POINT('Ctrl Pts',(0.543574013561436,0.064952217031977,
-2.28978242953646));
#66729=CARTESIAN_POINT('Ctrl Pts',(0.446078573681184,0.317341148953642,
-2.27587279959071));
#66730=CARTESIAN_POINT('Ctrl Pts',(0.239619682310341,0.492213273455875,
-2.26196316964494));
#66731=CARTESIAN_POINT('Ctrl Pts',(-0.0253710219968334,0.546852640077282,
-2.24805353969918));
#66732=CARTESIAN_POINT('Ctrl Pts',(-0.284164355957781,0.467912510539904,
-2.23414390975342));
#66733=CARTESIAN_POINT('Ctrl Pts',(-0.473544965697884,0.274675561670212,
-2.22023427980767));
#66734=CARTESIAN_POINT('Ctrl Pts',(-0.547252918325985,0.0143437129206318,
-2.20632464986191));
#66735=CARTESIAN_POINT('Ctrl Pts',(-0.487283598972591,-0.249491869384507,
-2.19241501991615));
#66736=CARTESIAN_POINT('Ctrl Pts',(-0.308285691537408,-0.452384163195352,
-2.17850538997039));
#66737=CARTESIAN_POINT('Ctrl Pts',(-0.0539829499832726,-0.544772741450746,
-2.16459576002463));
#66738=CARTESIAN_POINT('Ctrl Pts',(0.213506187194575,-0.504089879630896,
-2.15068613007887));
#66739=CARTESIAN_POINT('Ctrl Pts',(0.428842245421929,-0.340273165645094,
-2.13677650013311));
#66740=CARTESIAN_POINT('Ctrl Pts',(0.539425163814452,-0.0933380488354483,
-2.12286687018735));
#66741=CARTESIAN_POINT('Ctrl Pts',(0.518242892982467,0.176396719328393,
-2.10895724024159));
#66742=CARTESIAN_POINT('Ctrl Pts',(0.370469618543577,0.403043124805315,
-2.09504761029584));
#66743=CARTESIAN_POINT('Ctrl Pts',(0.13220186467748,0.531238332288299,-2.08113798035007));
#66744=CARTESIAN_POINT('Ctrl Pts',(-0.138358790750498,0.529668144915963,
-2.06722835040432));
#66745=CARTESIAN_POINT('Ctrl Pts',(-0.375122594516613,0.398716111788552,
-2.05331872045856));
#66746=CARTESIAN_POINT('Ctrl Pts',(-0.52025533810128,0.170369838568274,
-2.0394090905128));
#66747=CARTESIAN_POINT('Ctrl Pts',(-0.538305498839373,-0.0995926133603777,
-2.02549946056704));
#66748=CARTESIAN_POINT('Ctrl Pts',(-0.424863970510547,-0.345227613725596,
-2.01158983062128));
#66749=CARTESIAN_POINT('Ctrl Pts',(-0.207641074117375,-0.506533990030323,
-1.99768020067552));
#66750=CARTESIAN_POINT('Ctrl Pts',(0.0603022321810123,-0.544109492207814,
-1.98377057072976));
#66751=CARTESIAN_POINT('Ctrl Pts',(0.313515534083973,-0.448775565962206,
-1.969860940784));
#66752=CARTESIAN_POINT('Ctrl Pts',(0.490146510124936,-0.243819394899179,
-1.95595131083825));
#66753=CARTESIAN_POINT('Ctrl Pts',(0.547049575814728,0.0206944513718702,
-1.94204168089249));
#66754=CARTESIAN_POINT('Ctrl Pts',(0.470325039924538,0.280153271508007,
-1.92813205094673));
#66755=CARTESIAN_POINT('Ctrl Pts',(0.278714377023783,0.471179153567835,
-1.91422242100097));
#66756=CARTESIAN_POINT('Ctrl Pts',(0.0190222542807834,0.547110274587066,
-1.90031279105521));
#66757=CARTESIAN_POINT('Ctrl Pts',(-0.245316427619855,0.489398967159197,
-1.88640316110945));
#66758=CARTESIAN_POINT('Ctrl Pts',(-0.449731754672463,0.312142351429414,
-1.87249353116369));
#66759=CARTESIAN_POINT('Ctrl Pts',(-0.544291269038013,0.0586388366668922,
-1.85858390121793));
#66760=CARTESIAN_POINT('Ctrl Pts',(-0.505896952420048,-0.209188365471801,
-1.84467427127217));
#66761=CARTESIAN_POINT('Ctrl Pts',(-0.343927370620985,-0.425917201407025,
-1.83076464132642));
#66762=CARTESIAN_POINT('Ctrl Pts',(-0.0979467746732575,-0.538607396948615,
-1.81685501138066));
#66763=CARTESIAN_POINT('Ctrl Pts',(0.171959244418416,-0.519732158881576,
-1.8029453814349));
#66764=CARTESIAN_POINT('Ctrl Pts',(0.399860841210855,-0.373902134766311,
-1.78903575148914));
#66765=CARTESIAN_POINT('Ctrl Pts',(0.530088575269402,-0.136739171730388,
-1.77512612154338));
#66766=CARTESIAN_POINT('Ctrl Pts',(0.530831765202846,0.133825019216465,
-1.76121649159762));
#66767=CARTESIAN_POINT('Ctrl Pts',(0.401908872275551,0.371699821230588,
-1.74730686165186));
#66768=CARTESIAN_POINT('Ctrl Pts',(0.174811844808601,0.518779642653092,
-1.7333972317061));
#66769=CARTESIAN_POINT('Ctrl Pts',(-0.0949864086208329,0.539137348821219,
-1.71948760176035));
#66770=CARTESIAN_POINT('Ctrl Pts',(-0.341582366448823,0.427800170228903,
-1.70557797181458));
#66771=CARTESIAN_POINT('Ctrl Pts',(-0.504740123447223,0.211964399131406,
-1.69166834186883));
#66772=CARTESIAN_POINT('Ctrl Pts',(-0.54460519345837,-0.0556478389052866,
-1.67775871192307));
#66773=CARTESIAN_POINT('Ctrl Pts',(-0.451439750281636,-0.309666999504807,
-1.66384908197731));
#66774=CARTESIAN_POINT('Ctrl Pts',(-0.248001282949535,-0.488043914388902,
-1.64993945203155));
#66775=CARTESIAN_POINT('Ctrl Pts',(0.0160163678687228,-0.547206519220075,
-1.63602982208579));
#66776=CARTESIAN_POINT('Ctrl Pts',(0.276121706313586,-0.472703185962534,
-1.62212019214003));
#66777=CARTESIAN_POINT('Ctrl Pts',(0.468778895650747,-0.282732816823804,
-1.60821056219427));
#66778=CARTESIAN_POINT('Ctrl Pts',(0.546927634078633,-0.0236994050095503,
-1.59430093224851));
#66779=CARTESIAN_POINT('Ctrl Pts',(0.491478557590205,0.241123051875402,
-1.58039130230275));
#66780=CARTESIAN_POINT('Ctrl Pts',(0.315976191999128,0.44704646828533,-1.56648167235699));
#66781=CARTESIAN_POINT('Ctrl Pts',(0.0632904365291062,0.543770005940573,
-1.55257204241124));
#66782=CARTESIAN_POINT('Ctrl Pts',(-0.204855250929235,0.507667041360159,
-1.53866241246548));
#66783=CARTESIAN_POINT('Ctrl Pts',(-0.422961020502676,0.347556432614895,
-1.52475278251972));
#66784=CARTESIAN_POINT('Ctrl Pts',(-0.537750254920378,0.10254834006324,
-1.51084315257396));
#66785=CARTESIAN_POINT('Ctrl Pts',(-0.521183429501975,-0.16750919834211,
-1.4969335226282));
#66786=CARTESIAN_POINT('Ctrl Pts',(-0.377307316686986,-0.396649325590153,
-1.48302389268244));
#66787=CARTESIAN_POINT('Ctrl Pts',(-0.141266482397949,-0.528900065860808,
-1.46911426273668));
#66788=CARTESIAN_POINT('Ctrl Pts',(0.129281464337643,-0.531956578768767,
-1.45520463279092));
#66789=CARTESIAN_POINT('Ctrl Pts',(0.368249874643727,-0.405072251013983,
-1.44129500284516));
#66790=CARTESIAN_POINT('Ctrl Pts',(0.517266021560369,-0.179241071341825,
-1.4273853728994));
#66791=CARTESIAN_POINT('Ctrl Pts',(0.539929784898266,0.0903732598525054,
-1.41347574295365));
#66792=CARTESIAN_POINT('Ctrl Pts',(0.430705095402437,0.337912147622774,
-1.39956611300789));
#66793=CARTESIAN_POINT('Ctrl Pts',(0.216272228382311,0.502909357585645,
-1.38565648306213));
#66794=CARTESIAN_POINT('Ctrl Pts',(-0.0509893774665488,0.545061081074617,
-1.37174685311637));
#66795=CARTESIAN_POINT('Ctrl Pts',(-0.305795826565191,0.454070931872949,
-1.35783722317061));
#66796=CARTESIAN_POINT('Ctrl Pts',(-0.485905639959076,0.252165040742401,
-1.34392759322485));
#66797=CARTESIAN_POINT('Ctrl Pts',(-0.547323458819898,-0.0113371134810136,
-1.33001796327909));
#66798=CARTESIAN_POINT('Ctrl Pts',(-0.475046774798344,-0.2720699551041,
-1.31610833333333));
#66799=CARTESIAN_POINT('Ctrl Pts',(-0.286730587300225,-0.466344367418676,
-1.30219870338757));
#66800=CARTESIAN_POINT('Ctrl Pts',(-0.0283748231814932,-0.54670501015271,
-1.28828907344181));
#66801=CARTESIAN_POINT('Ctrl Pts',(0.236912048709972,-0.493522218236121,
-1.27437944349606));
#66802=CARTESIAN_POINT('Ctrl Pts',(0.444328500343154,-0.319786932971721,
-1.2604698135503));
#66803=CARTESIAN_POINT('Ctrl Pts',(0.543208990265627,-0.0679374095123898,
-1.24656018360454));
#66804=CARTESIAN_POINT('Ctrl Pts',(0.509400017047994,0.20050716034137,-1.23265055365878));
#66805=CARTESIAN_POINT('Ctrl Pts',(0.351160086322446,0.419973918821954,
-1.21874092371302));
#66806=CARTESIAN_POINT('Ctrl Pts',(0.10714240860568,0.536853800391532,-1.20483129376726));
#66807=CARTESIAN_POINT('Ctrl Pts',(-0.163046906422306,0.522596598747804,
-1.1909216638215));
#66808=CARTESIAN_POINT('Ctrl Pts',(-0.393408812722661,0.38068491536808,
-1.17701203387574));
#66809=CARTESIAN_POINT('Ctrl Pts',(-0.527672890949092,0.14578346570885,
-1.16310240392999));
#66810=CARTESIAN_POINT('Ctrl Pts',(-0.533042503383665,-0.124728458272891,
-1.14919277398422));
#66811=CARTESIAN_POINT('Ctrl Pts',(-0.408206016743456,-0.364773006966111,
-1.13528314403847));
#66812=CARTESIAN_POINT('Ctrl Pts',(-0.183657194367116,-0.515714585477138,
-1.12137351409271));
#66813=CARTESIAN_POINT('Ctrl Pts',(0.085753504301945,-0.540682749139079,
-1.10746388414695));
#66814=CARTESIAN_POINT('Ctrl Pts',(0.334217225560628,-0.43357853366514,
-1.09355425420119));
#66815=CARTESIAN_POINT('Ctrl Pts',(0.501041826284635,-0.220564246944092,
-1.07964462425543));
#66816=CARTESIAN_POINT('Ctrl Pts',(0.545477121728666,0.0463271884239284,
-1.06573499430967));
#66817=CARTESIAN_POINT('Ctrl Pts',(0.456668918382307,0.301902298269141,
-1.05182536436391));
#66818=CARTESIAN_POINT('Ctrl Pts',(0.256310363884194,0.483731843155078,
-1.03791573441815));
#66819=CARTESIAN_POINT('Ctrl Pts',(-0.00665703028796617,0.547400386065266,
-1.02400610447239));
#66820=CARTESIAN_POINT('Ctrl Pts',(-0.267998314084843,0.477355635102738,
-1.01009647452664));
#66821=CARTESIAN_POINT('Ctrl Pts',(-0.463875746849021,0.290707396194043,
-0.996186844580877));
#66822=CARTESIAN_POINT('Ctrl Pts',(-0.546442419084335,0.0330481669978269,
-0.982277214635117));
#66823=CARTESIAN_POINT('Ctrl Pts',(-0.495529799694107,-0.232683725971057,
-0.968367584689358));
#66824=CARTESIAN_POINT('Ctrl Pts',(-0.323574295761076,-0.441578049544336,
-0.9544579547436));
#66825=CARTESIAN_POINT('Ctrl Pts',(-0.0725794158974647,-0.542608263026504,
-0.940548324797841));
#66826=CARTESIAN_POINT('Ctrl Pts',(0.196144411577539,-0.511095752793503,
-0.926638694852082));
#66827=CARTESIAN_POINT('Ctrl Pts',(0.416956114738421,-0.354738068296732,
-0.912729064906324));
#66828=CARTESIAN_POINT('Ctrl Pts',(0.535918098897834,-0.111728644448898,
-0.898819434960564));
#66829=CARTESIAN_POINT('Ctrl Pts',(0.523971563308618,0.158572694877081,
-0.884909805014805));
#66830=CARTESIAN_POINT('Ctrl Pts',(0.384034683888557,0.390139539507691,
-0.871000175069045));
#66831=CARTESIAN_POINT('Ctrl Pts',(0.150289791446776,0.526407140247491,
-0.857090545123288));
#66832=CARTESIAN_POINT('Ctrl Pts',(-0.120166333871985,0.534089459660479,
-0.843180915177528));
#66833=CARTESIAN_POINT('Ctrl Pts',(-0.361269472375872,0.411309940368472,
-0.82927128523177));
#66834=CARTESIAN_POINT('Ctrl Pts',(-0.514125447821904,0.188059891041614,
-0.815361655286009));
#66835=CARTESIAN_POINT('Ctrl Pts',(-0.541396186497834,-0.0811274796986776,
-0.801452025340252));
#66836=CARTESIAN_POINT('Ctrl Pts',(-0.436420274952878,-0.330497870381506,
-0.787542395394492));
#66837=CARTESIAN_POINT('Ctrl Pts',(-0.224840141046584,-0.499137666071003,
-0.773632765448734));
#66838=CARTESIAN_POINT('Ctrl Pts',(0.0416616126090963,-0.545853285005657,
-0.759723135502974));
#66839=CARTESIAN_POINT('Ctrl Pts',(0.297986699255,-0.459233519882606,-0.745813505557216));
#66840=CARTESIAN_POINT('Ctrl Pts',(0.481522682893413,-0.260436949328981,
-0.731903875611456));
#66841=CARTESIAN_POINT('Ctrl Pts',(0.547437295332376,0.00197646042940402,
-0.717994245665697));
#66842=CARTESIAN_POINT('Ctrl Pts',(0.47962959808533,0.263907080915161,-0.704084615719938));
#66843=CARTESIAN_POINT('Ctrl Pts',(0.294662952778667,0.461373214411515,
-0.69017498577418));
#66844=CARTESIAN_POINT('Ctrl Pts',(0.0377190948114364,0.546139880070356,
-0.67626535582842));
#66845=CARTESIAN_POINT('Ctrl Pts',(-0.228438392772295,0.497501155198928,
-0.662355725882662));
#66846=CARTESIAN_POINT('Ctrl Pts',(-0.438795316961955,0.327338003490144,
-0.648446095936902));
#66847=CARTESIAN_POINT('Ctrl Pts',(-0.541967868139668,0.077216116328137,
-0.634536465991144));
#66848=CARTESIAN_POINT('Ctrl Pts',(-0.512754124629076,-0.191767323578675,
-0.620626836045384));
#66849=CARTESIAN_POINT('Ctrl Pts',(-0.358290116967589,-0.413907828870158,
-0.606717206099626));
#66850=CARTESIAN_POINT('Ctrl Pts',(-0.11630671231382,-0.534943218844212,
-0.592807576153866));
#66851=CARTESIAN_POINT('Ctrl Pts',(0.154086890795909,-0.525308222666945,
-0.578897946208108));
#66852=CARTESIAN_POINT('Ctrl Pts',(0.386841744947087,-0.387356377361918,
-0.564988316262349));
#66853=CARTESIAN_POINT('Ctrl Pts',(0.525102906289336,-0.154785130174539,
-0.55107868631659));
#66854=CARTESIAN_POINT('Ctrl Pts',(0.535097371060952,0.115595424651308,
-0.537169056370831));
#66855=CARTESIAN_POINT('Ctrl Pts',(0.414383794975135,0.357739527000668,
-0.523259426425071));
#66856=CARTESIAN_POINT('Ctrl Pts',(0.19244883950397,0.51249872476937,-0.509349796479313));
#66857=CARTESIAN_POINT('Ctrl Pts',(-0.0764955242305444,0.542070044818335,
-0.495440166533554));
#66858=CARTESIAN_POINT('Ctrl Pts',(-0.326754353990724,0.439230111518734,
-0.481530536587795));
#66859=CARTESIAN_POINT('Ctrl Pts',(-0.497197016149334,0.229099598098419,
-0.467620906642036));
#66860=CARTESIAN_POINT('Ctrl Pts',(-0.54618954340598,-0.0369929911013041,
-0.453711276696277));
#66861=CARTESIAN_POINT('Ctrl Pts',(-0.46176454888738,-0.294049315774561,
-0.439801646750518));
#66862=CARTESIAN_POINT('Ctrl Pts',(-0.264544495400683,-0.479278320675863,
-0.425892016804759));
#66863=CARTESIAN_POINT('Ctrl Pts',(-0.00270425391930869,-0.547434183922904,
-0.411982386859));
#66864=CARTESIAN_POINT('Ctrl Pts',(0.259796554686738,-0.481868497507032,
-0.398072756913241));
#66865=CARTESIAN_POINT('Ctrl Pts',(0.458836953054976,-0.298596967880934,
-0.384163126967482));
#66866=CARTESIAN_POINT('Ctrl Pts',(0.545797415228185,-0.0423872651522121,
-0.370253497021723));
#66867=CARTESIAN_POINT('Ctrl Pts',(0.499436140633363,0.224176359471699,
-0.356343867075964));
#66868=CARTESIAN_POINT('Ctrl Pts',(0.331077781011755,0.435980506027487,
-0.342434237130205));
#66869=CARTESIAN_POINT('Ctrl Pts',(0.0818471718350033,0.541287852424598,
-0.328524607184445));
#66870=CARTESIAN_POINT('Ctrl Pts',(-0.187376216331818,0.514375011312576,
-0.314614977238687));
#66871=CARTESIAN_POINT('Ctrl Pts',(-0.410829284067798,0.36181597267254,
-0.300705347292928));
#66872=CARTESIAN_POINT('Ctrl Pts',(-0.533929231491555,0.120876277495512,
-0.28679571734717));
#66873=CARTESIAN_POINT('Ctrl Pts',(-0.526606479121654,-0.149589822070715,
-0.27288608740141));
#66874=CARTESIAN_POINT('Ctrl Pts',(-0.390649752922828,-0.383515670215699,
-0.258976457455652));
#66875=CARTESIAN_POINT('Ctrl Pts',(-0.159269153319243,-0.523760284249544,
-0.245066827509892));
#66876=CARTESIAN_POINT('Ctrl Pts',(0.111016064888819,-0.53606616423677,
-0.231157197564133));
#66877=CARTESIAN_POINT('Ctrl Pts',(0.354183428665716,-0.41742735519224,
-0.217247567618374));
#66878=CARTESIAN_POINT('Ctrl Pts',(0.51083453569749,-0.196823720178588,
-0.203337937672615));
#66879=CARTESIAN_POINT('Ctrl Pts',(0.542704273947877,0.0718579790208525,
-0.189428307726856));
#66880=CARTESIAN_POINT('Ctrl Pts',(0.442007839686807,0.322986945172268,
-0.175518677781097));
#66881=CARTESIAN_POINT('Ctrl Pts',(0.233342303313345,0.495220027940256,
-0.161609047835339));
#66882=CARTESIAN_POINT('Ctrl Pts',(-0.0323216585670542,0.546485853693586,
-0.14769941788958));
#66883=CARTESIAN_POINT('Ctrl Pts',(-0.290090448635031,0.464261856806131,
-0.133789787943821));
#66884=CARTESIAN_POINT('Ctrl Pts',(-0.476998895253674,0.2686326306232,-0.119880157998062));
#66885=CARTESIAN_POINT('Ctrl Pts',(-0.5473911015369,0.00738490965168814,
-0.105970528052302));
#66886=CARTESIAN_POINT('Ctrl Pts',(-0.484072073042989,-0.255667307605576,
-0.0920608981065435));
#66887=CARTESIAN_POINT('Ctrl Pts',(-0.302509342715061,-0.456266617395285,
-0.0781512681607847));
#66888=CARTESIAN_POINT('Ctrl Pts',(-0.0470519678878475,-0.545416086573125,
-0.0642416382150256));
#66889=CARTESIAN_POINT('Ctrl Pts',(0.219897217017238,-0.501332588518456,
-0.0503320082692668));
#66890=CARTESIAN_POINT('Ctrl Pts',(0.433135230583494,-0.334797314980531,
-0.0364223783235079));
#66891=CARTESIAN_POINT('Ctrl Pts',(0.540565512147126,-0.0864644858093628,
-0.0225127483777489));
#66892=CARTESIAN_POINT('Ctrl Pts',(0.515963701837572,0.18295602369734,-0.00860311843199006));
#66893=CARTESIAN_POINT('Ctrl Pts',(0.365304511527139,0.407753219468906,
0.00530651151376877));
#66894=CARTESIAN_POINT('Ctrl Pts',(0.205409024163764,0.491108180259118,
0.0145795981442749));
#66895=CARTESIAN_POINT('Ctrl Pts',(0.120319876696228,0.511137837581914,
0.0192161414595281));
#66896=CARTESIAN_POINT('Ctrl Pts',(-0.243856727558445,0.502329722221634,
-3.96754114145953));
#66897=CARTESIAN_POINT('Ctrl Pts',(-0.327479587516629,0.461734877687463,
-3.96290459814427));
#66898=CARTESIAN_POINT('Ctrl Pts',(-0.473974953282714,0.33801685956352,
-3.95363151151377));
#66899=CARTESIAN_POINT('Ctrl Pts',(-0.577952945034314,0.0696920735605909,
-3.93972188156801));
#66900=CARTESIAN_POINT('Ctrl Pts',(-0.540746265833271,-0.215581171713082,
-3.92581225162225));
#66901=CARTESIAN_POINT('Ctrl Pts',(-0.371456103433689,-0.448231402072954,
-3.9119026216765));
#66902=CARTESIAN_POINT('Ctrl Pts',(-0.111428220693573,-0.571373559976427,
-3.89799299173073));
#66903=CARTESIAN_POINT('Ctrl Pts',(0.175817028445578,-0.554956089486103,
-3.88408336178498));
#66904=CARTESIAN_POINT('Ctrl Pts',(0.420116112083225,-0.402974791659343,
-3.87017373183921));
#66905=CARTESIAN_POINT('Ctrl Pts',(0.56179328006591,-0.152561497953608,
-3.85626410189346));
#66906=CARTESIAN_POINT('Ctrl Pts',(0.566241563426747,0.135119222564917,
-3.8423544719477));
#66907=CARTESIAN_POINT('Ctrl Pts',(0.432374145368927,0.389793761798776,
-3.82844484200194));
#66908=CARTESIAN_POINT('Ctrl Pts',(0.192890892497521,0.549253856835642,
-3.81453521205618));
#66909=CARTESIAN_POINT('Ctrl Pts',(-0.0937097697185672,0.574547739017817,
-3.80062558211042));
#66910=CARTESIAN_POINT('Ctrl Pts',(-0.357419969727719,0.45949714148416,
-3.78671595216466));
#66911=CARTESIAN_POINT('Ctrl Pts',(-0.533823328786559,0.232205298608011,
-3.7728063222189));
#66912=CARTESIAN_POINT('Ctrl Pts',(-0.579829854021713,-0.0518072252693176,
-3.75889669227314));
#66913=CARTESIAN_POINT('Ctrl Pts',(-0.48420155244083,-0.323164828842655,
-3.74498706232738));
#66914=CARTESIAN_POINT('Ctrl Pts',(-0.27029751243075,-0.515583070764315,
-3.73107743238163));
#66915=CARTESIAN_POINT('Ctrl Pts',(0.00963200258153823,-0.582060025988483,
-3.71716780243587));
#66916=CARTESIAN_POINT('Ctrl Pts',(0.287208712007788,-0.506357388072924,
-3.70325817249011));
#66917=CARTESIAN_POINT('Ctrl Pts',(0.494629053365649,-0.306967015338603,
-3.68934854254435));
#66918=CARTESIAN_POINT('Ctrl Pts',(0.581226535210402,-0.0325939206265673,
-3.67543891259859));
#66919=CARTESIAN_POINT('Ctrl Pts',(0.525848021966783,0.249740879048841,
-3.66152928265284));
#66920=CARTESIAN_POINT('Ctrl Pts',(0.342020803029351,0.471071564838469,
-3.64761965270707));
#66921=CARTESIAN_POINT('Ctrl Pts',(0.0746482865109549,0.577333770191651,
-3.63371002276131));
#66922=CARTESIAN_POINT('Ctrl Pts',(-0.210958539890159,0.542570864810902,
-3.61980039281555));
#66923=CARTESIAN_POINT('Ctrl Pts',(-0.445034600226093,0.37527437094894,
-3.6058907628698));
#66924=CARTESIAN_POINT('Ctrl Pts',(-0.570402220087964,0.116309742538902,
-3.59198113292404));
#66925=CARTESIAN_POINT('Ctrl Pts',(-0.556437896418977,-0.171065824522912,
-3.57807150297827));
#66926=CARTESIAN_POINT('Ctrl Pts',(-0.406552689499017,-0.416655204637545,
-3.56416187303252));
#66927=CARTESIAN_POINT('Ctrl Pts',(-0.157359004489718,-0.560468368952972,
-3.55025224308676));
#66928=CARTESIAN_POINT('Ctrl Pts',(0.13027270750405,-0.567376127952309,
-3.536342613141));
#66929=CARTESIAN_POINT('Ctrl Pts',(0.386082752459345,-0.435691125849609,
-3.52243298319524));
#66930=CARTESIAN_POINT('Ctrl Pts',(0.547584503425569,-0.197580010372577,
-3.50852335324949));
#66931=CARTESIAN_POINT('Ctrl Pts',(0.575327986238213,0.0887939026157717,
-3.49461372330372));
#66932=CARTESIAN_POINT('Ctrl Pts',(0.462536310407596,0.353478161199798,
-3.48070409335796));
#66933=CARTESIAN_POINT('Ctrl Pts',(0.236761057702121,0.531818437482596,
-3.46679446341221));
#66934=CARTESIAN_POINT('Ctrl Pts',(-0.046847732742882,0.580251616824556,
-3.45288483346644));
#66935=CARTESIAN_POINT('Ctrl Pts',(-0.319013044492984,0.486946944064727,
-3.43897520352069));
#66936=CARTESIAN_POINT('Ctrl Pts',(-0.513253155506318,0.274695917795417,
-3.42506557357493));
#66937=CARTESIAN_POINT('Ctrl Pts',(-0.582121104277277,-0.00465498073710868,
-3.41115594362916));
#66938=CARTESIAN_POINT('Ctrl Pts',(-0.508794541924058,-0.2828688088124,
-3.39724631368342));
#66939=CARTESIAN_POINT('Ctrl Pts',(-0.311184921251967,-0.491986375498414,
-3.38333668373764));
#66940=CARTESIAN_POINT('Ctrl Pts',(-0.0375622726695128,-0.580926608585422,
-3.3694270537919));
#66941=CARTESIAN_POINT('Ctrl Pts',(0.24523569864168,-0.527964109577901,
-3.35551742384613));
#66942=CARTESIAN_POINT('Ctrl Pts',(0.468130034743078,-0.346036008909629,
-3.34160779390038));
#66943=CARTESIAN_POINT('Ctrl Pts',(0.576674416953902,-0.0795818177823006,
-3.32769816395461));
#66944=CARTESIAN_POINT('Ctrl Pts',(0.544354748378621,0.206311795126474,
-3.31378853400886));
#66945=CARTESIAN_POINT('Ctrl Pts',(0.379065742744303,0.441809700627282,
-3.2998789040631));
#66946=CARTESIAN_POINT('Ctrl Pts',(0.121182485540343,0.569386910710919,
-3.28596927411734));
#66947=CARTESIAN_POINT('Ctrl Pts',(-0.166301973478169,0.557880186516715,
-3.27205964417158));
#66948=CARTESIAN_POINT('Ctrl Pts',(-0.413163909719271,0.41010027139243,
-3.25815001422582));
#66949=CARTESIAN_POINT('Ctrl Pts',(-0.559102447504268,0.162145311635571,
-3.24424038428006));
#66950=CARTESIAN_POINT('Ctrl Pts',(-0.568469233110817,-0.125416824617188,
-3.2303307543343));
#66951=CARTESIAN_POINT('Ctrl Pts',(-0.438976245214247,-0.382343438584031,
-3.21642112438855));
#66952=CARTESIAN_POINT('Ctrl Pts',(-0.202254689027127,-0.545875159406616,
-3.20251149444278));
#66953=CARTESIAN_POINT('Ctrl Pts',(0.0838715467317631,-0.576066152919507,
-3.18860186449702));
#66954=CARTESIAN_POINT('Ctrl Pts',(0.349510510173741,-0.465541676081477,
-3.17469223455127));
#66955=CARTESIAN_POINT('Ctrl Pts',(0.529774667992378,-0.241299502784869,
-3.16078260460551));
#66956=CARTESIAN_POINT('Ctrl Pts',(0.580630959702681,0.0418848125864526,
-3.14687297465975));
#66957=CARTESIAN_POINT('Ctrl Pts',(0.489656737363871,0.314837939970435,
-3.13296334471399));
#66958=CARTESIAN_POINT('Ctrl Pts',(0.279074241288692,0.51088571788591,-3.11905371476823));
#66959=CARTESIAN_POINT('Ctrl Pts',(0.000322381457725726,0.582139626688352,
-3.10514408482247));
#66960=CARTESIAN_POINT('Ctrl Pts',(-0.278508226375054,0.511194499903981,
-3.09123445487671));
#66961=CARTESIAN_POINT('Ctrl Pts',(-0.489307730709825,0.315380077934957,
-3.07732482493096));
#66962=CARTESIAN_POINT('Ctrl Pts',(-0.580584213037096,0.0425278786533559,
-3.06341519498519));
#66963=CARTESIAN_POINT('Ctrl Pts',(-0.530041600106311,-0.240712590130639,
-3.04950556503944));
#66964=CARTESIAN_POINT('Ctrl Pts',(-0.350025917656482,-0.465154281781214,
-3.03559593509368));
#66965=CARTESIAN_POINT('Ctrl Pts',(-0.0845095311843385,-0.575972905638505,
-3.02168630514792));
#66966=CARTESIAN_POINT('Ctrl Pts',(0.20164996783568,-0.546098836624404,
-3.00777667520216));
#66967=CARTESIAN_POINT('Ctrl Pts',(0.438552502310153,-0.382829402747702,
-2.9938670452564));
#66968=CARTESIAN_POINT('Ctrl Pts',(0.568329976019654,-0.126046369436643,
-2.97995741531064));
#66969=CARTESIAN_POINT('Ctrl Pts',(0.559281692505214,0.161525964845169,
-2.96604778536488));
#66970=CARTESIAN_POINT('Ctrl Pts',(0.413617872700921,0.409642410247063,
-2.95213815541912));
#66971=CARTESIAN_POINT('Ctrl Pts',(0.166919765067557,0.557695652592388,
-2.93822852547337));
#66972=CARTESIAN_POINT('Ctrl Pts',(-0.120551773070811,0.569520780042436,
-2.9243188955276));
#66973=CARTESIAN_POINT('Ctrl Pts',(-0.378576173300926,0.442229273001557,
-2.91040926558185));
#66974=CARTESIAN_POINT('Ctrl Pts',(-0.544125908911863,0.206914581751741,
-2.89649963563609));
#66975=CARTESIAN_POINT('Ctrl Pts',(-0.576762205997358,-0.0789430593764874,
-2.88259000569033));
#66976=CARTESIAN_POINT('Ctrl Pts',(-0.468513008098925,-0.34551730800751,
-2.86868037574457));
#66977=CARTESIAN_POINT('Ctrl Pts',(-0.245820307547111,-0.527692169060811,
-2.85477074579881));
#66978=CARTESIAN_POINT('Ctrl Pts',(0.0369188304199093,-0.580967855264889,
-2.84086111585305));
#66979=CARTESIAN_POINT('Ctrl Pts',(0.310639819063253,-0.492330734062996,
-2.82695148590729));
#66980=CARTESIAN_POINT('Ctrl Pts',(0.508480931710273,-0.283432162920356,
-2.81304185596153));
#66981=CARTESIAN_POINT('Ctrl Pts',(0.582115591491657,-0.00529972008470409,
-2.79913222601578));
#66982=CARTESIAN_POINT('Ctrl Pts',(0.513557086755012,0.274127283454903,
-2.78522259607001));
#66983=CARTESIAN_POINT('Ctrl Pts',(0.319552178600044,0.486593314835525,
-2.77131296612426));
#66984=CARTESIAN_POINT('Ctrl Pts',(0.047490375615416,0.58019937359029,-2.75740333617849));
#66985=CARTESIAN_POINT('Ctrl Pts',(-0.236171884205633,0.532080341679168,
-2.74349370623274));
#66986=CARTESIAN_POINT('Ctrl Pts',(-0.462144523483567,0.353990237584042,
-2.72958407628697));
#66987=CARTESIAN_POINT('Ctrl Pts',(-0.575229287536554,0.0894310664749516,
-2.71567444634122));
#66988=CARTESIAN_POINT('Ctrl Pts',(-0.547803002042353,-0.196973398823406,
-2.70176481639546));
#66989=CARTESIAN_POINT('Ctrl Pts',(-0.386565075816664,-0.435263243393599,
-2.6878551864497));
#66990=CARTESIAN_POINT('Ctrl Pts',(-0.130901038650237,-0.567231493282018,
-2.67394555650394));
#66991=CARTESIAN_POINT('Ctrl Pts',(0.156738147775943,-0.560642311926621,
-2.66003592655819));
#66992=CARTESIAN_POINT('Ctrl Pts',(0.406090963662131,-0.417105236268524,
-2.64612629661242));
#66993=CARTESIAN_POINT('Ctrl Pts',(0.55624808706166,-0.171682015746856,
-2.63221666666667));
#66994=CARTESIAN_POINT('Ctrl Pts',(0.570530691873357,0.115677908526938,
-2.61830703672091));
#66995=CARTESIAN_POINT('Ctrl Pts',(0.445449971397287,0.374781232017847,
-2.60439740677515));
#66996=CARTESIAN_POINT('Ctrl Pts',(0.211559347882646,0.54233687982114,-2.59048777682939));
#66997=CARTESIAN_POINT('Ctrl Pts',(-0.0740088008494859,0.57741609458646,
-2.57657814688363));
#66998=CARTESIAN_POINT('Ctrl Pts',(-0.341498846626141,0.471450089239226,
-2.56266851693787));
#66999=CARTESIAN_POINT('Ctrl Pts',(-0.52557109293002,0.250323141493158,
-2.54875888699211));
#67000=CARTESIAN_POINT('Ctrl Pts',(-0.58126227888226,-0.0319501492838499,
-2.53484925704635));
#67001=CARTESIAN_POINT('Ctrl Pts',(-0.494968738678243,-0.306418988677151,
-2.5209396271006));
#67002=CARTESIAN_POINT('Ctrl Pts',(-0.287769364102383,-0.506038972782501,
-2.50702999715484));
#67003=CARTESIAN_POINT('Ctrl Pts',(-0.0102766712730032,-0.582049000444297,
-2.49312036720908));
#67004=CARTESIAN_POINT('Ctrl Pts',(0.269726300322964,-0.515882129759062,
-2.47921073726332));
#67005=CARTESIAN_POINT('Ctrl Pts',(0.483843326314238,-0.323700918243729,
-2.46530110731756));
#67006=CARTESIAN_POINT('Ctrl Pts',(0.579772118378885,-0.0524494007698775,
-2.4513914773718));
#67007=CARTESIAN_POINT('Ctrl Pts',(0.534080185253253,0.231613912817236,
-2.43748184742604));
#67008=CARTESIAN_POINT('Ctrl Pts',(0.357928678878714,0.459100979880023,
-2.42357221748028));
#67009=CARTESIAN_POINT('Ctrl Pts',(0.0943460638628411,0.574443617010623,
-2.40966258753452));
#67010=CARTESIAN_POINT('Ctrl Pts',(-0.192282429972567,0.549467120048602,
-2.39575295758877));
#67011=CARTESIAN_POINT('Ctrl Pts',(-0.431942164340539,0.390272488852942,
-2.381843327643));
#67012=CARTESIAN_POINT('Ctrl Pts',(-0.566091542803142,0.135746138278104,
-2.36793369769725));
#67013=CARTESIAN_POINT('Ctrl Pts',(-0.561961945312173,-0.151938872286246,
-2.35402406775148));
#67014=CARTESIAN_POINT('Ctrl Pts',(-0.420562107149786,-0.402509829594746,
-2.34011443780573));
#67015=CARTESIAN_POINT('Ctrl Pts',(-0.176431715526768,-0.554759856737075,
-2.32620480785997));
#67016=CARTESIAN_POINT('Ctrl Pts',(0.110795587291858,-0.571498894773481,
-2.31229517791421));
#67017=CARTESIAN_POINT('Ctrl Pts',(0.370958892165863,-0.448638104950677,
-2.29838554796845));
#67018=CARTESIAN_POINT('Ctrl Pts',(0.540508202922305,-0.216188647861906,
-2.28447591802269));
#67019=CARTESIAN_POINT('Ctrl Pts',(0.578027770883962,0.0690691318721798,
-2.27056628807693));
#67020=CARTESIAN_POINT('Ctrl Pts',(0.474352704785602,0.337455419801257,
-2.25665665813117));
#67021=CARTESIAN_POINT('Ctrl Pts',(0.254807675441085,0.523411594662337,
-2.24274702818541));
#67022=CARTESIAN_POINT('Ctrl Pts',(-0.0269791324161961,0.581514209030809,
-2.22883739823966));
#67023=CARTESIAN_POINT('Ctrl Pts',(-0.302175757378049,0.497570558356965,
-2.2149277682939));
#67024=CARTESIAN_POINT('Ctrl Pts',(-0.503560019623222,0.292085527761509,
-2.20101813834814));
#67025=CARTESIAN_POINT('Ctrl Pts',(-0.581939858414442,0.0152528711801189,
-2.18710850840238));
#67026=CARTESIAN_POINT('Ctrl Pts',(-0.518169458942701,-0.265305598715306,
-2.17319887845662));
#67027=CARTESIAN_POINT('Ctrl Pts',(-0.327825993570329,-0.481057966185246,
-2.15928924851086));
#67028=CARTESIAN_POINT('Ctrl Pts',(-0.0574045915847395,-0.579302478637584,
-2.1453796185651));
#67029=CARTESIAN_POINT('Ctrl Pts',(0.227039009178215,-0.536040984629006,
-2.13146998861935));
#67030=CARTESIAN_POINT('Ctrl Pts',(0.456023873470351,-0.361840953618791,
-2.11756035867358));
#67031=CARTESIAN_POINT('Ctrl Pts',(0.573615951497547,-0.0992541640346744,
-2.10365072872783));
#67032=CARTESIAN_POINT('Ctrl Pts',(0.551091068986974,0.187577404218774,
-2.08974109878207));
#67033=CARTESIAN_POINT('Ctrl Pts',(0.393951370824267,0.428589507940103,
-2.07583146883631));
#67034=CARTESIAN_POINT('Ctrl Pts',(0.140581314116832,0.564910207919669,
-2.06192183889055));
#67035=CARTESIAN_POINT('Ctrl Pts',(-0.147128489229501,0.56324049618942,
-2.04801220894479));
#67036=CARTESIAN_POINT('Ctrl Pts',(-0.398899269845503,0.423988232628435,
-2.03410257899903));
#67037=CARTESIAN_POINT('Ctrl Pts',(-0.553231070416462,0.181168517178112,
-2.02019294905327));
#67038=CARTESIAN_POINT('Ctrl Pts',(-0.572425317961847,-0.105905166290112,
-2.00628331910751));
#67039=CARTESIAN_POINT('Ctrl Pts',(-0.451793440591628,-0.367109433179042,
-1.99237368916175));
#67040=CARTESIAN_POINT('Ctrl Pts',(-0.220802143262232,-0.538640011901701,
-1.97846405921599));
#67041=CARTESIAN_POINT('Ctrl Pts',(0.0641244135615362,-0.578597190172963,
-1.96455442927024));
#67042=CARTESIAN_POINT('Ctrl Pts',(0.333387323129587,-0.477220642540898,
-1.95064479932448));
#67043=CARTESIAN_POINT('Ctrl Pts',(0.521213832128952,-0.259273581546812,
-1.93673516937872));
#67044=CARTESIAN_POINT('Ctrl Pts',(0.581723627293058,0.0220061432256019,
-1.92282553943296));
#67045=CARTESIAN_POINT('Ctrl Pts',(0.500136002891841,0.297910435369479,
-1.9089159094872));
#67046=CARTESIAN_POINT('Ctrl Pts',(0.296380338362444,0.501044253457539,
-1.89500627954144));
#67047=CARTESIAN_POINT('Ctrl Pts',(0.0202279560184803,0.581788173380976,
-1.88109664959568));
#67048=CARTESIAN_POINT('Ctrl Pts',(-0.260865501809525,0.52041890708959,
-1.86718701964992));
#67049=CARTESIAN_POINT('Ctrl Pts',(-0.478237438073695,0.331927103014152,
-1.85327738970416));
#67050=CARTESIAN_POINT('Ctrl Pts',(-0.578790488699635,0.0623555858083014,
-1.8393677597584));
#67051=CARTESIAN_POINT('Ctrl Pts',(-0.537962596461209,-0.22244750773918,
-1.82545812981265));
#67052=CARTESIAN_POINT('Ctrl Pts',(-0.365726775795477,-0.452913429207948,
-1.81154849986689));
#67053=CARTESIAN_POINT('Ctrl Pts',(-0.104155008181343,-0.572746351504227,
-1.79763886992113));
#67054=CARTESIAN_POINT('Ctrl Pts',(0.182858665525284,-0.552674730137874,
-1.78372923997537));
#67055=CARTESIAN_POINT('Ctrl Pts',(0.425205519289921,-0.397601452784128,
-1.76981961002961));
#67056=CARTESIAN_POINT('Ctrl Pts',(0.56368757499368,-0.145406212688464,
-1.75590998008385));
#67057=CARTESIAN_POINT('Ctrl Pts',(0.564477871089254,0.142307350271176,
-1.74200035013809));
#67058=CARTESIAN_POINT('Ctrl Pts',(0.427383362235855,0.395259548366178,
-1.72809072019233));
#67059=CARTESIAN_POINT('Ctrl Pts',(0.185892074414644,0.551661839862501,
-1.71418109024657));
#67060=CARTESIAN_POINT('Ctrl Pts',(-0.101007003038359,0.573309893711828,
-1.70027146030082));
#67061=CARTESIAN_POINT('Ctrl Pts',(-0.363233136474001,0.454915747647758,
-1.68636183035506));
#67062=CARTESIAN_POINT('Ctrl Pts',(-0.536732443334361,0.225399496811739,
-1.6724522004093));
#67063=CARTESIAN_POINT('Ctrl Pts',(-0.579124310825782,-0.0591750074036544,
-1.65854257046354));
#67064=CARTESIAN_POINT('Ctrl Pts',(-0.48005369284309,-0.329294854011373,
-1.64463294051778));
#67065=CARTESIAN_POINT('Ctrl Pts',(-0.263720533328036,-0.518977965998399,
-1.63072331057202));
#67066=CARTESIAN_POINT('Ctrl Pts',(0.017031545264937,-0.581890518359379,
-1.61681368062626));
#67067=CARTESIAN_POINT('Ctrl Pts',(0.293623334469941,-0.502664884734763,
-1.6029040506805));
#67068=CARTESIAN_POINT('Ctrl Pts',(0.498491858201794,-0.300653481930913,
-1.58899442073474));
#67069=CARTESIAN_POINT('Ctrl Pts',(0.581593956432909,-0.0252015620820308,
-1.57508479078899));
#67070=CARTESIAN_POINT('Ctrl Pts',(0.522630309752701,0.256406334201118,
-1.56117516084322));
#67071=CARTESIAN_POINT('Ctrl Pts',(0.336003946761551,0.475381948175695,
-1.54726553089747));
#67072=CARTESIAN_POINT('Ctrl Pts',(0.0673020214956575,0.578236185994319,
-1.53335590095171));
#67073=CARTESIAN_POINT('Ctrl Pts',(-0.217839744164144,0.539844880269471,
-1.51944627100595));
#67074=CARTESIAN_POINT('Ctrl Pts',(-0.449769874483405,0.369585861333793,
-1.50553664106019));
#67075=CARTESIAN_POINT('Ctrl Pts',(-0.571834880603205,0.109048238024178,
-1.49162701111443));
#67076=CARTESIAN_POINT('Ctrl Pts',(-0.554217987726959,-0.17812655885785,
-1.47771738116867));
#67077=CARTESIAN_POINT('Ctrl Pts',(-0.401222467891465,-0.421790445778163,
-1.46380775122291));
#67078=CARTESIAN_POINT('Ctrl Pts',(-0.150220481266396,-0.562423733406362,
-1.44989812127715));
#67079=CARTESIAN_POINT('Ctrl Pts',(0.137475807863018,-0.565673979552772,
-1.4359884913314));
#67080=CARTESIAN_POINT('Ctrl Pts',(0.391590931240414,-0.430747247769412,
-1.42207886138564));
#67081=CARTESIAN_POINT('Ctrl Pts',(0.550052279794577,-0.190602041918361,
-1.40816923143988));
#67082=CARTESIAN_POINT('Ctrl Pts',(0.574152557356071,0.0961014556192658,
-1.39425960149412));
#67083=CARTESIAN_POINT('Ctrl Pts',(0.458004797861252,0.359330285429343,
-1.38034997154836));
#67084=CARTESIAN_POINT('Ctrl Pts',(0.229980372418605,0.534785636674041,
-1.3664403416026));
#67085=CARTESIAN_POINT('Ctrl Pts',(-0.05422127522735,0.579609094306998,
-1.35253071165684));
#67086=CARTESIAN_POINT('Ctrl Pts',(-0.325178311628612,0.482851648580621,
-1.33862108171108));
#67087=CARTESIAN_POINT('Ctrl Pts',(-0.516704159724784,0.26814820568813,
-1.32471145176532));
#67088=CARTESIAN_POINT('Ctrl Pts',(-0.582014870029119,-0.01205570220466,
-1.31080182181956));
#67089=CARTESIAN_POINT('Ctrl Pts',(-0.505157019010565,-0.289314768090083,
-1.2968921918738));
#67090=CARTESIAN_POINT('Ctrl Pts',(-0.304904646076622,-0.495903020450117,
-1.28298256192805));
#67091=CARTESIAN_POINT('Ctrl Pts',(-0.0301733257728146,-0.581357221768566,
-1.26907293198229));
#67092=CARTESIAN_POINT('Ctrl Pts',(0.251928421879756,-0.524803505266338,
-1.25516330203653));
#67093=CARTESIAN_POINT('Ctrl Pts',(0.472491705243263,-0.340056226772827,
-1.24125367209077));
#67094=CARTESIAN_POINT('Ctrl Pts',(0.577639611044211,-0.0722435370351632,
-1.22734404214501));
#67095=CARTESIAN_POINT('Ctrl Pts',(0.541687698448494,0.213216055305955,
-1.21343441219925));
#67096=CARTESIAN_POINT('Ctrl Pts',(0.373417928113377,0.446593439107845,
-1.19952478225349));
#67097=CARTESIAN_POINT('Ctrl Pts',(0.113933495841189,0.570881605428012,
-1.18561515230773));
#67098=CARTESIAN_POINT('Ctrl Pts',(-0.173381430159482,0.555720728933618,
-1.17170552236198));
#67099=CARTESIAN_POINT('Ctrl Pts',(-0.418344537065485,0.404814151430164,
-1.15779589241621));
#67100=CARTESIAN_POINT('Ctrl Pts',(-0.561118775551487,0.155023767901115,
-1.14388626247046));
#67101=CARTESIAN_POINT('Ctrl Pts',(-0.566828734137865,-0.132634215217362,
-1.1299766325247));
#67102=CARTESIAN_POINT('Ctrl Pts',(-0.434079643310568,-0.387893686664309,
-1.11606700257894));
#67103=CARTESIAN_POINT('Ctrl Pts',(-0.195298075364724,-0.548402507880383,
-1.10215737263318));
#67104=CARTESIAN_POINT('Ctrl Pts',(0.091188882655331,-0.574953247291231,
-1.08824774268742));
#67105=CARTESIAN_POINT('Ctrl Pts',(0.35540116536494,-0.461060365405552,
-1.07433811274166));
#67106=CARTESIAN_POINT('Ctrl Pts',(0.532799734243006,-0.23454443519564,
-1.0604284827959));
#67107=CARTESIAN_POINT('Ctrl Pts',(0.580051505176277,0.0492635791776641,
-1.04651885285014));
#67108=CARTESIAN_POINT('Ctrl Pts',(0.48561430520755,0.321037996923179,-1.03260922290439));
#67109=CARTESIAN_POINT('Ctrl Pts',(0.272556274939904,0.514392579535847,
-1.01869959295862));
#67110=CARTESIAN_POINT('Ctrl Pts',(-0.00707897780625726,0.582096673211485,
-1.00478996301287));
#67111=CARTESIAN_POINT('Ctrl Pts',(-0.284985051209799,0.507612223530529,
-0.990880333067108));
#67112=CARTESIAN_POINT('Ctrl Pts',(-0.493277929460783,0.309133520016096,
-0.976970703121349));
#67113=CARTESIAN_POINT('Ctrl Pts',(-0.581077986694556,0.03514288362756,
-0.96306107317559));
#67114=CARTESIAN_POINT('Ctrl Pts',(-0.526938334757956,-0.247432092205459,
-0.94915144322983));
#67115=CARTESIAN_POINT('Ctrl Pts',(-0.344083646804031,-0.469566920569047,
-0.935241813284073));
#67116=CARTESIAN_POINT('Ctrl Pts',(-0.0771797711748603,-0.577000807462221,
-0.921332183338313));
#67117=CARTESIAN_POINT('Ctrl Pts',(0.208576779181695,-0.543490916278138,
-0.907422553392554));
#67118=CARTESIAN_POINT('Ctrl Pts',(0.443384355296167,-0.377222695989068,
-0.893512923446795));
#67119=CARTESIAN_POINT('Ctrl Pts',(0.569886595668309,-0.118810424493158,
-0.879603293501035));
#67120=CARTESIAN_POINT('Ctrl Pts',(0.557182843899205,0.168623626325179,
-0.865693663555278));
#67121=CARTESIAN_POINT('Ctrl Pts',(0.408376240828409,0.414868045066761,
-0.851784033609518));
#67122=CARTESIAN_POINT('Ctrl Pts',(0.159815721445959,0.559772796828648,
-0.837874403663759));
#67123=CARTESIAN_POINT('Ctrl Pts',(-0.127782926281245,0.567942050425623,
-0.823964773718));
#67124=CARTESIAN_POINT('Ctrl Pts',(-0.384168084926761,0.437380305242891,
-0.810055143772241));
#67125=CARTESIAN_POINT('Ctrl Pts',(-0.546712644727315,0.199979831447884,
-0.796145513826482));
#67126=CARTESIAN_POINT('Ctrl Pts',(-0.57571190498247,-0.0862696432826438,
-0.782235883880722));
#67127=CARTESIAN_POINT('Ctrl Pts',(-0.46408222690187,-0.351446063521076,
-0.768326253934965));
#67128=CARTESIAN_POINT('Ctrl Pts',(-0.23909135148475,-0.530774881221648,
-0.754416623989205));
#67129=CARTESIAN_POINT('Ctrl Pts',(0.044302281689456,-0.58045151109095,
-0.740506994043447));
#67130=CARTESIAN_POINT('Ctrl Pts',(0.316874212574861,-0.488341460758475,
-0.726597364097687));
#67131=CARTESIAN_POINT('Ctrl Pts',(0.512043394420817,-0.276944418829243,
-0.712687734151928));
#67132=CARTESIAN_POINT('Ctrl Pts',(0.582135921926214,0.00210173589565668,
-0.698778104206169));
#67133=CARTESIAN_POINT('Ctrl Pts',(0.510030318805702,0.280634500355199,
-0.684868474260411));
#67134=CARTESIAN_POINT('Ctrl Pts',(0.313339794595404,0.490616777142373,
-0.670958844314651));
#67135=CARTESIAN_POINT('Ctrl Pts',(0.0401098723442771,0.580756271624496,
-0.657049214368893));
#67136=CARTESIAN_POINT('Ctrl Pts',(-0.242917673884644,0.529034642159786,
-0.643139584423133));
#67137=CARTESIAN_POINT('Ctrl Pts',(-0.46660780797089,0.348085912428613,
-0.629229954477375));
#67138=CARTESIAN_POINT('Ctrl Pts',(-0.576319821948403,0.0821103630488868,
-0.615320324531615));
#67139=CARTESIAN_POINT('Ctrl Pts',(-0.54525440193326,-0.203922254947967,
-0.601410694585856));
#67140=CARTESIAN_POINT('Ctrl Pts',(-0.380999886811408,-0.440142857650052,
-0.587501064640097));
#67141=CARTESIAN_POINT('Ctrl Pts',(-0.123678667449767,-0.568849924064782,
-0.573591434694338));
#67142=CARTESIAN_POINT('Ctrl Pts',(0.163853495176574,-0.558604225735071,
-0.55968180474858));
#67143=CARTESIAN_POINT('Ctrl Pts',(0.411361223932671,-0.411908475677878,
-0.545772174802822));
#67144=CARTESIAN_POINT('Ctrl Pts',(0.558385895636291,-0.164595991582775,
-0.531862544857061));
#67145=CARTESIAN_POINT('Ctrl Pts',(0.569013847026506,0.12292229571057,-0.517952914911304));
#67146=CARTESIAN_POINT('Ctrl Pts',(0.440648992269832,0.380414398389757,
-0.504043284965543));
#67147=CARTESIAN_POINT('Ctrl Pts',(0.204646967905711,0.544982813873664,
-0.490133655019786));
#67148=CARTESIAN_POINT('Ctrl Pts',(-0.0813440971246574,0.57642847496774,
-0.476224025074025));
#67149=CARTESIAN_POINT('Ctrl Pts',(-0.347465269037444,0.467070161435511,
-0.462314395128267));
#67150=CARTESIAN_POINT('Ctrl Pts',(-0.528711225637859,0.243620788881355,
-0.448404765182507));
#67151=CARTESIAN_POINT('Ctrl Pts',(-0.580809082808382,-0.0393377454608579,
-0.434495135236749));
#67152=CARTESIAN_POINT('Ctrl Pts',(-0.491032915863341,-0.312687262979163,
-0.42058550529099));
#67153=CARTESIAN_POINT('Ctrl Pts',(-0.281312316558704,-0.509656776118064,
-0.406675875345232));
#67154=CARTESIAN_POINT('Ctrl Pts',(-0.00287565966342121,-0.582132613303954,
-0.392766245399472));
#67155=CARTESIAN_POINT('Ctrl Pts',(0.27626343357552,-0.512411128060141,
-0.378856615453714));
#67156=CARTESIAN_POINT('Ctrl Pts',(0.487919758039686,-0.317523162312504,
-0.364946985507953));
#67157=CARTESIAN_POINT('Ctrl Pts',(0.580392100077682,-0.0450739288092028,
-0.351037355562195));
#67158=CARTESIAN_POINT('Ctrl Pts',(0.531092274219919,0.23838549694698,-0.337127725616436));
#67159=CARTESIAN_POINT('Ctrl Pts',(0.352062731059539,0.46361458377452,-0.323218095670677));
#67160=CARTESIAN_POINT('Ctrl Pts',(0.0870349522026898,0.57559670428983,
-0.309308465724917));
#67161=CARTESIAN_POINT('Ctrl Pts',(-0.199252822873789,0.546978026486944,
-0.295398835779159));
#67162=CARTESIAN_POINT('Ctrl Pts',(-0.436869183145239,0.38474922445954,
-0.2814892058334));
#67163=CARTESIAN_POINT('Ctrl Pts',(-0.567771666395103,0.12853786879123,
-0.267579575887641));
#67164=CARTESIAN_POINT('Ctrl Pts',(-0.559984770547422,-0.159071385388608,
-0.253669945941883));
#67165=CARTESIAN_POINT('Ctrl Pts',(-0.415410597719517,-0.40782433012463,
-0.239760315996123));
#67166=CARTESIAN_POINT('Ctrl Pts',(-0.169364228912487,-0.556958173181869,
-0.225850686050364));
#67167=CARTESIAN_POINT('Ctrl Pts',(0.118052678971086,-0.570044045943112,
-0.211941056104605));
#67168=CARTESIAN_POINT('Ctrl Pts',(0.376632901220441,-0.443885464735316,
-0.198031426158846));
#67169=CARTESIAN_POINT('Ctrl Pts',(0.543213142264004,-0.209299144906713,
-0.184121796213087));
#67170=CARTESIAN_POINT('Ctrl Pts',(0.577102903915469,0.0764126069263521,
-0.170212166267328));
#67171=CARTESIAN_POINT('Ctrl Pts',(0.470023952420832,0.343459067734565,
-0.156302536321569));
#67172=CARTESIAN_POINT('Ctrl Pts',(0.248132412646873,0.526608928509874,
-0.14239290637581));
#67173=CARTESIAN_POINT('Ctrl Pts',(-0.0343703263707898,0.581124174352056,
-0.128483276430052));
#67174=CARTESIAN_POINT('Ctrl Pts',(-0.308477468009576,0.493688512513425,
-0.114573646484293));
#67175=CARTESIAN_POINT('Ctrl Pts',(-0.507232872173408,0.285659573106642,
-0.100664016538534));
#67176=CARTESIAN_POINT('Ctrl Pts',(-0.582086800194928,0.00785299289084335,
-0.0867543865927742));
#67177=CARTESIAN_POINT('Ctrl Pts',(-0.514754374468628,-0.271872459345322,
-0.0728447566470155));
#67178=CARTESIAN_POINT('Ctrl Pts',(-0.321683518120199,-0.485186504876865,
-0.0589351267012566));
#67179=CARTESIAN_POINT('Ctrl Pts',(-0.0500342978791844,-0.579986601383926,
-0.0450254967554975));
#67180=CARTESIAN_POINT('Ctrl Pts',(0.233835126413185,-0.533108926076464,
-0.0311158668097387));
#67181=CARTESIAN_POINT('Ctrl Pts',(0.460588964113884,-0.356018023025415,
-0.0172062368639799));
#67182=CARTESIAN_POINT('Ctrl Pts',(0.574828579379531,-0.0919449288341774,
-0.00329660691822081));
#67183=CARTESIAN_POINT('Ctrl Pts',(0.548667414168985,0.194552461871164,
0.010613023027538));
#67184=CARTESIAN_POINT('Ctrl Pts',(0.388458879975545,0.433598146048481,
0.0245226529732968));
#67185=CARTESIAN_POINT('Ctrl Pts',(0.21842861762083,0.522236456518856,0.033795739603803));
#67186=CARTESIAN_POINT('Ctrl Pts',(0.127946201224893,0.543535668558097,
0.0384322829190561));
#67187=CARTESIAN_POINT('Ctrl Pts',(-0.258391981634413,0.532271443393351,
-3.948325));
#67188=CARTESIAN_POINT('Ctrl Pts',(-0.346999241769787,0.489256914213255,
-3.94368845668475));
#67189=CARTESIAN_POINT('Ctrl Pts',(-0.502226568239526,0.358164595428381,
-3.93441537005424));
#67190=CARTESIAN_POINT('Ctrl Pts',(-0.612402242308734,0.0738461192841877,
-3.92050574010848));
#67191=CARTESIAN_POINT('Ctrl Pts',(-0.572977832471654,-0.228431041127055,
-3.90659611016272));
#67192=CARTESIAN_POINT('Ctrl Pts',(-0.393597009266127,-0.474948554308979,
-3.89268648021697));
#67193=CARTESIAN_POINT('Ctrl Pts',(-0.118069979218058,-0.60543068831445,
-3.8787768502712));
#67194=CARTESIAN_POINT('Ctrl Pts',(0.186296727754779,-0.588034642792585,
-3.86486722032545));
#67195=CARTESIAN_POINT('Ctrl Pts',(0.445157432417822,-0.426994391371127,
-3.85095759037968));
#67196=CARTESIAN_POINT('Ctrl Pts',(0.595279368990698,-0.161655034790457,
-3.83704796043393));
#67197=CARTESIAN_POINT('Ctrl Pts',(0.599992795452154,0.143173100143741,
-3.82313833048817));
#67198=CARTESIAN_POINT('Ctrl Pts',(0.458146114515487,0.413027696829806,
-3.80922870054241));
#67199=CARTESIAN_POINT('Ctrl Pts',(0.204388291644403,0.581992524500238,
-3.79531907059665));
#67200=CARTESIAN_POINT('Ctrl Pts',(-0.0992954073423366,0.608794066560272,
-3.78140944065089));
#67201=CARTESIAN_POINT('Ctrl Pts',(-0.378724241805151,0.486885796148415,
-3.76749981070513));
#67202=CARTESIAN_POINT('Ctrl Pts',(-0.565642248827353,0.246046060955832,
-3.75359018075937));
#67203=CARTESIAN_POINT('Ctrl Pts',(-0.614391025794256,-0.0548952318615489,
-3.73968055081362));
#67204=CARTESIAN_POINT('Ctrl Pts',(-0.51306273113035,-0.342427298829336,
-3.72577092086785));
#67205=CARTESIAN_POINT('Ctrl Pts',(-0.286408788336976,-0.546314767223382,
-3.71186129092209));
#67206=CARTESIAN_POINT('Ctrl Pts',(0.0102061249614486,-0.616754128750851,
-3.69795166097634));
#67207=CARTESIAN_POINT('Ctrl Pts',(0.304327992019713,-0.536539181138772,
-3.68404203103058));
#67208=CARTESIAN_POINT('Ctrl Pts',(0.52411177068089,-0.325264003104992,
-3.67013240108482));
#67209=CARTESIAN_POINT('Ctrl Pts',(0.6158709571608,-0.034536704499633,-3.65622277113906));
#67210=CARTESIAN_POINT('Ctrl Pts',(0.557191568159499,0.264626862168828,
-3.6423131411933));
#67211=CARTESIAN_POINT('Ctrl Pts',(0.362407196798647,0.499150121257423,
-3.62840351124754));
#67212=CARTESIAN_POINT('Ctrl Pts',(0.0790977508404253,0.611746161108203,
-3.61449388130178));
#67213=CARTESIAN_POINT('Ctrl Pts',(-0.223532874039147,0.574911187971986,
-3.60058425135602));
#67214=CARTESIAN_POINT('Ctrl Pts',(-0.471561204809241,0.397642867338423,
-3.58667462141027));
#67215=CARTESIAN_POINT('Ctrl Pts',(-0.604401451019528,0.123242467652703,
-3.57276499146451));
#67216=CARTESIAN_POINT('Ctrl Pts',(-0.58960477388398,-0.181262324935473,
-3.55885536151875));
#67217=CARTESIAN_POINT('Ctrl Pts',(-0.430785552361987,-0.441490235116783,
-3.54494573157299));
#67218=CARTESIAN_POINT('Ctrl Pts',(-0.166738500123487,-0.593875485606428,
-3.53103610162723));
#67219=CARTESIAN_POINT('Ctrl Pts',(0.1380377050979,-0.601194986505021,-3.51712647168147));
#67220=CARTESIAN_POINT('Ctrl Pts',(0.409095490133358,-0.461660805982183,
-3.50321684173571));
#67221=CARTESIAN_POINT('Ctrl Pts',(0.580223668090182,-0.209356907732974,
-3.48930721178996));
#67222=CARTESIAN_POINT('Ctrl Pts',(0.609620820972426,0.0940865264766722,
-3.4753975818442));
#67223=CARTESIAN_POINT('Ctrl Pts',(0.490106116901962,0.37454747897006,-3.46148795189844));
#67224=CARTESIAN_POINT('Ctrl Pts',(0.250873369318255,0.563517854548059,
-3.44757832195268));
#67225=CARTESIAN_POINT('Ctrl Pts',(-0.0496401252477701,0.614837928069609,
-3.43366869200692));
#67226=CARTESIAN_POINT('Ctrl Pts',(-0.338028044413961,0.515971763779004,
-3.41975906206116));
#67227=CARTESIAN_POINT('Ctrl Pts',(-0.543845975705585,0.291069363788744,
-3.4058494321154));
#67228=CARTESIAN_POINT('Ctrl Pts',(-0.616818847654587,-0.00493244418218084,
-3.39193980216964));
#67229=CARTESIAN_POINT('Ctrl Pts',(-0.539121603282495,-0.299729405800725,
-3.37803017222388));
#67230=CARTESIAN_POINT('Ctrl Pts',(-0.329733320306996,-0.521311574115583,
-3.36412054227812));
#67231=CARTESIAN_POINT('Ctrl Pts',(-0.0398011987077191,-0.61555315319554,
-3.35021091233237));
#67232=CARTESIAN_POINT('Ctrl Pts',(0.259853147272044,-0.559433786681102,
-3.3363012823866));
#67233=CARTESIAN_POINT('Ctrl Pts',(0.496033259163867,-0.366661731887602,
-3.32239165244085));
#67234=CARTESIAN_POINT('Ctrl Pts',(0.611047506650708,-0.0843253487599979,
-3.30848202249508));
#67235=CARTESIAN_POINT('Ctrl Pts',(0.576801401191375,0.218609156741456,
-3.29457239254933));
#67236=CARTESIAN_POINT('Ctrl Pts',(0.401660226552276,0.468144082771018,
-3.28066276260357));
#67237=CARTESIAN_POINT('Ctrl Pts',(0.128405653974211,0.603325623403315,
-3.26675313265781));
#67238=CARTESIAN_POINT('Ctrl Pts',(-0.176214521153363,0.59113303271111,
-3.25284350271205));
#67239=CARTESIAN_POINT('Ctrl Pts',(-0.437790839076186,0.434544590403002,
-3.23893387276629));
#67240=CARTESIAN_POINT('Ctrl Pts',(-0.592428147436097,0.17181009851862,
-3.22502424282053));
#67241=CARTESIAN_POINT('Ctrl Pts',(-0.602353246975706,-0.132892383850119,
-3.21111461287477));
#67242=CARTESIAN_POINT('Ctrl Pts',(-0.465141737228301,-0.405133291788988,
-3.19720498292902));
#67243=CARTESIAN_POINT('Ctrl Pts',(-0.214310223941008,-0.578412437402498,
-3.18329535298325));
#67244=CARTESIAN_POINT('Ctrl Pts',(0.0888707700613648,-0.61040298660495,
-3.1693857230375));
#67245=CARTESIAN_POINT('Ctrl Pts',(0.37034333327631,-0.493290619539167,
-3.15547609309174));
#67246=CARTESIAN_POINT('Ctrl Pts',(0.561352264720504,-0.255682331655327,
-3.14156646314598));
#67247=CARTESIAN_POINT('Ctrl Pts',(0.615239881950394,0.0443813866976684,
-3.12765683320022));
#67248=CARTESIAN_POINT('Ctrl Pts',(0.518843076239383,0.333604079810181,
-3.11374720325446));
#67249=CARTESIAN_POINT('Ctrl Pts',(0.295708660374863,0.541337425278215,
-3.0998375733087));
#67250=CARTESIAN_POINT('Ctrl Pts',(0.000341597234319436,0.616838474107179,
-3.08592794336294));
#67251=CARTESIAN_POINT('Ctrl Pts',(-0.295108907738821,0.541664612468586,
-3.07201831341719));
#67252=CARTESIAN_POINT('Ctrl Pts',(-0.518473266794936,0.334178532294536,
-3.05810868347143));
#67253=CARTESIAN_POINT('Ctrl Pts',(-0.615190348916484,0.0450627831758913,
-3.04419905352566));
#67254=CARTESIAN_POINT('Ctrl Pts',(-0.561635107513367,-0.255060435653969,
-3.03028942357991));
#67255=CARTESIAN_POINT('Ctrl Pts',(-0.370889461989462,-0.492880134325488,
-3.01637979363415));
#67256=CARTESIAN_POINT('Ctrl Pts',(-0.0895467820320154,-0.610304181253294,
-3.00247016368839));
#67257=CARTESIAN_POINT('Ctrl Pts',(0.213669457911877,-0.578649447060298,
-2.98856053374263));
#67258=CARTESIAN_POINT('Ctrl Pts',(0.464692736826349,-0.405648222193048,
-2.97465090379687));
#67259=CARTESIAN_POINT('Ctrl Pts',(0.602205689366357,-0.133559453137302,
-2.96074127385111));
#67260=CARTESIAN_POINT('Ctrl Pts',(0.592618076463096,0.171153835121284,
-2.94683164390535));
#67261=CARTESIAN_POINT('Ctrl Pts',(0.438271860844959,0.434059438117684,
-2.9329220139596));
#67262=CARTESIAN_POINT('Ctrl Pts',(0.176869136650822,0.590937499510681,
-2.91901238401383));
#67263=CARTESIAN_POINT('Ctrl Pts',(-0.127737347438336,0.603467472111763,
-2.90510275406808));
#67264=CARTESIAN_POINT('Ctrl Pts',(-0.401141475973243,0.46858866405575,
-2.89119312412232));
#67265=CARTESIAN_POINT('Ctrl Pts',(-0.576558921585075,0.219247872893211,
-2.87728349417656));
#67266=CARTESIAN_POINT('Ctrl Pts',(-0.61114052842268,-0.0836485167040743,
-2.8633738642308));
#67267=CARTESIAN_POINT('Ctrl Pts',(-0.496439059919587,-0.366112113448463,
-2.84946423428504));
#67268=CARTESIAN_POINT('Ctrl Pts',(-0.260472602208015,-0.55914563695564,
-2.83555460433928));
#67269=CARTESIAN_POINT('Ctrl Pts',(0.0391194036241582,-0.615596858412739,
-2.82164497439352));
#67270=CARTESIAN_POINT('Ctrl Pts',(0.329155726913755,-0.521676458417879,
-2.80773534444777));
#67271=CARTESIAN_POINT('Ctrl Pts',(0.538789300108363,-0.300326339031866,
-2.793825714502));
#67272=CARTESIAN_POINT('Ctrl Pts',(0.616813006275451,-0.00561561367818421,
-2.77991608455625));
#67273=CARTESIAN_POINT('Ctrl Pts',(0.54416802299301,0.29046683559302,-2.76600645461049));
#67274=CARTESIAN_POINT('Ctrl Pts',(0.338599313993788,0.515597056227515,
-2.75209682466473));
#67275=CARTESIAN_POINT('Ctrl Pts',(0.0503210733068214,0.614782570840124,
-2.73818719471897));
#67276=CARTESIAN_POINT('Ctrl Pts',(-0.250249077715523,0.563795369730963,
-2.72427756477321));
#67277=CARTESIAN_POINT('Ctrl Pts',(-0.489690977239046,0.375090078032214,
-2.71036793482745));
#67278=CARTESIAN_POINT('Ctrl Pts',(-0.609516239264299,0.094761668941873,
-2.69645830488169));
#67279=CARTESIAN_POINT('Ctrl Pts',(-0.580455190472774,-0.208714138669999,
-2.68254867493593));
#67280=CARTESIAN_POINT('Ctrl Pts',(-0.409606562718208,-0.461207419287372,
-2.66863904499017));
#67281=CARTESIAN_POINT('Ctrl Pts',(-0.138703488369955,-0.601041730782106,
-2.65472941504442));
#67282=CARTESIAN_POINT('Ctrl Pts',(0.166080636802718,-0.594059796575014,
-2.64081978509865));
#67283=CARTESIAN_POINT('Ctrl Pts',(0.430296305027459,-0.441967091203926,
-2.6269101551529));
#67284=CARTESIAN_POINT('Ctrl Pts',(0.589403650804615,-0.181915244676564,
-2.61300052520714));
#67285=CARTESIAN_POINT('Ctrl Pts',(0.60453758045727,0.12257297272406,-2.59909089526138));
#67286=CARTESIAN_POINT('Ctrl Pts',(0.472001334475186,0.397120334509814,
-2.58518126531562));
#67287=CARTESIAN_POINT('Ctrl Pts',(0.224169493620305,0.574663256140115,
-2.57127163536986));
#67288=CARTESIAN_POINT('Ctrl Pts',(-0.0784201481802541,0.61183339250725,
-2.5573620054241));
#67289=CARTESIAN_POINT('Ctrl Pts',(-0.361854128811955,0.499551207874913,
-2.54345237547834));
#67290=CARTESIAN_POINT('Ctrl Pts',(-0.556898132570094,0.265243830781198,
-2.52954274553259));
#67291=CARTESIAN_POINT('Ctrl Pts',(-0.615908831359701,-0.0338545607071286,
-2.51563311558682));
#67292=CARTESIAN_POINT('Ctrl Pts',(-0.524471703178682,-0.324683310923731,
-2.50172348564107));
#67293=CARTESIAN_POINT('Ctrl Pts',(-0.304922062182061,-0.536201786477984,
-2.48781385569531));
#67294=CARTESIAN_POINT('Ctrl Pts',(-0.0108892195898121,-0.616742446021246,
-2.47390422574955));
#67295=CARTESIAN_POINT('Ctrl Pts',(0.285803528724323,-0.54663165184269,
-2.45999459580379));
#67296=CARTESIAN_POINT('Ctrl Pts',(0.512683152680125,-0.342995342221306,
-2.44608496585803));
#67297=CARTESIAN_POINT('Ctrl Pts',(0.61432984877728,-0.0555756846905864,
-2.43217533591227));
#67298=CARTESIAN_POINT('Ctrl Pts',(0.565914415406841,0.245419425193436,
-2.41826570596651));
#67299=CARTESIAN_POINT('Ctrl Pts',(0.379263272927718,0.486466021049465,
-2.40435607602075));
#67300=CARTESIAN_POINT('Ctrl Pts',(0.0999696282526544,0.608683738286615,
-2.390446446075));
#67301=CARTESIAN_POINT('Ctrl Pts',(-0.203743561276915,0.582218499419028,
-2.37653681612924));
#67302=CARTESIAN_POINT('Ctrl Pts',(-0.45768838494997,0.413534958751291,
-2.36262718618348));
#67303=CARTESIAN_POINT('Ctrl Pts',(-0.599833832742337,0.143837383614901,
-2.34871755623772));
#67304=CARTESIAN_POINT('Ctrl Pts',(-0.595458087649196,-0.160995297076361,
-2.33480792629196));
#67305=CARTESIAN_POINT('Ctrl Pts',(-0.445630011338248,-0.426501714911226,
-2.3208982963462));
#67306=CARTESIAN_POINT('Ctrl Pts',(-0.186948053697615,-0.58782671345067,
-2.30698866640044));
#67307=CARTESIAN_POINT('Ctrl Pts',(0.117399637251469,-0.605563493781425,
-2.29307903645468));
#67308=CARTESIAN_POINT('Ctrl Pts',(0.393070161366252,-0.475379499001643,
-2.27916940650892));
#67309=CARTESIAN_POINT('Ctrl Pts',(0.57272557965118,-0.22907472632476,-2.26525977656316));
#67310=CARTESIAN_POINT('Ctrl Pts',(0.612481528206489,0.0731860467123818,
-2.2513501466174));
#67311=CARTESIAN_POINT('Ctrl Pts',(0.50262683589002,0.357569690648873,-2.23744051667165));
#67312=CARTESIAN_POINT('Ctrl Pts',(0.269995668571828,0.554609915868798,
-2.22353088672589));
#67313=CARTESIAN_POINT('Ctrl Pts',(-0.0285872428355586,0.616175777984337,
-2.20962125678013));
#67314=CARTESIAN_POINT('Ctrl Pts',(-0.320187158798318,0.527228606174024,
-2.19571162683437));
#67315=CARTESIAN_POINT('Ctrl Pts',(-0.53357507354856,0.309495493852806,
-2.18180199688861));
#67316=CARTESIAN_POINT('Ctrl Pts',(-0.6166267985029,0.0161620294396055,
-2.16789236694285));
#67317=CARTESIAN_POINT('Ctrl Pts',(-0.549055318912811,-0.281119328046106,
-2.15398273699709));
#67318=CARTESIAN_POINT('Ctrl Pts',(-0.34736629560325,-0.509731769175141,
-2.14007310705134));
#67319=CARTESIAN_POINT('Ctrl Pts',(-0.0608262331862064,-0.613832215824423,
-2.12616347710557));
#67320=CARTESIAN_POINT('Ctrl Pts',(0.240571831161854,-0.567992089627114,
-2.11225384715982));
#67321=CARTESIAN_POINT('Ctrl Pts',(0.483205501518772,-0.383408741592487,
-2.09834421721406));
#67322=CARTESIAN_POINT('Ctrl Pts',(0.607806739180643,-0.1051702792339,-2.0844345872683));
#67323=CARTESIAN_POINT('Ctrl Pts',(0.583939244991481,0.198758089109155,
-2.07052495732254));
#67324=CARTESIAN_POINT('Ctrl Pts',(0.417433123104956,0.454135891074891,
-2.05661532737678));
#67325=CARTESIAN_POINT('Ctrl Pts',(0.148960763556184,0.598582083551038,
-2.04270569743102));
#67326=CARTESIAN_POINT('Ctrl Pts',(-0.155898187708505,0.596812847462877,
-2.02879606748526));
#67327=CARTESIAN_POINT('Ctrl Pts',(-0.422675945174393,0.449260353468318,
-2.0148864375395));
#67328=CARTESIAN_POINT('Ctrl Pts',(-0.586206802731642,0.19196719578795,
-2.00097680759374));
#67329=CARTESIAN_POINT('Ctrl Pts',(-0.606545137084321,-0.112217719219845,
-1.98706717764799));
#67330=CARTESIAN_POINT('Ctrl Pts',(-0.478722910672709,-0.388991252632488,
-1.97315754770223));
#67331=CARTESIAN_POINT('Ctrl Pts',(-0.233963212407088,-0.570746033773078,
-1.95924791775647));
#67332=CARTESIAN_POINT('Ctrl Pts',(0.067946594942059,-0.613084888138114,
-1.94533828781071));
#67333=CARTESIAN_POINT('Ctrl Pts',(0.353259112175203,-0.505665719119589,
-1.93142865786495));
#67334=CARTESIAN_POINT('Ctrl Pts',(0.552281154132965,-0.274727768194447,
-1.91751902791919));
#67335=CARTESIAN_POINT('Ctrl Pts',(0.616397678771389,0.023317835079334,
-1.90360939797343));
#67336=CARTESIAN_POINT('Ctrl Pts',(0.529946965859142,0.31566759923095,-1.88969976802767));
#67337=CARTESIAN_POINT('Ctrl Pts',(0.314046299701105,0.530909353347243,
-1.87579013808191));
#67338=CARTESIAN_POINT('Ctrl Pts',(0.0214336577561771,0.616466072174888,
-1.86188050813615));
#67339=CARTESIAN_POINT('Ctrl Pts',(-0.276414575999195,0.551438847019983,
-1.84797087819039));
#67340=CARTESIAN_POINT('Ctrl Pts',(-0.506743121474926,0.351711854598891,
-1.83406124824464));
#67341=CARTESIAN_POINT('Ctrl Pts',(-0.613289708361258,0.0660723349497104,
-1.82015161829888));
#67342=CARTESIAN_POINT('Ctrl Pts',(-0.570028240502371,-0.235706650006559,
-1.80624198835312));
#67343=CARTESIAN_POINT('Ctrl Pts',(-0.387526180969968,-0.479909657008872,
-1.79233235840736));
#67344=CARTESIAN_POINT('Ctrl Pts',(-0.11036324168943,-0.60688530605984,
-1.7784227284616));
#67345=CARTESIAN_POINT('Ctrl Pts',(0.193758086632153,-0.585617301394169,
-1.76451309851584));
#67346=CARTESIAN_POINT('Ctrl Pts',(0.450550197368985,-0.421300770801945,
-1.75060346857009));
#67347=CARTESIAN_POINT('Ctrl Pts',(0.59728657471796,-0.154073253646539,
-1.73669383862432));
#67348=CARTESIAN_POINT('Ctrl Pts',(0.598123976975661,0.150789681325887,
-1.72278420867856));
#67349=CARTESIAN_POINT('Ctrl Pts',(0.452857852196158,0.418819275501768,
-1.7088745787328));
#67350=CARTESIAN_POINT('Ctrl Pts',(0.196972304020687,0.584544037071908,
-1.69496494878705));
#67351=CARTESIAN_POINT('Ctrl Pts',(-0.107027597455884,0.607482438602438,
-1.68105531884129));
#67352=CARTESIAN_POINT('Ctrl Pts',(-0.38488390649918,0.482031325066612,
-1.66714568889553));
#67353=CARTESIAN_POINT('Ctrl Pts',(-0.568724763221498,0.238834594492074,
-1.65323605894977));
#67354=CARTESIAN_POINT('Ctrl Pts',(-0.613643428193194,-0.0627021759020232,
-1.63932642900401));
#67355=CARTESIAN_POINT('Ctrl Pts',(-0.508667635404544,-0.348922708517937,
-1.62541679905825));
#67356=CARTESIAN_POINT('Ctrl Pts',(-0.279439783706537,-0.549912017607897,
-1.61150716911249));
#67357=CARTESIAN_POINT('Ctrl Pts',(0.0180467226611512,-0.616574517498683,
-1.59759753916674));
#67358=CARTESIAN_POINT('Ctrl Pts',(0.311124962626296,-0.53262658350699,
-1.58368790922097));
#67359=CARTESIAN_POINT('Ctrl Pts',(0.52820482075284,-0.318574147038023,
-1.56977827927522));
#67360=CARTESIAN_POINT('Ctrl Pts',(0.616260278787186,-0.0267037191545109,
-1.55586864932946));
#67361=CARTESIAN_POINT('Ctrl Pts',(0.553782061915196,0.271689616526834,
-1.5419590193837));
#67362=CARTESIAN_POINT('Ctrl Pts',(0.356031701523973,0.503717428066061,
-1.52804938943794));
#67363=CARTESIAN_POINT('Ctrl Pts',(0.071313606462209,0.612702366048064,
-1.51413975949218));
#67364=CARTESIAN_POINT('Ctrl Pts',(-0.230824237399053,0.572022719178783,
-1.50023012954642));
#67365=CARTESIAN_POINT('Ctrl Pts',(-0.476578728464133,0.391615290052691,
-1.48632049960066));
#67366=CARTESIAN_POINT('Ctrl Pts',(-0.605919506286032,0.115548135985117,
-1.4724108696549));
#67367=CARTESIAN_POINT('Ctrl Pts',(-0.587252545951943,-0.18874391937359,
-1.45850123970914));
#67368=CARTESIAN_POINT('Ctrl Pts',(-0.425137619095944,-0.446931565966172,
-1.44459160976338));
#67369=CARTESIAN_POINT('Ctrl Pts',(-0.159174480134843,-0.595947400951918,
-1.43068197981763));
#67370=CARTESIAN_POINT('Ctrl Pts',(0.145670151388394,-0.599391380336776,
-1.41677234987187));
#67371=CARTESIAN_POINT('Ctrl Pts',(0.414931987837101,-0.456422244524842,
-1.40286271992611));
#67372=CARTESIAN_POINT('Ctrl Pts',(0.582838538028783,-0.201963012494897,
-1.38895308998035));
#67373=CARTESIAN_POINT('Ctrl Pts',(0.608375329813878,0.101829651386026,
-1.37504346003459));
#67374=CARTESIAN_POINT('Ctrl Pts',(0.485304500320067,0.380748423235913,
-1.36113383008883));
#67375=CARTESIAN_POINT('Ctrl Pts',(0.2436885164549,0.566661915762435,-1.34722420014307));
#67376=CARTESIAN_POINT('Ctrl Pts',(-0.0574531729881512,0.61415710753938,
-1.33331457019731));
#67377=CARTESIAN_POINT('Ctrl Pts',(-0.344560796692032,0.511632365288294,
-1.31940494025155));
#67378=CARTESIAN_POINT('Ctrl Pts',(-0.547502679490492,0.284131370633859,
-1.3054953103058));
#67379=CARTESIAN_POINT('Ctrl Pts',(-0.61670628123834,-0.0127742909283064,
-1.29158568036004));
#67380=CARTESIAN_POINT('Ctrl Pts',(-0.535267263222785,-0.306559581076066,
-1.27767605041428));
#67381=CARTESIAN_POINT('Ctrl Pts',(-0.32307870485302,-0.525461673481557,
-1.26376642046852));
#67382=CARTESIAN_POINT('Ctrl Pts',(-0.031971828364136,-0.616009433384423,
-1.24985679052276));
#67383=CARTESIAN_POINT('Ctrl Pts',(0.26694479504954,-0.556084792296555,
-1.235947160577));
#67384=CARTESIAN_POINT('Ctrl Pts',(0.500654910143371,-0.360325520573934,
-1.22203753063124));
#67385=CARTESIAN_POINT('Ctrl Pts',(0.612070231822795,-0.0765496645579366,
-1.20812790068548));
#67386=CARTESIAN_POINT('Ctrl Pts',(0.573975379848994,0.22592495027054,-1.19421827073972));
#67387=CARTESIAN_POINT('Ctrl Pts',(0.395675769904307,0.473212959393736,
-1.18030864079397));
#67388=CARTESIAN_POINT('Ctrl Pts',(0.120724583076698,0.604909410464494,
-1.1663990108482));
#67389=CARTESIAN_POINT('Ctrl Pts',(-0.183715953896658,0.588844859119433,
-1.15248938090245));
#67390=CARTESIAN_POINT('Ctrl Pts',(-0.443280261408307,0.428943387492249,
-1.13857975095669));
#67391=CARTESIAN_POINT('Ctrl Pts',(-0.59456466015388,0.16426407009338,-1.12467012101093));
#67392=CARTESIAN_POINT('Ctrl Pts',(-0.600614964892065,-0.140539972161831,
-1.11076049106517));
#67393=CARTESIAN_POINT('Ctrl Pts',(-0.459953269877679,-0.411014366362508,
-1.09685086111941));
#67394=CARTESIAN_POINT('Ctrl Pts',(-0.206938956362332,-0.581090430283628,
-1.08294123117365));
#67395=CARTESIAN_POINT('Ctrl Pts',(0.0966242610087171,-0.609223745443381,
-1.06903160122789));
#67396=CARTESIAN_POINT('Ctrl Pts',(0.376585105169253,-0.488542197145964,
-1.05512197128214));
#67397=CARTESIAN_POINT('Ctrl Pts',(0.564557642201376,-0.248524623447187,
-1.04121234133637));
#67398=CARTESIAN_POINT('Ctrl Pts',(0.614625888623889,0.0521999699313994,
-1.02730271139062));
#67399=CARTESIAN_POINT('Ctrl Pts',(0.514559692032791,0.340173695577218,
-1.01339308144486));
#67400=CARTESIAN_POINT('Ctrl Pts',(0.288802185995616,0.545053315916615,
-0.999483451499097));
#67401=CARTESIAN_POINT('Ctrl Pts',(-0.00750092532454894,0.616792960357703,
-0.985573821553339));
#67402=CARTESIAN_POINT('Ctrl Pts',(-0.301971788334754,0.53786881195832,
-0.97166419160758));
#67403=CARTESIAN_POINT('Ctrl Pts',(-0.522680112072545,0.32755964383815,
-0.957754561661821));
#67404=CARTESIAN_POINT('Ctrl Pts',(-0.615713554304776,0.0372376002572928,
-0.943844931716061));
#67405=CARTESIAN_POINT('Ctrl Pts',(-0.558346869821805,-0.262180458439861,
-0.929935301770303));
#67406=CARTESIAN_POINT('Ctrl Pts',(-0.364592997846987,-0.497555791593757,
-0.916025671824543));
#67407=CARTESIAN_POINT('Ctrl Pts',(-0.0817801264522559,-0.611393351897938,
-0.902116041878785));
#67408=CARTESIAN_POINT('Ctrl Pts',(0.221009146785851,-0.575886079762772,
-0.888206411933026));
#67409=CARTESIAN_POINT('Ctrl Pts',(0.469812595853912,-0.399707323681405,
-0.874296781987267));
#67410=CARTESIAN_POINT('Ctrl Pts',(0.603855092438784,-0.125892204537418,
-0.860387152041508));
#67411=CARTESIAN_POINT('Ctrl Pts',(0.590394124489792,0.178674557773277,
-0.846477522095749));
#67412=CARTESIAN_POINT('Ctrl Pts',(0.432717797768262,0.439596550625831,
-0.83256789214999));
#67413=CARTESIAN_POINT('Ctrl Pts',(0.16934165144514,0.593138453409806,-0.818658262204231));
#67414=CARTESIAN_POINT('Ctrl Pts',(-0.135399518690504,0.601794641190765,
-0.804748632258472));
#67415=CARTESIAN_POINT('Ctrl Pts',(-0.407066697477651,0.463450670117309,
-0.790839002312714));
#67416=CARTESIAN_POINT('Ctrl Pts',(-0.579299841632726,0.211899771854153,
-0.776929372366953));
#67417=CARTESIAN_POINT('Ctrl Pts',(-0.610027623467106,-0.0914118068666102,
-0.763019742421195));
#67418=CARTESIAN_POINT('Ctrl Pts',(-0.491744178850862,-0.372394256660645,
-0.749110112475436));
#67419=CARTESIAN_POINT('Ctrl Pts',(-0.253342561922915,-0.562412096372292,
-0.735200482529677));
#67420=CARTESIAN_POINT('Ctrl Pts',(0.0469429507698155,-0.615049737176244,
-0.721290852583919));
#67421=CARTESIAN_POINT('Ctrl Pts',(0.335761725894722,-0.517449401634344,
-0.707381222638159));
#67422=CARTESIAN_POINT('Ctrl Pts',(0.54256410594822,-0.293451888329505,
-0.6934715926924));
#67423=CARTESIAN_POINT('Ctrl Pts',(0.616834548520052,0.00222701136191001,
-0.679561962746641));
#67424=CARTESIAN_POINT('Ctrl Pts',(0.540431039526075,0.297361919795237,
-0.665652332800882));
#67425=CARTESIAN_POINT('Ctrl Pts',(0.332016636412141,0.519860339873232,
-0.651742702855123));
#67426=CARTESIAN_POINT('Ctrl Pts',(0.0425006498771184,0.615372663178635,
-0.637833072909365));
#67427=CARTESIAN_POINT('Ctrl Pts',(-0.257396954996995,0.560568129120644,
-0.623923442963605));
#67428=CARTESIAN_POINT('Ctrl Pts',(-0.494420298979825,0.36883382136708,
-0.610013813017847));
#67429=CARTESIAN_POINT('Ctrl Pts',(-0.610671775757138,0.0870046097696368,
-0.596104183072087));
#67430=CARTESIAN_POINT('Ctrl Pts',(-0.577754679237444,-0.216077186317258,
-0.582194553126328));
#67431=CARTESIAN_POINT('Ctrl Pts',(-0.403709656655228,-0.466377886429944,
-0.568284923180569));
#67432=CARTESIAN_POINT('Ctrl Pts',(-0.131050622585714,-0.602756629285352,
-0.55437529323481));
#67433=CARTESIAN_POINT('Ctrl Pts',(0.173620099557238,-0.591900228803197,
-0.540465663289051));
#67434=CARTESIAN_POINT('Ctrl Pts',(0.435880702918256,-0.436460573993837,
-0.526556033343293));
#67435=CARTESIAN_POINT('Ctrl Pts',(0.591668884983244,-0.174406852991011,
-0.512646403397534));
#67436=CARTESIAN_POINT('Ctrl Pts',(0.602930322992061,0.130249166769832,
-0.498736773451775));
#67437=CARTESIAN_POINT('Ctrl Pts',(0.466914189564528,0.403089269778846,
-0.484827143506015));
#67438=CARTESIAN_POINT('Ctrl Pts',(0.216845096307452,0.577466902977956,
-0.470917513560257));
#67439=CARTESIAN_POINT('Ctrl Pts',(-0.0861926700187708,0.610786905117146,
-0.457007883614498));
#67440=CARTESIAN_POINT('Ctrl Pts',(-0.368176184084162,0.494910211352286,
-0.443098253668738));
#67441=CARTESIAN_POINT('Ctrl Pts',(-0.560225435126384,0.258141979664292,
-0.42918862372298));
#67442=CARTESIAN_POINT('Ctrl Pts',(-0.615428622210783,-0.0416824998204124,
-0.415278993777221));
#67443=CARTESIAN_POINT('Ctrl Pts',(-0.520301282839302,-0.331325210183763,
-0.401369363831462));
#67444=CARTESIAN_POINT('Ctrl Pts',(-0.298080137716725,-0.540035231560265,
-0.387459733885703));
#67445=CARTESIAN_POINT('Ctrl Pts',(-0.00304706540753377,-0.616831042685003,
-0.373550103939944));
#67446=CARTESIAN_POINT('Ctrl Pts',(0.292730312464302,-0.542953758613251,
-0.359640473994185));
#67447=CARTESIAN_POINT('Ctrl Pts',(0.517002563024396,-0.336449356744073,
-0.345730844048426));
#67448=CARTESIAN_POINT('Ctrl Pts',(0.61498678492718,-0.0477605924661943,
-0.331821214102667));
#67449=CARTESIAN_POINT('Ctrl Pts',(0.562748407806475,0.252594634422262,
-0.317911584156908));
#67450=CARTESIAN_POINT('Ctrl Pts',(0.373047681107323,0.491248661521552,
-0.304001954211149));
#67451=CARTESIAN_POINT('Ctrl Pts',(0.0922227325703765,0.609905556155062,
-0.290092324265389));
#67452=CARTESIAN_POINT('Ctrl Pts',(-0.211129429415761,0.579581041661311,
-0.276182694319631));
#67453=CARTESIAN_POINT('Ctrl Pts',(-0.462909082222679,0.407682476246539,
-0.262273064373872));
#67454=CARTESIAN_POINT('Ctrl Pts',(-0.601614101298651,0.136199460086949,
-0.248363434428113));
#67455=CARTESIAN_POINT('Ctrl Pts',(-0.59336306197319,-0.168552948706501,
-0.234453804482354));
#67456=CARTESIAN_POINT('Ctrl Pts',(-0.440171442516207,-0.432132990033561,
-0.220544174536595));
#67457=CARTESIAN_POINT('Ctrl Pts',(-0.179459304505732,-0.590156062114196,
-0.206634544590836));
#67458=CARTESIAN_POINT('Ctrl Pts',(0.125089293053353,-0.604021927649452,
-0.192724914645077));
#67459=CARTESIAN_POINT('Ctrl Pts',(0.399082373775165,-0.470343574278392,
-0.178815284699318));
#67460=CARTESIAN_POINT('Ctrl Pts',(0.575591748830518,-0.221774569634837,
-0.164905654753559));
#67461=CARTESIAN_POINT('Ctrl Pts',(0.61150153388306,0.0809672348318517,
-0.1509960248078));
#67462=CARTESIAN_POINT('Ctrl Pts',(0.498040065154857,0.363931190296861,
-0.137086394862041));
#67463=CARTESIAN_POINT('Ctrl Pts',(0.2629225219804,0.557997829079493,-0.123176764916282));
#67464=CARTESIAN_POINT('Ctrl Pts',(-0.0364189941745252,0.615762495010526,
-0.109267134970524));
#67465=CARTESIAN_POINT('Ctrl Pts',(-0.326864487384122,0.523115168220719,
-0.0953575050247646));
#67466=CARTESIAN_POINT('Ctrl Pts',(-0.537466849093141,0.302686515590083,
-0.0814478750790057));
#67467=CARTESIAN_POINT('Ctrl Pts',(-0.616782498852957,0.00832107612999849,
-0.0675382451332462));
#67468=CARTESIAN_POINT('Ctrl Pts',(-0.545436675894266,-0.288077611085068,
-0.0536286151874875));
#67469=CARTESIAN_POINT('Ctrl Pts',(-0.340857693525337,-0.514106392358444,
-0.0397189852417285));
#67470=CARTESIAN_POINT('Ctrl Pts',(-0.0530166278705213,-0.614557116194729,
-0.0258093552959695));
#67471=CARTESIAN_POINT('Ctrl Pts',(0.247773035809132,-0.56488526363447,
-0.0118997253502107));
#67472=CARTESIAN_POINT('Ctrl Pts',(0.488042697644273,-0.3772387310703,0.00200990459554817));
#67473=CARTESIAN_POINT('Ctrl Pts',(0.609091646611938,-0.0974253718589915,
0.0159195345413072));
#67474=CARTESIAN_POINT('Ctrl Pts',(0.581371126500397,0.206148900044987,
0.0298291644870661));
#67475=CARTESIAN_POINT('Ctrl Pts',(0.411613248423951,0.459443072628057,
0.0437387944328249));
#67476=CARTESIAN_POINT('Ctrl Pts',(0.231448211077896,0.553364732778595,
0.053011881063331));
#67477=CARTESIAN_POINT('Ctrl Pts',(0.135572525753558,0.575933499534279,
0.0576484243785842));
#67478=CARTESIAN_POINT('',(0.440852672434193,-0.394665718124065,-4.71844785465692E-16));
#67479=CARTESIAN_POINT('Ctrl Pts',(0.440852672434205,-0.394665718124053,
3.19189119579733E-16));
#67480=CARTESIAN_POINT('Ctrl Pts',(0.449473509661235,-0.383319951516819,
2.21718747786181E-16));
#67481=CARTESIAN_POINT('Ctrl Pts',(0.457669236756327,-0.371675141957999,
4.69429510016819E-16));
#67482=CARTESIAN_POINT('Ctrl Pts',(0.465417977049806,-0.359748402674913,
3.60822483003176E-16));
#67483=CARTESIAN_POINT('Ctrl Pts',(0.478522792578465,-0.339577676564143,
1.76477524638973E-16));
#67484=CARTESIAN_POINT('Ctrl Pts',(0.49035035518446,-0.318600789054235,
-4.07976529536807E-18));
#67485=CARTESIAN_POINT('Ctrl Pts',(0.500848641456442,-0.296948624890611,
2.77555756156289E-17));
#67486=CARTESIAN_POINT('Ctrl Pts',(0.505567169591327,-0.287216908385617,
4.20641920774481E-17));
#67487=CARTESIAN_POINT('Ctrl Pts',(0.510016871609266,-0.277348695241159,
-2.85300624831399E-16));
#67488=CARTESIAN_POINT('Ctrl Pts',(0.514191524236475,-0.26735564627476,
-1.59594559789866E-16));
#67489=CARTESIAN_POINT('Ctrl Pts',(0.517202709096176,-0.260147641097573,
-6.89225365995604E-17));
#67490=CARTESIAN_POINT('Ctrl Pts',(0.520070283326975,-0.252875404171917,
-8.31119041629936E-16));
#67491=CARTESIAN_POINT('Ctrl Pts',(0.522787666333145,-0.245555707113886,
-8.04911692853238E-16));
#67492=CARTESIAN_POINT('Ctrl Pts',(0.532118251028885,-0.220422314731567,
-7.14924419488921E-16));
#67493=CARTESIAN_POINT('Ctrl Pts',(0.53969714499334,-0.194692026166733,
-1.18934555017748E-15));
#67494=CARTESIAN_POINT('Ctrl Pts',(0.545444196280439,-0.168547995663248,
-9.43689570931383E-16));
#67495=CARTESIAN_POINT('Ctrl Pts',(0.549056990058101,-0.152112960371672,
-7.89261787198568E-16));
#67496=CARTESIAN_POINT('Ctrl Pts',(0.551945138461182,-0.135514277280572,
-7.18348360232636E-16));
#67497=CARTESIAN_POINT('Ctrl Pts',(0.554080825173503,-0.118797873410177,
-9.29811783123569E-16));
#67498=CARTESIAN_POINT('Ctrl Pts',(0.554897574044646,-0.112405033153251,
-1.01068156188733E-15));
#67499=CARTESIAN_POINT('Ctrl Pts',(0.555603692483668,-0.105998251700886,
-1.76377181419899E-16));
#67500=CARTESIAN_POINT('Ctrl Pts',(0.556197239913037,-0.0995885671750501,
-1.87350135405495E-16));
#67501=CARTESIAN_POINT('Ctrl Pts',(0.556520563146984,-0.0960970181817748,
-1.93327435269043E-16));
#67502=CARTESIAN_POINT('Ctrl Pts',(0.556810578854251,-0.0926038658318057,
-1.40863978828908E-15));
#67503=CARTESIAN_POINT('Ctrl Pts',(0.557067136889026,-0.089109521299019,
-1.346145417358E-15));
#67504=CARTESIAN_POINT('Ctrl Pts',(0.559148466251058,-0.0607616198835184,
-8.46098165632735E-16));
#67505=CARTESIAN_POINT('Ctrl Pts',(0.559032168734981,-0.0323347809399321,
-4.55844185429651E-16));
#67506=CARTESIAN_POINT('Ctrl Pts',(0.556766473320541,-0.0040747224533165,
1.87350135405495E-16));
#67507=CARTESIAN_POINT('Ctrl Pts',(0.554526618031147,0.0238630317021695,
8.23208862244566E-16));
#67508=CARTESIAN_POINT('Ctrl Pts',(0.550185657357224,0.0516390508176347,
-7.9422394213067E-16));
#67509=CARTESIAN_POINT('Ctrl Pts',(0.543742991249869,0.0789988052988092,
-5.89805981832114E-16));
#67510=CARTESIAN_POINT('Ctrl Pts',(0.542274703309206,0.08523411175344,-5.43218991142229E-16));
#67511=CARTESIAN_POINT('Ctrl Pts',(0.540697075429711,0.0914476831063459,
1.45157397677984E-16));
#67512=CARTESIAN_POINT('Ctrl Pts',(0.539009788839933,0.0976362763365649,
2.42861286636753E-16));
#67513=CARTESIAN_POINT('Ctrl Pts',(0.537244937498979,0.104109359882143,
3.45056634178706E-16));
#67514=CARTESIAN_POINT('Ctrl Pts',(0.535362451489014,0.110546340367326,
-1.62037308714591E-15));
#67515=CARTESIAN_POINT('Ctrl Pts',(0.533364232540718,0.116939620311351,
-1.51961776495568E-15));
#67516=CARTESIAN_POINT('Ctrl Pts',(0.526576398179125,0.138657223041689,
-1.17735775453025E-15));
#67517=CARTESIAN_POINT('Ctrl Pts',(0.518450319389671,0.159887678821144,
6.33155996280266E-16));
#67518=CARTESIAN_POINT('Ctrl Pts',(0.508999488902565,0.180499514917125,
3.98986399474666E-16));
#67519=CARTESIAN_POINT('Ctrl Pts',(0.499647078040256,0.200896702239358,
1.70100247173171E-16));
#67520=CARTESIAN_POINT('Ctrl Pts',(0.488996977302556,0.220688443939696,
-4.72088927560211E-16));
#67521=CARTESIAN_POINT('Ctrl Pts',(0.477125179451088,0.239761360845527,
-4.64905891561784E-16));
#67522=CARTESIAN_POINT('Ctrl Pts',(0.47033617898477,0.250668389703985,-4.60798204137098E-16));
#67523=CARTESIAN_POINT('Ctrl Pts',(0.463147348768218,0.261340063898874,
-1.21895900032892E-16));
#67524=CARTESIAN_POINT('Ctrl Pts',(0.455570893148401,0.27175245401761,-6.93889390390723E-17));
#67525=CARTESIAN_POINT('Ctrl Pts',(0.451960029834125,0.276714895478408,
-4.43646442090714E-17));
#67526=CARTESIAN_POINT('Ctrl Pts',(0.448259716184265,0.281620175565426,
-6.41205537235798E-16));
#67527=CARTESIAN_POINT('Ctrl Pts',(0.444475691970243,0.286459782798141,
-6.27969898303604E-16));
#67528=CARTESIAN_POINT('Ctrl Pts',(0.427914097738285,0.30764136269746,-5.70041283422271E-16));
#67529=CARTESIAN_POINT('Ctrl Pts',(0.409817642639405,0.327486298662323,
7.7277447926029E-16));
#67530=CARTESIAN_POINT('Ctrl Pts',(0.390329877941827,0.345809367181636,
3.92047505570758E-16));
#67531=CARTESIAN_POINT('Ctrl Pts',(0.375751687837344,0.359516284332848,
1.07237508812116E-16));
#67532=CARTESIAN_POINT('Ctrl Pts',(0.360393975723452,0.372370990775624,
-6.33097378333802E-16));
#67533=CARTESIAN_POINT('Ctrl Pts',(0.344306626863597,0.384279754800389,
-6.34908792207511E-16));
#67534=CARTESIAN_POINT('Ctrl Pts',(0.332937466072583,0.392695849596323,
-6.35893524695548E-16));
#67535=CARTESIAN_POINT('Ctrl Pts',(0.32120367197883,0.400639160697862,6.99898877407392E-16));
#67536=CARTESIAN_POINT('Ctrl Pts',(0.309136986598197,0.408089796563423,
1.08246744900953E-15));
#67537=CARTESIAN_POINT('Ctrl Pts',(0.304304445479439,0.411073673497764,
1.23568088705765E-15));
#67538=CARTESIAN_POINT('Ctrl Pts',(0.29941766815734,0.413978964054048,1.25373440441593E-15));
#67539=CARTESIAN_POINT('Ctrl Pts',(0.294481278576378,0.416802725091794,
1.11195774810113E-15));
#67540=CARTESIAN_POINT('Ctrl Pts',(0.271684194616619,0.42984333228132,4.57209113591521E-16));
#67541=CARTESIAN_POINT('Ctrl Pts',(0.247966811548276,0.44107191162788,4.1615832323067E-17));
#67542=CARTESIAN_POINT('Ctrl Pts',(0.223548691019426,0.45040451255921,2.97505076130022E-16));
#67543=CARTESIAN_POINT('Ctrl Pts',(0.199611204723685,0.459553415179844,
5.48357522354108E-16));
#67544=CARTESIAN_POINT('Ctrl Pts',(0.174999006015723,0.466880411586669,
-3.64733594368152E-16));
#67545=CARTESIAN_POINT('Ctrl Pts',(0.149912367171149,0.472257916219641,
-1.23165366794353E-16));
#67546=CARTESIAN_POINT('Ctrl Pts',(0.137612004500597,0.474894588978313,
-4.7207705593021E-18));
#67547=CARTESIAN_POINT('Ctrl Pts',(0.125197600089965,0.477061825059574,
-3.93939898786201E-18));
#67548=CARTESIAN_POINT('Ctrl Pts',(0.112693552167563,0.478740006605732,
0.));
#67549=CARTESIAN_POINT('Ctrl Pts',(-0.591724986204225,2.85874560315911E-6,
-0.0671625192204902));
#67550=CARTESIAN_POINT('Ctrl Pts',(-0.591699563611128,-0.0958074619682504,
-0.0626512178761559));
#67551=CARTESIAN_POINT('Ctrl Pts',(-0.567976406750561,-0.19163001081242,
-0.0581399165318217));
#67552=CARTESIAN_POINT('Ctrl Pts',(-0.523231149325893,-0.27634929342812,
-0.0536286151874874));
#67553=CARTESIAN_POINT('Ctrl Pts',(-0.47724368177129,-0.363420538176193,
-0.0489920718722345));
#67554=CARTESIAN_POINT('Ctrl Pts',(-0.409050687648318,-0.438763465267315,
-0.0443555285569818));
#67555=CARTESIAN_POINT('Ctrl Pts',(-0.326980679644361,-0.493176716118926,
-0.0397189852417288));
#67556=CARTESIAN_POINT('Ctrl Pts',(-0.244910671640404,-0.547589966970536,
-0.0350824419264758));
#67557=CARTESIAN_POINT('Ctrl Pts',(-0.148963649755454,-0.581073541582635,
-0.0304458986112222));
#67558=CARTESIAN_POINT('Ctrl Pts',(-0.0508585281997095,-0.589536686795305,
-0.0258093552959693));
#67559=CARTESIAN_POINT('Ctrl Pts',(0.0472465933560355,-0.597999832007976,
-0.0211728119807163));
#67560=CARTESIAN_POINT('Ctrl Pts',(0.147509814582582,-0.581442547821224,
-0.0165362686654636));
#67561=CARTESIAN_POINT('Ctrl Pts',(0.237686368835047,-0.541889483633819,
-0.0118997253502107));
#67562=CARTESIAN_POINT('Ctrl Pts',(0.314832650426807,-0.508051732203712,
-0.00793315023347389));
#67563=CARTESIAN_POINT('Ctrl Pts',(0.384596653849161,-0.457383719090204,
-0.00396657511673726));
#67564=CARTESIAN_POINT('Ctrl Pts',(0.440852672434193,-0.394665718124065,
-4.71844785465692E-16));
#67565=CARTESIAN_POINT('',(-0.285727948592038,-0.40034239738492,-3.948325));
#67566=CARTESIAN_POINT('Ctrl Pts',(-0.285727948592038,-0.40034239738492,
-3.948325));
#67567=CARTESIAN_POINT('Ctrl Pts',(-0.296082595521109,-0.394398284770688,
-3.948325));
#67568=CARTESIAN_POINT('Ctrl Pts',(-0.306205674003326,-0.388080952767024,
-3.948325));
#67569=CARTESIAN_POINT('Ctrl Pts',(-0.316075703283998,-0.381402204064925,
-3.948325));
#67570=CARTESIAN_POINT('Ctrl Pts',(-0.333628984468336,-0.369524432419702,
-3.948325));
#67571=CARTESIAN_POINT('Ctrl Pts',(-0.350382541823529,-0.356504844564474,
-3.948325));
#67572=CARTESIAN_POINT('Ctrl Pts',(-0.366265661797884,-0.342458377831604,
-3.948325));
#67573=CARTESIAN_POINT('Ctrl Pts',(-0.373067338029369,-0.336443217141036,
-3.948325));
#67574=CARTESIAN_POINT('Ctrl Pts',(-0.379709280111531,-0.330239464740281,
-3.948325));
#67575=CARTESIAN_POINT('Ctrl Pts',(-0.386185328609897,-0.32385498795212,
-3.948325));
#67576=CARTESIAN_POINT('Ctrl Pts',(-0.390906098569952,-0.319200969959539,
-3.948325));
#67577=CARTESIAN_POINT('Ctrl Pts',(-0.395536981686774,-0.314452441162492,
-3.948325));
#67578=CARTESIAN_POINT('Ctrl Pts',(-0.400069693202905,-0.309619281567598,
-3.948325));
#67579=CARTESIAN_POINT('Ctrl Pts',(-0.416474734625152,-0.292126841761447,
-3.948325));
#67580=CARTESIAN_POINT('Ctrl Pts',(-0.431618982752109,-0.273504975619171,
-3.948325));
#67581=CARTESIAN_POINT('Ctrl Pts',(-0.445400119986255,-0.253908755436526,
-3.948325));
#67582=CARTESIAN_POINT('Ctrl Pts',(-0.451206944048774,-0.24565168630227,
-3.948325));
#67583=CARTESIAN_POINT('Ctrl Pts',(-0.456771538061931,-0.237221261837567,
-3.948325));
#67584=CARTESIAN_POINT('Ctrl Pts',(-0.462085123502627,-0.228627650838076,
-3.948325));
#67585=CARTESIAN_POINT('Ctrl Pts',(-0.46560519169573,-0.222934678158739,
-3.948325));
#67586=CARTESIAN_POINT('Ctrl Pts',(-0.469016405936867,-0.217167713895661,
-3.948325));
#67587=CARTESIAN_POINT('Ctrl Pts',(-0.472311582807742,-0.211337460706846,
-3.948325));
#67588=CARTESIAN_POINT('Ctrl Pts',(-0.475847180328577,-0.205081824202959,
-3.948325));
#67589=CARTESIAN_POINT('Ctrl Pts',(-0.479246974049362,-0.19875752364046,
-3.948325));
#67590=CARTESIAN_POINT('Ctrl Pts',(-0.482508590030484,-0.192368808372637,
-3.948325));
#67591=CARTESIAN_POINT('Ctrl Pts',(-0.494734148213928,-0.168421902704926,
-3.948325));
#67592=CARTESIAN_POINT('Ctrl Pts',(-0.505021436671191,-0.14357295390494,
-3.948325));
#67593=CARTESIAN_POINT('Ctrl Pts',(-0.513371142735674,-0.118078037500813,
-3.948325));
#67594=CARTESIAN_POINT('Ctrl Pts',(-0.518853109089587,-0.101339451394439,
-3.948325));
#67595=CARTESIAN_POINT('Ctrl Pts',(-0.523499115474155,-0.0843215126712255,
-3.948325));
#67596=CARTESIAN_POINT('Ctrl Pts',(-0.527299444230766,-0.0670897043369155,
-3.948325));
#67597=CARTESIAN_POINT('Ctrl Pts',(-0.530337067689686,-0.053316226149045,
-3.948325));
#67598=CARTESIAN_POINT('Ctrl Pts',(-0.532834254606844,-0.0394059791423619,
-3.948325));
#67599=CARTESIAN_POINT('Ctrl Pts',(-0.534782029141017,-0.0253909900826123,
-3.948325));
#67600=CARTESIAN_POINT('Ctrl Pts',(-0.535644228960787,-0.0191871298157362,
-3.948325));
#67601=CARTESIAN_POINT('Ctrl Pts',(-0.536398045645329,-0.0129667940238257,
-3.948325));
#67602=CARTESIAN_POINT('Ctrl Pts',(-0.537042228310059,-0.00674248143224362,
-3.948325));
#67603=CARTESIAN_POINT('Ctrl Pts',(-0.539515522073872,0.0171553263785874,
-3.948325));
#67604=CARTESIAN_POINT('Ctrl Pts',(-0.54038057067284,0.0411519544184588,
-3.948325));
#67605=CARTESIAN_POINT('Ctrl Pts',(-0.539627056960311,0.0650829329353078,
-3.948325));
#67606=CARTESIAN_POINT('Ctrl Pts',(-0.538898018290729,0.0882366041288409,
-3.948325));
#67607=CARTESIAN_POINT('Ctrl Pts',(-0.536653985044464,0.111329445677917,
-3.948325));
#67608=CARTESIAN_POINT('Ctrl Pts',(-0.532953652586977,0.134229883485741,
-3.948325));
#67609=CARTESIAN_POINT('Ctrl Pts',(-0.530626779492689,0.148630322688061,
-3.948325));
#67610=CARTESIAN_POINT('Ctrl Pts',(-0.527723528323636,0.162954790975836,
-3.948325));
#67611=CARTESIAN_POINT('Ctrl Pts',(-0.524253375751702,0.177170538350544,
-3.948325));
#67612=CARTESIAN_POINT('Ctrl Pts',(-0.522340300985194,0.185007596527629,
-3.948325));
#67613=CARTESIAN_POINT('Ctrl Pts',(-0.520253718058824,0.192814707355631,
-3.948325));
#67614=CARTESIAN_POINT('Ctrl Pts',(-0.518002646091187,0.200561489135888,
-3.948325));
#67615=CARTESIAN_POINT('Ctrl Pts',(-0.510004128433378,0.228087384243376,
-3.948325));
#67616=CARTESIAN_POINT('Ctrl Pts',(-0.499919583291045,0.254914254992326,
-3.948325));
#67617=CARTESIAN_POINT('Ctrl Pts',(-0.487866003040689,0.280804612238299,
-3.948325));
#67618=CARTESIAN_POINT('Ctrl Pts',(-0.480108922853125,0.297466348674306,
-3.948325));
#67619=CARTESIAN_POINT('Ctrl Pts',(-0.471535246924139,0.313740425559195,
-3.948325));
#67620=CARTESIAN_POINT('Ctrl Pts',(-0.462164839595945,0.329562331281333,
-3.948325));
#67621=CARTESIAN_POINT('Ctrl Pts',(-0.454710650331234,0.34214870833523,
-3.948325));
#67622=CARTESIAN_POINT('Ctrl Pts',(-0.446752088203126,0.354448939593675,
-3.948325));
#67623=CARTESIAN_POINT('Ctrl Pts',(-0.438312880065648,0.366442036514319,
-3.948325));
#67624=CARTESIAN_POINT('Ctrl Pts',(-0.434649842629724,0.371647639016038,
-3.948325));
#67625=CARTESIAN_POINT('Ctrl Pts',(-0.430896211124093,0.376795355434164,
-3.948325));
#67626=CARTESIAN_POINT('Ctrl Pts',(-0.427053747527973,0.381883355554364,
-3.948325));
#67627=CARTESIAN_POINT('Ctrl Pts',(-0.423072494282475,0.387155134059201,
-3.948325));
#67628=CARTESIAN_POINT('Ctrl Pts',(-0.419000871875213,0.392356106729907,
-3.948325));
#67629=CARTESIAN_POINT('Ctrl Pts',(-0.414844342099757,0.397481307504267,
-3.948325));
#67630=CARTESIAN_POINT('Ctrl Pts',(-0.396507671020364,0.42009130331621,
-3.948325));
#67631=CARTESIAN_POINT('Ctrl Pts',(-0.37650644191244,0.441249440744765,
-3.948325));
#67632=CARTESIAN_POINT('Ctrl Pts',(-0.355056904178872,0.460812670257216,
-3.948325));
#67633=CARTESIAN_POINT('Ctrl Pts',(-0.333444871567189,0.480524104576441,
-3.948325));
#67634=CARTESIAN_POINT('Ctrl Pts',(-0.310361705037122,0.49861742897275,
-3.948325));
#67635=CARTESIAN_POINT('Ctrl Pts',(-0.285984798569953,0.5149186212662,-3.948325));
#67636=CARTESIAN_POINT('Ctrl Pts',(-0.276962187040763,0.5209521729691,-3.948325));
#67637=CARTESIAN_POINT('Ctrl Pts',(-0.267761970436877,0.526739857966417,
-3.948325));
#67638=CARTESIAN_POINT('Ctrl Pts',(-0.258391981634414,0.532271443393351,
-3.948325));
#67639=CARTESIAN_POINT('Ctrl Pts',(-0.285727948592038,-0.40034239738492,
-3.948325));
#67640=CARTESIAN_POINT('Ctrl Pts',(-0.228684894383911,-0.440971740204431,
-3.94435842488326));
#67641=CARTESIAN_POINT('Ctrl Pts',(-0.08595864849882,-0.50256281066439,
-3.93575530645127));
#67642=CARTESIAN_POINT('Ctrl Pts',(0.154857629827177,-0.488798982873136,
-3.92251564470403));
#67643=CARTESIAN_POINT('Ctrl Pts',(0.37003347141403,-0.354935592235777,
-3.90860601475827));
#67644=CARTESIAN_POINT('Ctrl Pts',(0.494821102216335,-0.134374424279909,
-3.89469638481251));
#67645=CARTESIAN_POINT('Ctrl Pts',(0.498739099375933,0.119011467407269,
-3.88078675486675));
#67646=CARTESIAN_POINT('Ctrl Pts',(0.380830207075808,0.343325891736714,
-3.86687712492099));
#67647=CARTESIAN_POINT('Ctrl Pts',(0.169896094203756,0.483776521506451,
-3.85296749497524));
#67648=CARTESIAN_POINT('Ctrl Pts',(-0.0825384944710284,0.506055083932911,
-3.83905786502947));
#67649=CARTESIAN_POINT('Ctrl Pts',(-0.314811425572855,0.404719832155649,
-3.82514823508372));
#67650=CARTESIAN_POINT('Ctrl Pts',(-0.46094408502887,0.21643111900778,-3.81206592794025));
#67651=CARTESIAN_POINT('Ctrl Pts',(-0.491770333220413,0.0672463213179462,
-3.80362016411204));
#67652=CARTESIAN_POINT('Ctrl Pts',(-0.491838560105423,-1.18860308867142E-5,
-3.79981094359907));
#67653=CARTESIAN_POINT('Origin',(-7.01450167938425E-17,0.,-3.948325));
#67654=CARTESIAN_POINT('',(-0.591675,-7.2459289488551E-17,-3.948325));
#67655=CARTESIAN_POINT('Origin',(0.,0.,-3.948325));
#67656=CARTESIAN_POINT('Origin',(0.,0.,-3.948325));
#67657=CARTESIAN_POINT('',(0.285706463458477,-0.400329423553965,-3.948325));
#67658=CARTESIAN_POINT('Ctrl Pts',(0.258414858989731,0.532291148796132,
-3.948325));
#67659=CARTESIAN_POINT('Ctrl Pts',(0.270692196855467,0.525058429447917,
-3.948325));
#67660=CARTESIAN_POINT('Ctrl Pts',(0.282689452115837,0.517387875687169,
-3.948325));
#67661=CARTESIAN_POINT('Ctrl Pts',(0.294379894662667,0.509287034300484,
-3.948325));
#67662=CARTESIAN_POINT('Ctrl Pts',(0.314150991282511,0.495586738771328,
-3.948325));
#67663=CARTESIAN_POINT('Ctrl Pts',(0.333045588916465,0.480656394447447,
-3.948325));
#67664=CARTESIAN_POINT('Ctrl Pts',(0.350965945749258,0.464597409889149,
-3.948325));
#67665=CARTESIAN_POINT('Ctrl Pts',(0.359020375799688,0.457379586660928,
-3.948325));
#67666=CARTESIAN_POINT('Ctrl Pts',(0.366877754573242,0.44993357574956,-3.948325));
#67667=CARTESIAN_POINT('Ctrl Pts',(0.374527904104896,0.44226780995476,-3.948325));
#67668=CARTESIAN_POINT('Ctrl Pts',(0.380045971174055,0.436738478845983,
-3.948325));
#67669=CARTESIAN_POINT('Ctrl Pts',(0.385455478952879,0.431095285495367,
-3.948325));
#67670=CARTESIAN_POINT('Ctrl Pts',(0.39074398206846,0.425351256933648,-3.948325));
#67671=CARTESIAN_POINT('Ctrl Pts',(0.408902933400678,0.405628183537733,
-3.948325));
#67672=CARTESIAN_POINT('Ctrl Pts',(0.425667032165364,0.384688931004672,
-3.948325));
#67673=CARTESIAN_POINT('Ctrl Pts',(0.440892698522948,0.362672619611768,
-3.948325));
#67674=CARTESIAN_POINT('Ctrl Pts',(0.450464075156269,0.34883241035794,-3.948325));
#67675=CARTESIAN_POINT('Ctrl Pts',(0.459426866363713,0.334566154978976,
-3.948325));
#67676=CARTESIAN_POINT('Ctrl Pts',(0.467737926515355,0.319905814085685,
-3.948325));
#67677=CARTESIAN_POINT('Ctrl Pts',(0.470916318295014,0.314299272184647,
-3.948325));
#67678=CARTESIAN_POINT('Ctrl Pts',(0.473997613735816,0.308637905559322,
-3.948325));
#67679=CARTESIAN_POINT('Ctrl Pts',(0.476975834115326,0.302931193698179,
-3.948325));
#67680=CARTESIAN_POINT('Ctrl Pts',(0.478598160818049,0.29982257517526,-3.948325));
#67681=CARTESIAN_POINT('Ctrl Pts',(0.480190271744143,0.296699851021107,
-3.948325));
#67682=CARTESIAN_POINT('Ctrl Pts',(0.481751872132746,0.293563344844831,
-3.948325));
#67683=CARTESIAN_POINT('Ctrl Pts',(0.494420368969739,0.268118411004285,
-3.948325));
#67684=CARTESIAN_POINT('Ctrl Pts',(0.505085056951574,0.241767638286393,
-3.948325));
#67685=CARTESIAN_POINT('Ctrl Pts',(0.513697452978676,0.214756695707742,
-3.948325));
#67686=CARTESIAN_POINT('Ctrl Pts',(0.52221162370046,0.188053815841646,-3.948325));
#67687=CARTESIAN_POINT('Ctrl Pts',(0.528720105838612,0.160704397593371,
-3.948325));
#67688=CARTESIAN_POINT('Ctrl Pts',(0.533125889963004,0.132943760576394,
-3.948325));
#67689=CARTESIAN_POINT('Ctrl Pts',(0.534129969718082,0.126617101614028,
-3.948325));
#67690=CARTESIAN_POINT('Ctrl Pts',(0.535024628194969,0.120269122589768,
-3.948325));
#67691=CARTESIAN_POINT('Ctrl Pts',(0.535808341459282,0.113902703852351,
-3.948325));
#67692=CARTESIAN_POINT('Ctrl Pts',(0.536628084967519,0.107243596920824,
-3.948325));
#67693=CARTESIAN_POINT('Ctrl Pts',(0.537325285579543,0.100573322813461,
-3.948325));
#67694=CARTESIAN_POINT('Ctrl Pts',(0.537898824104105,0.0938996332282421,
-3.948325));
#67695=CARTESIAN_POINT('Ctrl Pts',(0.539847098021773,0.0712295338423138,
-3.948325));
#67696=CARTESIAN_POINT('Ctrl Pts',(0.540372332158008,0.048503123801434,
-3.948325));
#67697=CARTESIAN_POINT('Ctrl Pts',(0.539437191193445,0.0258471839316688,
-3.948325));
#67698=CARTESIAN_POINT('Ctrl Pts',(0.538511788225682,0.00342716942321664,
-3.948325));
#67699=CARTESIAN_POINT('Ctrl Pts',(0.536156044637272,-0.0189243113481171,
-3.948325));
#67700=CARTESIAN_POINT('Ctrl Pts',(0.532397321112644,-0.0410735384121692,
-3.948325));
#67701=CARTESIAN_POINT('Ctrl Pts',(0.530247857204089,-0.0537397970142222,
-3.948325));
#67702=CARTESIAN_POINT('Ctrl Pts',(0.527639194833725,-0.066339768733417,
-3.948325));
#67703=CARTESIAN_POINT('Ctrl Pts',(0.524573560199496,-0.0788466840532584,
-3.948325));
#67704=CARTESIAN_POINT('Ctrl Pts',(0.523112516145411,-0.0848073272619983,
-3.948325));
#67705=CARTESIAN_POINT('Ctrl Pts',(0.52154703257174,-0.0907489695288106,
-3.948325));
#67706=CARTESIAN_POINT('Ctrl Pts',(0.519879195788693,-0.0966615590501735,
-3.948325));
#67707=CARTESIAN_POINT('Ctrl Pts',(0.512579525727885,-0.122539362651615,
-3.948325));
#67708=CARTESIAN_POINT('Ctrl Pts',(0.503352948066008,-0.147761845315584,
-3.948325));
#67709=CARTESIAN_POINT('Ctrl Pts',(0.492262118340815,-0.172103200481393,
-3.948325));
#67710=CARTESIAN_POINT('Ctrl Pts',(0.483965425647558,-0.190312184709993,
-3.948325));
#67711=CARTESIAN_POINT('Ctrl Pts',(0.474624408392381,-0.20802791865184,
-3.948325));
#67712=CARTESIAN_POINT('Ctrl Pts',(0.464249712096462,-0.225144758296707,
-3.948325));
#67713=CARTESIAN_POINT('Ctrl Pts',(0.456917754127682,-0.237241493011135,
-3.948325));
#67714=CARTESIAN_POINT('Ctrl Pts',(0.449069197429663,-0.249038883086192,
-3.948325));
#67715=CARTESIAN_POINT('Ctrl Pts',(0.440725878633132,-0.260506491692914,
-3.948325));
#67716=CARTESIAN_POINT('Ctrl Pts',(0.437384497280559,-0.26509910699284,
-3.948325));
#67717=CARTESIAN_POINT('Ctrl Pts',(0.433963144714414,-0.269639549928986,
-3.948325));
#67718=CARTESIAN_POINT('Ctrl Pts',(0.430464984712528,-0.274123344607859,
-3.948325));
#67719=CARTESIAN_POINT('Ctrl Pts',(0.414309880260752,-0.294830279493182,
-3.948325));
#67720=CARTESIAN_POINT('Ctrl Pts',(0.396616450072697,-0.314209078958056,
-3.948325));
#67721=CARTESIAN_POINT('Ctrl Pts',(0.377556066500118,-0.332098849600154,
-3.948325));
#67722=CARTESIAN_POINT('Ctrl Pts',(0.358870868001475,-0.349636477542946,
-3.948325));
#67723=CARTESIAN_POINT('Ctrl Pts',(0.338870871116485,-0.365743763761861,
-3.948325));
#67724=CARTESIAN_POINT('Ctrl Pts',(0.317693061872851,-0.380226744315664,
-3.948325));
#67725=CARTESIAN_POINT('Ctrl Pts',(0.307309243671757,-0.387327981055998,
-3.948325));
#67726=CARTESIAN_POINT('Ctrl Pts',(0.296641996093472,-0.39403800768009,
-3.948325));
#67727=CARTESIAN_POINT('Ctrl Pts',(0.28570646345848,-0.400329423553963,
-3.948325));
#67728=CARTESIAN_POINT('Origin',(0.,0.,-3.948325));
#67729=CARTESIAN_POINT('Origin',(0.,0.,-4.27183905640093));
#67730=CARTESIAN_POINT('Ctrl Pts',(0.285706463458477,-0.400329423553965,
-3.948325));
#67731=CARTESIAN_POINT('Ctrl Pts',(0.35234932738247,-0.352767850893538,
-3.94368845668475));
#67732=CARTESIAN_POINT('Ctrl Pts',(0.461355386710151,-0.223767338793563,
-3.93441537005424));
#67733=CARTESIAN_POINT('Ctrl Pts',(0.512153850375005,0.024551470863185,
-3.92050574010848));
#67734=CARTESIAN_POINT('Ctrl Pts',(0.437852459283724,0.266806684479465,
-3.90659611016272));
#67735=CARTESIAN_POINT('Ctrl Pts',(0.256595437328703,0.443921775016828,
-3.89268648021697));
#67736=CARTESIAN_POINT('Ctrl Pts',(0.0126607096365889,0.51258367325088,
-3.8787768502712));
#67737=CARTESIAN_POINT('Ctrl Pts',(-0.234367035151384,0.456045416423434,
-3.86486722032544));
#67738=CARTESIAN_POINT('Ctrl Pts',(-0.424145829883178,0.288104776438461,
-3.85095759037969));
#67739=CARTESIAN_POINT('Ctrl Pts',(-0.487188530294114,0.113758445818203,
-3.84078153573818));
#67740=CARTESIAN_POINT('Ctrl Pts',(-0.491850800983448,0.0159562304202861,
-3.83524202441192));
#67741=CARTESIAN_POINT('Ctrl Pts',(-0.491834365111822,1.24153615857388E-5,
-3.83433905640092));
#67742=CARTESIAN_POINT('Ctrl Pts',(0.343710408716095,-0.481604049573106,
-4.00597342437858));
#67743=CARTESIAN_POINT('Ctrl Pts',(0.423883064665323,-0.424386556554537,
-4.00133688106333));
#67744=CARTESIAN_POINT('Ctrl Pts',(0.555019465118139,-0.269196442191191,
-3.99206379443282));
#67745=CARTESIAN_POINT('Ctrl Pts',(0.616131000702752,0.0295358949280207,
-3.97815416448707));
#67746=CARTESIAN_POINT('Ctrl Pts',(0.526744988251306,0.320973608579041,
-3.9642445345413));
#67747=CARTESIAN_POINT('Ctrl Pts',(0.308689280499083,0.534046492620507,
-3.95033490459555));
#67748=CARTESIAN_POINT('Ctrl Pts',(0.015231078888283,0.616648085946656,
-3.93642527464979));
#67749=CARTESIAN_POINT('Ctrl Pts',(-0.281948082190197,0.548631468026912,
-3.92251564470403));
#67750=CARTESIAN_POINT('Ctrl Pts',(-0.510255647631026,0.346595625678295,
-3.90860601475827));
#67751=CARTESIAN_POINT('Ctrl Pts',(-0.613923373668732,0.0598996637254193,
-3.89469638481251));
#67752=CARTESIAN_POINT('Ctrl Pts',(-0.567628196994441,-0.241429332723434,
-3.88078675486675));
#67753=CARTESIAN_POINT('Ctrl Pts',(-0.382678718524923,-0.483783774923831,
-3.86687712492099));
#67754=CARTESIAN_POINT('Ctrl Pts',(-0.104252431765138,-0.607964887305674,
-3.85296749497524));
#67755=CARTESIAN_POINT('Ctrl Pts',(0.199639550299989,-0.583638454109383,
-3.83905786502947));
#67756=CARTESIAN_POINT('Ctrl Pts',(0.454765656086047,-0.416746960908529,
-3.82514823508372));
#67757=CARTESIAN_POINT('Ctrl Pts',(0.59880631770923,-0.148056790733748,
-3.81123860513795));
#67758=CARTESIAN_POINT('Ctrl Pts',(0.596576778298504,0.156799133531066,
-3.7973289751922));
#67759=CARTESIAN_POINT('Ctrl Pts',(0.448621644933921,0.423353802830726,
-3.78341934524643));
#67760=CARTESIAN_POINT('Ctrl Pts',(0.191081865280786,0.586495985759321,
-3.76950971530068));
#67761=CARTESIAN_POINT('Ctrl Pts',(-0.113133412488725,0.606375010134377,
-3.75560008535492));
#67762=CARTESIAN_POINT('Ctrl Pts',(-0.389713632522964,0.47813502891289,
-3.74169045540916));
#67763=CARTESIAN_POINT('Ctrl Pts',(-0.571098644850701,0.233101178361757,
-3.72778082546341));
#67764=CARTESIAN_POINT('Ctrl Pts',(-0.61298159820254,-0.0688722129692012,
-3.71387119551764));
#67765=CARTESIAN_POINT('Ctrl Pts',(-0.505131758776296,-0.354022213579012,
-3.69996156557189));
#67766=CARTESIAN_POINT('Ctrl Pts',(-0.27389356773763,-0.55269533652539,
-3.68605193562612));
#67767=CARTESIAN_POINT('Ctrl Pts',(0.0242485058037712,-0.616361769910605,
-3.67214230568037));
#67768=CARTESIAN_POINT('Ctrl Pts',(0.316467405623905,-0.52946973721973,
-3.6582326757346));
#67769=CARTESIAN_POINT('Ctrl Pts',(0.531382926990323,-0.313244323734379,
-3.64432304578885));
#67770=CARTESIAN_POINT('Ctrl Pts',(0.616497733406334,-0.0205028328487188,
-3.63041341584309));
#67771=CARTESIAN_POINT('Ctrl Pts',(0.551020861962079,0.27724687758871,-3.61650378589733));
#67772=CARTESIAN_POINT('Ctrl Pts',(0.350946324310309,0.507273593736863,
-3.60259415595157));
#67773=CARTESIAN_POINT('Ctrl Pts',(0.0651462552364883,0.613388773029548,
-3.58868452600582));
#67774=CARTESIAN_POINT('Ctrl Pts',(-0.236567065988548,0.569671699085858,
-3.57477489606005));
#67775=CARTESIAN_POINT('Ctrl Pts',(-0.480494235759622,0.386801125711496,
-3.5608652661143));
#67776=CARTESIAN_POINT('Ctrl Pts',(-0.6070512527398,0.109446781574009,-3.54695563616854));
#67777=CARTESIAN_POINT('Ctrl Pts',(-0.585324080267991,-0.194642088224266,
-3.53304600622278));
#67778=CARTESIAN_POINT('Ctrl Pts',(-0.420620006887823,-0.451185805689371,
-3.51913637627702));
#67779=CARTESIAN_POINT('Ctrl Pts',(-0.153171236899005,-0.597518529952587,
-3.50522674633126));
#67780=CARTESIAN_POINT('Ctrl Pts',(0.151692615602894,-0.597895619503463,
-3.4913171163855));
#67781=CARTESIAN_POINT('Ctrl Pts',(0.419502567879716,-0.452224962814082,
-3.47740748643974));
#67782=CARTESIAN_POINT('Ctrl Pts',(0.584840779969329,-0.196089478388676,
-3.46349785649398));
#67783=CARTESIAN_POINT('Ctrl Pts',(0.607320146739344,0.107944711840726,
-3.44958822654823));
#67784=CARTESIAN_POINT('Ctrl Pts',(0.481449641417571,0.385611286438515,
-3.43567859660246));
#67785=CARTESIAN_POINT('Ctrl Pts',(0.237975606711176,0.569084731881223,
-3.42176896665671));
#67786=CARTESIAN_POINT('Ctrl Pts',(-0.0636286431809187,0.613548056159279,
-3.40785933671094));
#67787=CARTESIAN_POINT('Ctrl Pts',(-0.349690347468453,0.508140219169145,
-3.39394970676519));
#67788=CARTESIAN_POINT('Ctrl Pts',(-0.55033331734186,0.27860915504229,-3.38004007681943));
#67789=CARTESIAN_POINT('Ctrl Pts',(-0.616546567282803,-0.0189776663915349,
-3.36613044687367));
#67790=CARTESIAN_POINT('Ctrl Pts',(-0.532156210730363,-0.311928820135262,
-3.35222081692791));
#67791=CARTESIAN_POINT('Ctrl Pts',(-0.317776249488288,-0.528685234058066,
-3.33831118698215));
#67792=CARTESIAN_POINT('Ctrl Pts',(-0.0257731989769087,-0.616299897504756,
-3.32440155703639));
#67793=CARTESIAN_POINT('Ctrl Pts',(0.272525461505833,-0.55337120839533,
-3.31049192709064));
#67794=CARTESIAN_POINT('Ctrl Pts',(0.504254426296432,-0.355270734807036,
-3.29658229714487));
#67795=CARTESIAN_POINT('Ctrl Pts',(0.612809345166734,-0.0703884076122953,
-3.28267266719912));
#67796=CARTESIAN_POINT('Ctrl Pts',(0.57167354743521,0.231687670394254,-3.26876303725335));
#67797=CARTESIAN_POINT('Ctrl Pts',(0.390895259502109,0.477169485139876,
-3.25485340730761));
#67798=CARTESIAN_POINT('Ctrl Pts',(0.114633128229106,0.606093282723282,
-3.24094377736183));
#67799=CARTESIAN_POINT('Ctrl Pts',(-0.189630395722162,0.586966893843369,
-3.22703414741608));
#67800=CARTESIAN_POINT('Ctrl Pts',(-0.447572971650981,0.424462314578555,
-3.21312451747032));
#67801=CARTESIAN_POINT('Ctrl Pts',(-0.596187060038844,0.158274479598307,
-3.19921488752456));
#67802=CARTESIAN_POINT('Ctrl Pts',(-0.599170751387531,-0.146575005139266,
-3.1853052575788));
#67803=CARTESIAN_POINT('Ctrl Pts',(-0.455795220492882,-0.415620666504591,
-3.17139562763305));
#67804=CARTESIAN_POINT('Ctrl Pts',(-0.201082756313209,-0.58314281832443,
-3.15748599768728));
#67805=CARTESIAN_POINT('Ctrl Pts',(0.102748119859029,-0.608220885300159,
-3.14357636774153));
#67806=CARTESIAN_POINT('Ctrl Pts',(0.38148075003927,-0.484729057102369,
-3.12966673779576));
#67807=CARTESIAN_POINT('Ctrl Pts',(0.567029215693361,-0.242832637839412,
-3.11575710785001));
#67808=CARTESIAN_POINT('Ctrl Pts',(0.614069660376893,0.0583804218422761,
-3.10184747790425));
#67809=CARTESIAN_POINT('Ctrl Pts',(0.511111531719077,0.345332917043329,
-3.0879378479585));
#67810=CARTESIAN_POINT('Ctrl Pts',(0.283304374485059,0.547931065780637,
-3.07402821801273));
#67811=CARTESIAN_POINT('Ctrl Pts',(-0.0137054396072017,0.616686291703527,
-3.06011858806698));
#67812=CARTESIAN_POINT('Ctrl Pts',(-0.307367430934806,0.534803780699439,
-3.04620895812121));
#67813=CARTESIAN_POINT('Ctrl Pts',(-0.525948891327989,0.322284944049105,
-3.03229932817546));
#67814=CARTESIAN_POINT('Ctrl Pts',(-0.616057006691815,0.0310416809434863,
-3.01838969822969));
#67815=CARTESIAN_POINT('Ctrl Pts',(-0.555681100350354,-0.267784122313653,
-3.00448006828394));
#67816=CARTESIAN_POINT('Ctrl Pts',(-0.359569173059506,-0.5011983950844,
-2.99057043833818));
#67817=CARTESIAN_POINT('Ctrl Pts',(-0.0756254142084532,-0.612185117571209,
-2.97666080839242));
#67818=CARTESIAN_POINT('Ctrl Pts',(0.226791337157252,-0.573633603304672,
-2.96275117844666));
#67819=CARTESIAN_POINT('Ctrl Pts',(0.47380985080692,-0.394960816699834,
-2.9488415485009));
#67820=CARTESIAN_POINT('Ctrl Pts',(0.605091003955021,-0.119811094572164,
-2.93493191855514));
#67821=CARTESIAN_POINT('Ctrl Pts',(0.588566796911201,0.184604840195385,
-2.92102228860939));
#67822=CARTESIAN_POINT('Ctrl Pts',(0.428273591740068,0.443927417567261,
-2.90711265866362));
#67823=CARTESIAN_POINT('Ctrl Pts',(0.163366151562832,0.594812005572706,
-2.89320302871787));
#67824=CARTESIAN_POINT('Ctrl Pts',(-0.141446679236782,0.600402080594964,
-2.87929339877211));
#67825=CARTESIAN_POINT('Ctrl Pts',(-0.411708380973339,0.459332157034739,
-2.86538376882635));
#67826=CARTESIAN_POINT('Ctrl Pts',(-0.581402225732933,0.206061333982548,
-2.85147413888059));
#67827=CARTESIAN_POINT('Ctrl Pts',(-0.609077159569785,-0.0975440164247773,
-2.83756450893483));
#67828=CARTESIAN_POINT('Ctrl Pts',(-0.487973036427672,-0.377322325299515,
-2.82365487898907));
#67829=CARTESIAN_POINT('Ctrl Pts',(-0.247671916566535,-0.564932246551864,
-2.80974524904331));
#67830=CARTESIAN_POINT('Ctrl Pts',(0.0531279325737788,-0.614546372725696,
-2.79583561909755));
#67831=CARTESIAN_POINT('Ctrl Pts',(0.340950240883056,-0.514045479205549,
-2.7819259891518));
#67832=CARTESIAN_POINT('Ctrl Pts',(0.545488757445549,-0.287978882820228,
-2.76801635920603));
#67833=CARTESIAN_POINT('Ctrl Pts',(0.616780932965306,0.00843221087987096,
-2.75410672926028));
#67834=CARTESIAN_POINT('Ctrl Pts',(0.537412253571372,0.302783571485002,
-2.74019709931452));
#67835=CARTESIAN_POINT('Ctrl Pts',(0.326770077808336,0.523174098841876,
-2.72628746936876));
#67836=CARTESIAN_POINT('Ctrl Pts',(0.0363078935924984,0.615769078724119,
-2.712377839423));
#67837=CARTESIAN_POINT('Ctrl Pts',(-0.263023206629647,0.557950368961374,
-2.69846820947724));
#67838=CARTESIAN_POINT('Ctrl Pts',(-0.498105723513708,0.363841324828228,
-2.68455857953148));
#67839=CARTESIAN_POINT('Ctrl Pts',(-0.611516135877317,0.0808568921709814,
-2.67064894958572));
#67840=CARTESIAN_POINT('Ctrl Pts',(-0.575551723403444,-0.221878424226423,
-2.65673931963997));
#67841=CARTESIAN_POINT('Ctrl Pts',(-0.398997500090059,-0.470415578368488,
-2.6428296896942));
#67842=CARTESIAN_POINT('Ctrl Pts',(-0.1249803020654,-0.604044489707105,
-2.62892005974845));
#67843=CARTESIAN_POINT('Ctrl Pts',(0.179565789039688,-0.59012367250978,
-2.61501042980268));
#67844=CARTESIAN_POINT('Ctrl Pts',(0.440249409948256,-0.432053559747037,
-2.60110079985693));
#67845=CARTESIAN_POINT('Ctrl Pts',(0.593393467078218,-0.168445880563364,
-2.58719116991117));
#67846=CARTESIAN_POINT('Ctrl Pts',(0.601589517108825,0.136308012804258,
-2.57328153996541));
#67847=CARTESIAN_POINT('Ctrl Pts',(0.462835513870151,0.407765997295543,
-2.55937191001965));
#67848=CARTESIAN_POINT('Ctrl Pts',(0.211024847435283,0.579619129441731,
-2.54546228007389));
#67849=CARTESIAN_POINT('Ctrl Pts',(-0.0923327819865527,0.609888906949863,
-2.53155265012813));
#67850=CARTESIAN_POINT('Ctrl Pts',(-0.373136316222966,0.491181342240755,
-2.51764302018237));
#67851=CARTESIAN_POINT('Ctrl Pts',(-0.5627939777567,0.252493089114664,-2.50373339023661));
#67852=CARTESIAN_POINT('Ctrl Pts',(-0.614978158355398,-0.0478715593612716,
-2.48982376029085));
#67853=CARTESIAN_POINT('Ctrl Pts',(-0.516941847140863,-0.336542639385364,
-2.4759141303451));
#67854=CARTESIAN_POINT('Ctrl Pts',(-0.292632338315525,-0.54300657088277,
-2.46200450039934));
#67855=CARTESIAN_POINT('Ctrl Pts',(0.00315836571155932,-0.616830484149337,
-2.44809487045358));
#67856=CARTESIAN_POINT('Ctrl Pts',(0.29817757689118,-0.539981438652459,
-2.43418524050782));
#67857=CARTESIAN_POINT('Ctrl Pts',(0.520361059452317,-0.331231322878041,
-2.42027561056206));
#67858=CARTESIAN_POINT('Ctrl Pts',(0.615436134650789,-0.0415714519348385,
-2.4063659806163));
#67859=CARTESIAN_POINT('Ctrl Pts',(0.560178848332374,0.258243062502926,
-2.39245635067054));
#67860=CARTESIAN_POINT('Ctrl Pts',(0.368086877795425,0.494976637675649,
-2.37854672072479));
#67861=CARTESIAN_POINT('Ctrl Pts',(0.0860824590500775,0.610802448991298,
-2.36463709077902));
#67862=CARTESIAN_POINT('Ctrl Pts',(-0.216949290762728,0.5774277675064,-2.35072746083327));
#67863=CARTESIAN_POINT('Ctrl Pts',(-0.466986915964566,0.403005014569022,
-2.3368178308875));
#67864=CARTESIAN_POINT('Ctrl Pts',(-0.60295381648548,0.130140372811313,
-2.32290820094175));
#67865=CARTESIAN_POINT('Ctrl Pts',(-0.591637406822937,-0.174513610637414,
-2.30899857099599));
#67866=CARTESIAN_POINT('Ctrl Pts',(-0.435801942263024,-0.436539217676546,
-2.29508894105023));
#67867=CARTESIAN_POINT('Ctrl Pts',(-0.173513295243778,-0.591931548258345,
-2.28117931110447));
#67868=CARTESIAN_POINT('Ctrl Pts',(0.131159381506471,-0.602732974120973,
-2.26726968115871));
#67869=CARTESIAN_POINT('Ctrl Pts',(0.403793803681125,-0.466305034884467,
-2.25336005121295));
#67870=CARTESIAN_POINT('Ctrl Pts',(0.577793659804967,-0.215972933811292,
-2.2394504212672));
#67871=CARTESIAN_POINT('Ctrl Pts',(0.610656068097196,0.0871147975142503,
-2.22554079132143));
#67872=CARTESIAN_POINT('Ctrl Pts',(0.494353739996816,0.368923028829912,
-2.21163116137568));
#67873=CARTESIAN_POINT('Ctrl Pts',(0.257295803029569,0.560614565627085,
-2.19772153142991));
#67874=CARTESIAN_POINT('Ctrl Pts',(-0.0426116864745436,0.615364985700089,
-2.18381190148416));
#67875=CARTESIAN_POINT('Ctrl Pts',(-0.33211043477016,0.5198004237846,-2.1699022715384));
#67876=CARTESIAN_POINT('Ctrl Pts',(-0.540484687553777,0.297264400777774,
-2.15599264159264));
#67877=CARTESIAN_POINT('Ctrl Pts',(-0.616834941633162,0.00211571035066239,
-2.14208301164688));
#67878=CARTESIAN_POINT('Ctrl Pts',(-0.542511148121141,-0.293549783876869,
-2.12817338170112));
#67879=CARTESIAN_POINT('Ctrl Pts',(-0.335668353116679,-0.517509978807957,
-2.11426375175536));
#67880=CARTESIAN_POINT('Ctrl Pts',(-0.0468319711754508,-0.615058198811867,
-2.10035412180961));
#67881=CARTESIAN_POINT('Ctrl Pts',(0.253444039388315,-0.562366375549258,
-2.08644449186384));
#67882=CARTESIAN_POINT('Ctrl Pts',(0.491811366323612,-0.372305521587819,
-2.07253486191809));
#67883=CARTESIAN_POINT('Ctrl Pts',(0.610044109087587,-0.0913017328280638,
-2.05862523197233));
#67884=CARTESIAN_POINT('Ctrl Pts',(0.5792615984644,0.212004297112923,-2.04471560202657));
#67885=CARTESIAN_POINT('Ctrl Pts',(0.406983067165381,0.46352411424923,-2.03080597208081));
#67886=CARTESIAN_POINT('Ctrl Pts',(0.135290929580357,0.60181906402436,-2.01689634213505));
#67887=CARTESIAN_POINT('Ctrl Pts',(-0.169448674330592,0.593107889188367,
-2.00298671218929));
#67888=CARTESIAN_POINT('Ctrl Pts',(-0.432797111987588,0.439518465260651,
-1.98907708224353));
#67889=CARTESIAN_POINT('Ctrl Pts',(-0.590426355987388,0.178568025148203,
-1.97516745229777));
#67890=CARTESIAN_POINT('Ctrl Pts',(-0.603832368038419,-0.126001161736678,
-1.96125782235201));
#67891=CARTESIAN_POINT('Ctrl Pts',(-0.46974046643662,-0.399792090519286,
-1.94734819240625));
#67892=CARTESIAN_POINT('Ctrl Pts',(-0.220905231378247,-0.575925950274512,
-1.9334385624605));
#67893=CARTESIAN_POINT('Ctrl Pts',(0.0818904444712269,-0.611378586928083,
-1.91952893251474));
#67894=CARTESIAN_POINT('Ctrl Pts',(0.364682771134822,-0.49748999777614,
-1.90561930256898));
#67895=CARTESIAN_POINT('Ctrl Pts',(0.558394169490021,-0.262079707206459,
-1.89170967262322));
#67896=CARTESIAN_POINT('Ctrl Pts',(0.615706826480567,0.0373486984392127,
-1.87780004267746));
#67897=CARTESIAN_POINT('Ctrl Pts',(0.522621000159094,0.327653951055963,
-1.8638904127317));
#67898=CARTESIAN_POINT('Ctrl Pts',(0.301874731577736,0.537923291822119,
-1.84998078278594));
#67899=CARTESIAN_POINT('Ctrl Pts',(0.00738963174281488,0.616794305090912,
-1.83607115284018));
#67900=CARTESIAN_POINT('Ctrl Pts',(-0.288900530759199,0.545001197041739,
-1.82216152289442));
#67901=CARTESIAN_POINT('Ctrl Pts',(-0.514621065338475,0.340080844152928,
-1.80825189294867));
#67902=CARTESIAN_POINT('Ctrl Pts',(-0.614635298836539,0.052089066741446,
-1.79434226300291));
#67903=CARTESIAN_POINT('Ctrl Pts',(-0.564512790691757,-0.248626488120793,
-1.78043263305715));
#67904=CARTESIAN_POINT('Ctrl Pts',(-0.376496947799364,-0.488610140856324,
-1.76652300311139));
#67905=CARTESIAN_POINT('Ctrl Pts',(-0.0965143319473462,-0.609241171605,
-1.75261337316563));
#67906=CARTESIAN_POINT('Ctrl Pts',(0.207043804783216,-0.581053082214322,
-1.73870374321987));
#67907=CARTESIAN_POINT('Ctrl Pts',(0.460027426372314,-0.410931367061632,
-1.72479411327411));
#67908=CARTESIAN_POINT('Ctrl Pts',(0.600640315280387,-0.140431595838519,
-1.71088448332835));
#67909=CARTESIAN_POINT('Ctrl Pts',(0.594535012105725,0.164371350393919,
-1.69697485338259));
#67910=CARTESIAN_POINT('Ctrl Pts',(0.443202857041646,0.429023366449892,
-1.68306522343683));
#67911=CARTESIAN_POINT('Ctrl Pts',(0.183609700748073,0.588878000303185,
-1.66915559349108));
#67912=CARTESIAN_POINT('Ctrl Pts',(-0.120833730589114,0.604887618489413,
-1.65524596354532));
#67913=CARTESIAN_POINT('Ctrl Pts',(-0.39576115035726,0.473141557377675,
-1.64133633359956));
#67914=CARTESIAN_POINT('Ctrl Pts',(-0.574016137390193,0.225821379558084,
-1.6274267036538));
#67915=CARTESIAN_POINT('Ctrl Pts',(-0.61205641062243,-0.0766601047864005,
-1.61351707370804));
#67916=CARTESIAN_POINT('Ctrl Pts',(-0.500589886301045,-0.360415853123835,
-1.59960744376228));
#67917=CARTESIAN_POINT('Ctrl Pts',(-0.266844451915646,-0.556132951668676,
-1.58569781381652));
#67918=CARTESIAN_POINT('Ctrl Pts',(0.0320829800086549,-0.616003655706393,
-1.57178818387076));
#67919=CARTESIAN_POINT('Ctrl Pts',(0.323173514036252,-0.525403370064692,
-1.557878553925));
#67920=CARTESIAN_POINT('Ctrl Pts',(0.53532257093991,-0.306462993674867,
-1.54396892397925));
#67921=CARTESIAN_POINT('Ctrl Pts',(0.61670857749334,-0.0126630129122495,
-1.53005929403348));
#67922=CARTESIAN_POINT('Ctrl Pts',(0.54745140337799,0.284230157424129,-1.51614966408773));
#67923=CARTESIAN_POINT('Ctrl Pts',(0.344468473409441,0.511694530239325,
-1.50224003414196));
#67924=CARTESIAN_POINT('Ctrl Pts',(0.0573423543102443,0.614167465641117,
-1.48833040419621));
#67925=CARTESIAN_POINT('Ctrl Pts',(-0.243790760889837,0.566617936845128,
-1.47442077425045));
#67926=CARTESIAN_POINT('Ctrl Pts',(-0.485373195300982,0.38066085001375,
-1.46051114430469));
#67927=CARTESIAN_POINT('Ctrl Pts',(-0.608393695242684,0.101719875338241,
-1.44660151435893));
#67928=CARTESIAN_POINT('Ctrl Pts',(-0.582802087788846,-0.202068176412908,
-1.43269188441317));
#67929=CARTESIAN_POINT('Ctrl Pts',(-0.414849625615314,-0.456497107960948,
-1.41878225446741));
#67930=CARTESIAN_POINT('Ctrl Pts',(-0.145561995774814,-0.599417656426576,
-1.40487262452166));
#67931=CARTESIAN_POINT('Ctrl Pts',(0.159282010007692,-0.595918671244479,
-1.3909629945759));
#67932=CARTESIAN_POINT('Ctrl Pts',(0.425218256945002,-0.446854848256713,
-1.37705336463014));
#67933=CARTESIAN_POINT('Ctrl Pts',(0.587286594399046,-0.188637953469192,
-1.36314373468438));
#67934=CARTESIAN_POINT('Ctrl Pts',(0.60589864832935,0.115657465831397,-1.34923410473862));
#67935=CARTESIAN_POINT('Ctrl Pts',(0.47650805906919,0.391701277878931,-1.33532447479286));
#67936=CARTESIAN_POINT('Ctrl Pts',(0.230721018953334,0.572064360769845,
-1.3214148448471));
#67937=CARTESIAN_POINT('Ctrl Pts',(-0.0714241608263882,0.612689489627594,
-1.30750521490134));
#67938=CARTESIAN_POINT('Ctrl Pts',(-0.356122586732152,0.503653178952617,
-1.29359558495559));
#67939=CARTESIAN_POINT('Ctrl Pts',(-0.553831077470514,0.271589688828064,
-1.27968595500982));
#67940=CARTESIAN_POINT('Ctrl Pts',(-0.616255451677714,-0.0268149161358486,
-1.26577632506407));
#67941=CARTESIAN_POINT('Ctrl Pts',(-0.528147330094856,-0.318669451255607,
-1.2518666951183));
#67942=CARTESIAN_POINT('Ctrl Pts',(-0.311028851641987,-0.53268271503414,
-1.23795706517255));
#67943=CARTESIAN_POINT('Ctrl Pts',(-0.0179354683458115,-0.616577765107606,
-1.22404743522679));
#67944=CARTESIAN_POINT('Ctrl Pts',(0.279539005301622,-0.54986158800634,
-1.21013780528103));
#67945=CARTESIAN_POINT('Ctrl Pts',(0.508730587456313,-0.348830920126398,
-1.19622817533527));
#67946=CARTESIAN_POINT('Ctrl Pts',(0.613654733426786,-0.0625914498376293,
-1.18231854538951));
#67947=CARTESIAN_POINT('Ctrl Pts',(0.568681660111602,0.238937211213715,
-1.16840891544375));
#67948=CARTESIAN_POINT('Ctrl Pts',(0.384796923826821,0.482100766296105,
-1.15449928549799));
#67949=CARTESIAN_POINT('Ctrl Pts',(0.106917982446909,0.607501741955822,
-1.14058965555223));
#67950=CARTESIAN_POINT('Ctrl Pts',(-0.197077775747773,0.584508487326049,
-1.12668002560648));
#67951=CARTESIAN_POINT('Ctrl Pts',(-0.452933417100812,0.418737556380195,
-1.11277039566072));
#67952=CARTESIAN_POINT('Ctrl Pts',(-0.598151176846013,0.150681754328804,
-1.09886076571496));
#67953=CARTESIAN_POINT('Ctrl Pts',(-0.597258765451536,-0.154181025230674,
-1.0849511357692));
#67954=CARTESIAN_POINT('Ctrl Pts',(-0.45047417192522,-0.421382061647338,
-1.07104150582344));
#67955=CARTESIAN_POINT('Ctrl Pts',(-0.193652415718641,-0.585652254615492,
-1.05713187587768));
#67956=CARTESIAN_POINT('Ctrl Pts',(0.110472745876953,-0.606865383646391,
-1.04322224593192));
#67957=CARTESIAN_POINT('Ctrl Pts',(0.387612769883316,-0.479839725401367,
-1.02931261598616));
#67958=CARTESIAN_POINT('Ctrl Pts',(0.570070763099067,-0.235603791373405,
-1.0154029860404));
#67959=CARTESIAN_POINT('Ctrl Pts',(0.613277777662018,0.0661829953674764,
-1.00149335609464));
#67960=CARTESIAN_POINT('Ctrl Pts',(0.506679651787328,0.351803285821137,
-0.987583726148887));
#67961=CARTESIAN_POINT('Ctrl Pts',(0.276315071040818,0.55148871517519,-0.973674096203127));
#67962=CARTESIAN_POINT('Ctrl Pts',(-0.021544891945215,0.61646219598686,
-0.959764466257368));
#67963=CARTESIAN_POINT('Ctrl Pts',(-0.314142091985768,0.530852679651031,
-0.94585483631161));
#67964=CARTESIAN_POINT('Ctrl Pts',(-0.530003917092785,0.315571971689786,
-0.931945206365851));
#67965=CARTESIAN_POINT('Ctrl Pts',(-0.616401877496817,0.0232066125980274,
-0.918035576420091));
#67966=CARTESIAN_POINT('Ctrl Pts',(-0.552231574729038,-0.274827417340706,
-0.904125946474334));
#67967=CARTESIAN_POINT('Ctrl Pts',(-0.353167865384941,-0.505729453669963,
-0.890216316528573));
#67968=CARTESIAN_POINT('Ctrl Pts',(-0.0678359695858457,-0.613097139677086,
-0.876306686582815));
#67969=CARTESIAN_POINT('Ctrl Pts',(0.234066193913592,-0.570703809621663,
-0.862397056637055));
#67970=CARTESIAN_POINT('Ctrl Pts',(0.478793093074244,-0.388904866868846,
-0.848487426691297));
#67971=CARTESIAN_POINT('Ctrl Pts',(0.6065653769511,-0.112108273263145,-0.834577796745537));
#67972=CARTESIAN_POINT('Ctrl Pts',(0.586172156078744,0.192072967613535,
-0.820668166799778));
#67973=CARTESIAN_POINT('Ctrl Pts',(0.422594875127169,0.449336614317292,
-0.806758536854021));
#67974=CARTESIAN_POINT('Ctrl Pts',(0.155790497218003,0.596840969125313,
-0.79284890690826));
#67975=CARTESIAN_POINT('Ctrl Pts',(-0.149068768972891,0.598555196758647,
-0.778939276962503));
#67976=CARTESIAN_POINT('Ctrl Pts',(-0.417515061003882,0.454060563454701,
-0.765029647016743));
#67977=CARTESIAN_POINT('Ctrl Pts',(-0.583975100431752,0.198652720911643,
-0.751120017070985));
#67978=CARTESIAN_POINT('Ctrl Pts',(-0.607787753766864,-0.105279949757325,
-0.737210387125225));
#67979=CARTESIAN_POINT('Ctrl Pts',(-0.48313631281108,-0.383495925262826,
-0.723300757179466));
#67980=CARTESIAN_POINT('Ctrl Pts',(-0.240469339860789,-0.568035490120813,
-0.709391127233706));
#67981=CARTESIAN_POINT('Ctrl Pts',(0.0609369915676775,-0.613821231718611,
-0.695481497287948));
#67982=CARTESIAN_POINT('Ctrl Pts',(0.34745826615543,-0.509669083553375,
-0.681571867342189));
#67983=CARTESIAN_POINT('Ctrl Pts',(0.549106036022265,-0.281020253102492,
-0.667662237396431));
#67984=CARTESIAN_POINT('Ctrl Pts',(0.616623873519691,0.0162732927045065,
-0.653752607450671));
#67985=CARTESIAN_POINT('Ctrl Pts',(0.533519220957275,0.309591767201617,
-0.639842977504913));
#67986=CARTESIAN_POINT('Ctrl Pts',(0.320092021691175,0.527286372950726,
-0.625933347559153));
#67987=CARTESIAN_POINT('Ctrl Pts',(0.0284760603192387,0.61618092751932,
-0.612023717613395));
#67988=CARTESIAN_POINT('Ctrl Pts',(-0.270095737984369,0.554561190287018,
-0.598114087667635));
#67989=CARTESIAN_POINT('Ctrl Pts',(-0.502691348279656,0.357478992130528,
-0.584204457721876));
#67990=CARTESIAN_POINT('Ctrl Pts',(-0.612494725155188,0.0730755301516669,
-0.570294827776117));
#67991=CARTESIAN_POINT('Ctrl Pts',(-0.572684237545063,-0.229178065087615,
-0.556385197830358));
#67992=CARTESIAN_POINT('Ctrl Pts',(-0.392984378826605,-0.475450417444492,
-0.542475567884599));
#67993=CARTESIAN_POINT('Ctrl Pts',(-0.117290368348157,-0.60558466868195,
-0.52856593793884));
#67994=CARTESIAN_POINT('Ctrl Pts',(0.187054117889196,-0.587792972423601,
-0.514656307993082));
#67995=CARTESIAN_POINT('Ctrl Pts',(0.44570696255647,-0.426421299865004,
-0.500746678047323));
#67996=CARTESIAN_POINT('Ctrl Pts',(0.595487129047879,-0.160887850965181,
-0.486837048101563));
#67997=CARTESIAN_POINT('Ctrl Pts',(0.599807870389539,0.143945614968422,
-0.472927418155804));
#67998=CARTESIAN_POINT('Ctrl Pts',(0.457613760660216,0.413617537713629,
-0.459017788210046));
#67999=CARTESIAN_POINT('Ctrl Pts',(0.203638503498379,0.58225525445705,-0.445108158264286));
#68000=CARTESIAN_POINT('Ctrl Pts',(-0.100079457094422,0.608665691260386,
-0.431198528318528));
#68001=CARTESIAN_POINT('Ctrl Pts',(-0.379351044981491,0.486397580299782,
-0.417288898372769));
#68002=CARTESIAN_POINT('Ctrl Pts',(-0.565958690624595,0.245317308716941,
-0.40337926842701));
#68003=CARTESIAN_POINT('Ctrl Pts',(-0.61431981206814,-0.0556865329382699,
-0.389469638481251));
#68004=CARTESIAN_POINT('Ctrl Pts',(-0.512621255706389,-0.343087845380705,
-0.375560008535491));
#68005=CARTESIAN_POINT('Ctrl Pts',(-0.2857048910393,-0.546683214197066,
-0.361650378589733));
#68006=CARTESIAN_POINT('Ctrl Pts',(0.0110005037984258,-0.61674047245988,
-0.347740748643974));
#68007=CARTESIAN_POINT('Ctrl Pts',(0.305018809553407,-0.536146759068512,
-0.333831118698214));
#68008=CARTESIAN_POINT('Ctrl Pts',(0.524530281282194,-0.324588671217872,
-0.319921488752457));
#68009=CARTESIAN_POINT('Ctrl Pts',(0.615914931314421,-0.0337434262600359,
-0.306011858806697));
#68010=CARTESIAN_POINT('Ctrl Pts',(0.55685026439868,0.265344313097788,-0.292102228860939));
#68011=CARTESIAN_POINT('Ctrl Pts',(0.361763985145107,0.499616493478627,
-0.278192598915179));
#68012=CARTESIAN_POINT('Ctrl Pts',(0.0783097485940909,0.61184753372299,
-0.26428296896942));
#68013=CARTESIAN_POINT('Ctrl Pts',(-0.224273182279628,0.574622799449323,
-0.250373339023661));
#68014=CARTESIAN_POINT('Ctrl Pts',(-0.47207298339421,0.397035160785883,
-0.236463709077903));
#68015=CARTESIAN_POINT('Ctrl Pts',(-0.60455968958736,0.122463890190093,
-0.222554079132143));
#68016=CARTESIAN_POINT('Ctrl Pts',(-0.58937081641643,-0.182021596075152,
-0.208644449186384));
#68017=CARTESIAN_POINT('Ctrl Pts',(-0.430216553701672,-0.442044722094857,
-0.194734819240625));
#68018=CARTESIAN_POINT('Ctrl Pts',(-0.165973437374469,-0.594089765496738,
-0.180825189294867));
#68019=CARTESIAN_POINT('Ctrl Pts',(0.138811926899389,-0.601016675400649,
-0.166915559349108));
#68020=CARTESIAN_POINT('Ctrl Pts',(0.409689797907612,-0.461133541629717,
-0.153005929403349));
#68021=CARTESIAN_POINT('Ctrl Pts',(0.580492800990502,-0.208609325030388,
-0.13909629945759));
#68022=CARTESIAN_POINT('Ctrl Pts',(0.609499212910961,0.0948715035369464,
-0.12518666951183));
#68023=CARTESIAN_POINT('Ctrl Pts',(0.489623131224122,0.375178714510168,
-0.111277039566072));
#68024=CARTESIAN_POINT('Ctrl Pts',(0.250147652741445,0.563839964446146,
-0.0973674096203128));
#68025=CARTESIAN_POINT('Ctrl Pts',(-0.0504326075969051,0.614774560998643,
-0.0834577796745534));
#68026=CARTESIAN_POINT('Ctrl Pts',(-0.338691162031732,0.515533844114401,
-0.0695481497287943));
#68027=CARTESIAN_POINT('Ctrl Pts',(-0.544222735363936,0.290372764715117,
-0.0556385197830353));
#68028=CARTESIAN_POINT('Ctrl Pts',(-0.61680746585949,-0.00573499015792564,
-0.0417288898372768));
#68029=CARTESIAN_POINT('Ctrl Pts',(-0.538744006451602,-0.300407514267951,
-0.0278192598915181));
#68030=CARTESIAN_POINT('Ctrl Pts',(-0.329043395961403,-0.521769848422279,
-0.0139096299457593));
#68031=CARTESIAN_POINT('Ctrl Pts',(-0.135716027844311,-0.584261894770184,
-0.00463654331525315));
#68032=CARTESIAN_POINT('Ctrl Pts',(-0.0374170035146652,-0.590490705661811,
0.));
#68033=CARTESIAN_POINT('Ctrl Pts',(0.324375760296889,-0.454512507566726,
-3.98675728291906));
#68034=CARTESIAN_POINT('Ctrl Pts',(0.400038485571038,-0.400513654667537,
-3.9821207396038));
#68035=CARTESIAN_POINT('Ctrl Pts',(0.52379810564881,-0.254053407725315,
-3.97284765297329));
#68036=CARTESIAN_POINT('Ctrl Pts',(0.581471950593503,0.0278744202397417,
-3.95893802302754));
#68037=CARTESIAN_POINT('Ctrl Pts',(0.497114145262111,0.302917967212516,
-3.94502839308178));
#68038=CARTESIAN_POINT('Ctrl Pts',(0.291324666108956,0.504004920085947,
-3.93111876313602));
#68039=CARTESIAN_POINT('Ctrl Pts',(0.0143742891377185,0.581959948381398,
-3.91720913319026));
#68040=CARTESIAN_POINT('Ctrl Pts',(-0.26608773317726,0.517769450825752,
-3.9032995032445));
#68041=CARTESIAN_POINT('Ctrl Pts',(-0.48155237504841,0.327098675931684,
-3.88938987329875));
#68042=CARTESIAN_POINT('Ctrl Pts',(-0.579388508604397,0.0565301441845764,
-3.87548024335298));
#68043=CARTESIAN_POINT('Ctrl Pts',(-0.535697561949923,-0.227848273936975,
-3.86157061340723));
#68044=CARTESIAN_POINT('Ctrl Pts',(-0.36115199634089,-0.456569617418363,
-3.84766098346147));
#68045=CARTESIAN_POINT('Ctrl Pts',(-0.098387947990684,-0.573765203358985,
-3.8337513535157));
#68046=CARTESIAN_POINT('Ctrl Pts',(0.188409280812262,-0.550807198412802,
-3.81984172356995));
#68047=CARTESIAN_POINT('Ctrl Pts',(0.429183846950857,-0.393303807123812,
-3.80593209362419));
#68048=CARTESIAN_POINT('Ctrl Pts',(0.565121828294565,-0.139728192232451,
-3.79202246367843));
#68049=CARTESIAN_POINT('Ctrl Pts',(0.563017706559736,0.147978754391011,
-3.77811283373267));
#68050=CARTESIAN_POINT('Ctrl Pts',(0.423385453192029,0.399538996158907,
-3.76420320378691));
#68051=CARTESIAN_POINT('Ctrl Pts',(0.180332988927896,0.553503986109699,
-3.75029357384115));
#68052=CARTESIAN_POINT('Ctrl Pts',(-0.106769349313841,0.572264761117087,
-3.7363839438954));
#68053=CARTESIAN_POINT('Ctrl Pts',(-0.367791177229423,0.451238628785029,
-3.72247431394964));
#68054=CARTESIAN_POINT('Ctrl Pts',(-0.53897278764399,0.2199886009843,-3.70856468400387));
#68055=CARTESIAN_POINT('Ctrl Pts',(-0.578499710578128,-0.064997963048793,
-3.69465505405812));
#68056=CARTESIAN_POINT('Ctrl Pts',(-0.476716718924004,-0.334107497997054,
-3.68074542411236));
#68057=CARTESIAN_POINT('Ctrl Pts',(-0.258486307142088,-0.521604715631567,
-3.6668357941666));
#68058=CARTESIAN_POINT('Ctrl Pts',(0.0228844611821437,-0.581689738403682,
-3.65292616422084));
#68059=CARTESIAN_POINT('Ctrl Pts',(0.298665250470289,-0.499685619665673,
-3.63901653427508));
#68060=CARTESIAN_POINT('Ctrl Pts',(0.501491187290892,-0.295623475732306,
-3.62510690432932));
#68061=CARTESIAN_POINT('Ctrl Pts',(0.581818053581754,-0.0193494925521338,
-3.61119727438356));
#68062=CARTESIAN_POINT('Ctrl Pts',(0.520024434831806,0.261650984163416,
-3.5972876444378));
#68063=CARTESIAN_POINT('Ctrl Pts',(0.331204635893308,0.478738069823327,
-3.58337801449205));
#68064=CARTESIAN_POINT('Ctrl Pts',(0.0614816006060668,0.578883980710003,
-3.56946838454629));
#68065=CARTESIAN_POINT('Ctrl Pts',(-0.223259522974249,0.537626111472319,
-3.55555875460053));
#68066=CARTESIAN_POINT('Ctrl Pts',(-0.453465123808749,0.365042506873849,
-3.54164912465477));
#68067=CARTESIAN_POINT('Ctrl Pts',(-0.5729029632306,0.103290101448284,-3.52773949470901));
#68068=CARTESIAN_POINT('Ctrl Pts',(-0.552398003500193,-0.183692939615547,
-3.51382986476325));
#68069=CARTESIAN_POINT('Ctrl Pts',(-0.396958983697868,-0.425805372907814,
-3.49992023481749));
#68070=CARTESIAN_POINT('Ctrl Pts',(-0.144554936844433,-0.563906482113393,
-3.48601060487173));
#68071=CARTESIAN_POINT('Ctrl Pts',(0.143159492031142,-0.564262359348016,
-3.47210097492597));
#68072=CARTESIAN_POINT('Ctrl Pts',(0.395904403683274,-0.426786074608572,
-3.45819134498022));
#68073=CARTESIAN_POINT('Ctrl Pts',(0.551941890162178,-0.185058910133518,
-3.44428171503445));
#68074=CARTESIAN_POINT('Ctrl Pts',(0.573156731208902,0.101872527236398,
-3.4303720850887));
#68075=CARTESIAN_POINT('Ctrl Pts',(0.454366785291294,0.36391959930685,-3.41646245514293));
#68076=CARTESIAN_POINT('Ctrl Pts',(0.224588829437554,0.537072162774681,
-3.40255282519718));
#68077=CARTESIAN_POINT('Ctrl Pts',(-0.0600493583699365,0.57903430372903,
-3.38864319525142));
#68078=CARTESIAN_POINT('Ctrl Pts',(-0.330019311176162,0.479555945210164,
-3.37473356530566));
#68079=CARTESIAN_POINT('Ctrl Pts',(-0.51937556647267,0.262936629792801,
-3.3608239353599));
#68080=CARTESIAN_POINT('Ctrl Pts',(-0.581864140419413,-0.0179101208700953,
-3.34691430541415));
#68081=CARTESIAN_POINT('Ctrl Pts',(-0.50222097171039,-0.294381972800433,
-3.33300467546838));
#68082=CARTESIAN_POINT('Ctrl Pts',(-0.299900468295682,-0.498945246947632,
-3.31909504552263));
#68083=CARTESIAN_POINT('Ctrl Pts',(-0.0243233862036543,-0.581631346489502,
-3.30518541557686));
#68084=CARTESIAN_POINT('Ctrl Pts',(0.257195160619166,-0.522242567864479,
-3.29127578563111));
#68085=CARTESIAN_POINT('Ctrl Pts',(0.475888738790229,-0.335285786498994,
-3.27736615568535));
#68086=CARTESIAN_POINT('Ctrl Pts',(0.578337147245635,-0.0664288676057664,
-3.26345652573959));
#68087=CARTESIAN_POINT('Ctrl Pts',(0.539515350389306,0.218654606697199,
-3.24954689579383));
#68088=CARTESIAN_POINT('Ctrl Pts',(0.368906334466525,0.450327399484059,
-3.23563726584807));
#68089=CARTESIAN_POINT('Ctrl Pts',(0.108184701951348,0.571998881641653,
-3.22172763590231));
#68090=CARTESIAN_POINT('Ctrl Pts',(-0.178963168492766,0.553948404328989,
-3.20781800595655));
#68091=CARTESIAN_POINT('Ctrl Pts',(-0.422395770642912,0.400585151095974,
-3.19390837601079));
#68092=CARTESIAN_POINT('Ctrl Pts',(-0.562649911015658,0.149371108215993,
-3.17999874606504));
#68093=CARTESIAN_POINT('Ctrl Pts',(-0.565465761583983,-0.138329761121207,
-3.16608911611927));
#68094=CARTESIAN_POINT('Ctrl Pts',(-0.430155495550294,-0.392240869853568,
-3.15217948617352));
#68095=CARTESIAN_POINT('Ctrl Pts',(-0.189771302548966,-0.550339443493261,
-3.13826985622776));
#68096=CARTESIAN_POINT('Ctrl Pts',(0.0969682577343136,-0.574006800767704,
-3.124360226282));
#68097=CARTESIAN_POINT('Ctrl Pts',(0.360021416851612,-0.457461724894838,
-3.11045059633624));
#68098=CARTESIAN_POINT('Ctrl Pts',(0.53513227498155,-0.22917263931079,-3.09654096639048));
#68099=CARTESIAN_POINT('Ctrl Pts',(0.579526566286031,0.0550963638031215,
-3.08263133644472));
#68100=CARTESIAN_POINT('Ctrl Pts',(0.482360113320941,0.325906998103159,
-3.06872170649896));
#68101=CARTESIAN_POINT('Ctrl Pts',(0.267367730329437,0.517108448117112,
-3.05481207655321));
#68102=CARTESIAN_POINT('Ctrl Pts',(-0.0129344712294171,0.581996004960188,
-3.04090244660744));
#68103=CARTESIAN_POINT('Ctrl Pts',(-0.290077174189779,0.504719608643924,
-3.02699281666169));
#68104=CARTESIAN_POINT('Ctrl Pts',(-0.496362830963149,0.30415553648397,
-3.01308318671593));
#68105=CARTESIAN_POINT('Ctrl Pts',(-0.581402118947598,0.0292955016827951,
-2.99917355677017));
#68106=CARTESIAN_POINT('Ctrl Pts',(-0.524422522093719,-0.252720534694878,
-2.98526392682441));
#68107=CARTESIAN_POINT('Ctrl Pts',(-0.339342425870034,-0.473004617673278,
-2.97135429687865));
#68108=CARTESIAN_POINT('Ctrl Pts',(-0.0713712782899644,-0.577748034155773,
-2.95744466693289));
#68109=CARTESIAN_POINT('Ctrl Pts',(0.214033705566062,-0.541365147767442,
-2.94353503698713));
#68110=CARTESIAN_POINT('Ctrl Pts',(0.447156753750219,-0.372743192977644,
-2.92962540704137));
#68111=CARTESIAN_POINT('Ctrl Pts',(0.571052983789159,-0.113071393557795,
-2.91571577709561));
#68112=CARTESIAN_POINT('Ctrl Pts',(0.555458308483385,0.174220314178282,
-2.90180614714986));
#68113=CARTESIAN_POINT('Ctrl Pts',(0.404182033516805,0.418955288924514,
-2.8878965172041));
#68114=CARTESIAN_POINT('Ctrl Pts',(0.154176359738182,0.561352207115539,
-2.87398688725834));
#68115=CARTESIAN_POINT('Ctrl Pts',(-0.133489917545092,0.566627825163402,
-2.86007725731258));
#68116=CARTESIAN_POINT('Ctrl Pts',(-0.388548661059429,0.433493469759958,
-2.84616762736682));
#68117=CARTESIAN_POINT('Ctrl Pts',(-0.548696763984826,0.194469821638688,
-2.83225799742106));
#68118=CARTESIAN_POINT('Ctrl Pts',(-0.574814907273033,-0.092056899319377,
-2.8183483674753));
#68119=CARTESIAN_POINT('Ctrl Pts',(-0.46052322153081,-0.356096914851124,
-2.80443873752954));
#68120=CARTESIAN_POINT('Ctrl Pts',(-0.23373969540392,-0.533153266076544,
-2.79052910758379));
#68121=CARTESIAN_POINT('Ctrl Pts',(0.0501393413891527,-0.579976462264345,
-2.77661947763802));
#68122=CARTESIAN_POINT('Ctrl Pts',(0.3217708594365,-0.48512901825504,-2.76270984769227));
#68123=CARTESIAN_POINT('Ctrl Pts',(0.51480352629053,-0.271779284814791,
-2.74880021774651));
#68124=CARTESIAN_POINT('Ctrl Pts',(0.58208532239273,0.00795787600776863,
-2.73489058780075));
#68125=CARTESIAN_POINT('Ctrl Pts',(0.507181347798721,0.285751169342622,
-2.72098095785499));
#68126=CARTESIAN_POINT('Ctrl Pts',(0.308388369230054,0.493744128126331,
-2.70707132790923));
#68127=CARTESIAN_POINT('Ctrl Pts',(0.0342654754996764,0.581130387713793,
-2.69316169796347));
#68128=CARTESIAN_POINT('Ctrl Pts',(-0.248227433509849,0.526564138152911,
-2.67925206801771));
#68129=CARTESIAN_POINT('Ctrl Pts',(-0.470085917317827,0.343374257443769,
-2.66534243807196));
#68130=CARTESIAN_POINT('Ctrl Pts',(-0.577116684507702,0.0763084713412617,
-2.65143280812619));
#68131=CARTESIAN_POINT('Ctrl Pts',(-0.543175368376425,-0.209397157394121,
-2.63752317818044));
#68132=CARTESIAN_POINT('Ctrl Pts',(-0.376552801911728,-0.443953418398857,
-2.62361354823468));
#68133=CARTESIAN_POINT('Ctrl Pts',(-0.117949819023622,-0.570065338823453,
-2.60970391828892));
#68134=CARTESIAN_POINT('Ctrl Pts',(0.169464723400831,-0.556927605581088,
-2.59579428834316));
#68135=CARTESIAN_POINT('Ctrl Pts',(0.415484179270755,-0.407749368008474,
-2.5818846583974));
#68136=CARTESIAN_POINT('Ctrl Pts',(0.560013465282322,-0.158970340120692,
-2.56797502845164));
#68137=CARTESIAN_POINT('Ctrl Pts',(0.567748465133041,0.128640315121969,
-2.55406539850589));
#68138=CARTESIAN_POINT('Ctrl Pts',(0.436799753213296,0.384828047221623,
-2.54015576856012));
#68139=CARTESIAN_POINT('Ctrl Pts',(0.199154123915099,0.54701397172578,-2.52624613861437));
#68140=CARTESIAN_POINT('Ctrl Pts',(-0.0871388110389003,0.575580991647856,
-2.5123365086686));
#68141=CARTESIAN_POINT('Ctrl Pts',(-0.352146380208058,0.46355105138697,
-2.49842687872284));
#68142=CARTESIAN_POINT('Ctrl Pts',(-0.531135280736092,0.238289663840034,
-2.48451724877709));
#68143=CARTESIAN_POINT('Ctrl Pts',(-0.580383958774104,-0.0451786535136231,
-2.47060761883133));
#68144=CARTESIAN_POINT('Ctrl Pts',(-0.487862457590284,-0.317611197550671,
-2.45669798888557));
#68145=CARTESIAN_POINT('Ctrl Pts',(-0.276170970739966,-0.512460969495384,
-2.44278835893981));
#68146=CARTESIAN_POINT('Ctrl Pts',(0.00298069902162641,-0.582132086187444,
-2.42887872899405));
#68147=CARTESIAN_POINT('Ctrl Pts',(0.281404274513702,-0.509606009208113,
-2.41496909904829));
#68148=CARTESIAN_POINT('Ctrl Pts',(0.491089329878754,-0.312598657090589,
-2.40105946910253));
#68149=CARTESIAN_POINT('Ctrl Pts',(0.580816172653138,-0.0392329443218781,
-2.38714983915677));
#68150=CARTESIAN_POINT('Ctrl Pts',(0.528667259478138,0.243716185534479,
-2.37324020921101));
#68151=CARTESIAN_POINT('Ctrl Pts',(0.347380986471149,0.467132851096918,
-2.35933057926526));
#68152=CARTESIAN_POINT('Ctrl Pts',(0.0812400858236996,0.576443144456556,
-2.3454209493195));
#68153=CARTESIAN_POINT('Ctrl Pts',(-0.20474530113855,0.544945879879174,
-2.33151131937374));
#68154=CARTESIAN_POINT('Ctrl Pts',(-0.44071762761141,0.380334882765405,
-2.31760168942798));
#68155=CARTESIAN_POINT('Ctrl Pts',(-0.569036018946812,0.122819621709097,
-2.30369205948222));
#68156=CARTESIAN_POINT('Ctrl Pts',(-0.558356188208398,-0.164696743820245,
-2.28978242953646));
#68157=CARTESIAN_POINT('Ctrl Pts',(-0.411286893779221,-0.41198269543883,
-2.2758727995907));
#68158=CARTESIAN_POINT('Ctrl Pts',(-0.163752698897196,-0.558633783385402,
-2.26196316964495));
#68159=CARTESIAN_POINT('Ctrl Pts',(0.123781308384447,-0.568827599567951,
-2.24805353969918));
#68160=CARTESIAN_POINT('Ctrl Pts',(0.381079300337477,-0.440074104202806,
-2.23414390975343));
#68161=CARTESIAN_POINT('Ctrl Pts',(0.545291189737489,-0.203823866929948,
-2.22023427980766));
#68162=CARTESIAN_POINT('Ctrl Pts',(0.576304997887196,0.0822143524321826,
-2.20632464986191));
#68163=CARTESIAN_POINT('Ctrl Pts',(0.466544993112303,0.348170101728228,
-2.19241501991615));
#68164=CARTESIAN_POINT('Ctrl Pts',(0.242822211991412,0.529078466486023,
-2.17850538997039));
#68165=CARTESIAN_POINT('Ctrl Pts',(-0.0402146628300982,0.580749026025068,
-2.16459576002463));
#68166=CARTESIAN_POINT('Ctrl Pts',(-0.313428316539825,0.490560231497228,
-2.15068613007887));
#68167=CARTESIAN_POINT('Ctrl Pts',(-0.510080948985451,0.280542467048581,
-2.13677650013311));
#68168=CARTESIAN_POINT('Ctrl Pts',(-0.582136292925639,0.00199669587001278,
-2.12286687018735));
#68169=CARTESIAN_POINT('Ctrl Pts',(-0.511993415616024,-0.277036807484928,
-2.10895724024159));
#68170=CARTESIAN_POINT('Ctrl Pts',(-0.31678609227038,-0.488398630300768,
-2.09504761029584));
#68171=CARTESIAN_POINT('Ctrl Pts',(-0.0441975450001183,-0.580459496736478,
-2.08113798035008));
#68172=CARTESIAN_POINT('Ctrl Pts',(0.239187120565808,-0.530731732319673,
-2.06722835040432));
#68173=CARTESIAN_POINT('Ctrl Pts',(0.464145634895935,-0.351362320038238,
-2.05331872045856));
#68174=CARTESIAN_POINT('Ctrl Pts',(0.575727463241813,-0.0861657612091384,
-2.0394090905128));
#68175=CARTESIAN_POINT('Ctrl Pts',(0.546676552841566,0.200078476875617,
-2.02549946056704));
#68176=CARTESIAN_POINT('Ctrl Pts',(0.384089159047769,0.437449617941975,
-2.01158983062128));
#68177=CARTESIAN_POINT('Ctrl Pts',(0.127680445604864,0.567965099408182,
-1.99768020067552));
#68178=CARTESIAN_POINT('Ctrl Pts',(-0.159916724002057,0.559743951928069,
-1.98377057072976));
#68179=CARTESIAN_POINT('Ctrl Pts',(-0.408451093406464,0.414794352216454,
-1.969860940784));
#68180=CARTESIAN_POINT('Ctrl Pts',(-0.557213262287108,0.168523086450973,
-1.95595131083824));
#68181=CARTESIAN_POINT('Ctrl Pts',(-0.569865149577474,-0.118913252552635,
-1.94204168089249));
#68182=CARTESIAN_POINT('Ctrl Pts',(-0.443316283355426,-0.377302694461006,
-1.92813205094673));
#68183=CARTESIAN_POINT('Ctrl Pts',(-0.208478709299335,-0.543528543964792,
-1.91422242100097));
#68184=CARTESIAN_POINT('Ctrl Pts',(0.0772838835042257,-0.576986873062212,
-1.90031279105521));
#68185=CARTESIAN_POINT('Ctrl Pts',(0.34416837009945,-0.46950482783321,-1.88640316110945));
#68186=CARTESIAN_POINT('Ctrl Pts',(0.526982973690763,-0.247337008503869,
-1.87249353116369));
#68187=CARTESIAN_POINT('Ctrl Pts',(0.581071637328817,0.0352477322335796,
-1.85858390121793));
#68188=CARTESIAN_POINT('Ctrl Pts',(0.493222142753769,0.30922252219556,-1.84467427127217));
#68189=CARTESIAN_POINT('Ctrl Pts',(0.284893454160213,0.507663638753324,
-1.83076464132642));
#68190=CARTESIAN_POINT('Ctrl Pts',(0.00697394479219623,0.582097942299781,
-1.81685501138065));
#68191=CARTESIAN_POINT('Ctrl Pts',(-0.272649087542171,0.514343392489906,
-1.8029453814349));
#68192=CARTESIAN_POINT('Ctrl Pts',(-0.485672226097312,0.320950368644881,
-1.78903575148914));
#68193=CARTESIAN_POINT('Ctrl Pts',(-0.580060386038787,0.0491589145947808,
-1.77512612154338));
#68194=CARTESIAN_POINT('Ctrl Pts',(-0.532757405753194,-0.234640569703385,
-1.76121649159762));
#68195=CARTESIAN_POINT('Ctrl Pts',(-0.355317967087673,-0.461124487096798,
-1.74730686165186));
#68196=CARTESIAN_POINT('Ctrl Pts',(-0.0910851374036396,-0.574969693183704,
-1.7333972317061));
#68197=CARTESIAN_POINT('Ctrl Pts',(0.19539702577582,-0.548367260741893,
-1.71948760176034));
#68198=CARTESIAN_POINT('Ctrl Pts',(0.434149628300019,-0.387815356300597,
-1.70557797181458));
#68199=CARTESIAN_POINT('Ctrl Pts',(0.566852658497668,-0.132531935357976,
-1.69166834186883));
#68200=CARTESIAN_POINT('Ctrl Pts',(0.561090795286944,0.155125013392,-1.67775871192306));
#68201=CARTESIAN_POINT('Ctrl Pts',(0.418271486905671,0.404889631353191,
-1.66384908197731));
#68202=CARTESIAN_POINT('Ctrl Pts',(0.173281154040451,0.555752005835349,
-1.64993945203155));
#68203=CARTESIAN_POINT('Ctrl Pts',(-0.114036503508187,0.570861039310996,
-1.63602982208579));
#68204=CARTESIAN_POINT('Ctrl Pts',(-0.373498505682864,0.446526053650032,
-1.62212019214003));
#68205=CARTESIAN_POINT('Ctrl Pts',(-0.54172616326678,0.213118310728701,
-1.60821056219427));
#68206=CARTESIAN_POINT('Ctrl Pts',(-0.577626567324083,-0.0723477646994037,
-1.59430093224851));
#68207=CARTESIAN_POINT('Ctrl Pts',(-0.472430339169505,-0.340141477870296,
-1.58039130230275));
#68208=CARTESIAN_POINT('Ctrl Pts',(-0.251833723320963,-0.524848955542358,
-1.566481672357));
#68209=CARTESIAN_POINT('Ctrl Pts',(0.0302782248340165,-0.581351769100692,
-1.55257204241123));
#68210=CARTESIAN_POINT('Ctrl Pts',(0.30499412198458,-0.49584799675955,-1.53866241246548));
#68211=CARTESIAN_POINT('Ctrl Pts',(0.505209215517677,-0.289223613993771,
-1.52475278251972));
#68212=CARTESIAN_POINT('Ctrl Pts',(0.582017037113508,-0.0119506838806641,
-1.51084315257396));
#68213=CARTESIAN_POINT('Ctrl Pts',(0.516655768033535,0.268241435451875,
-1.4969335226282));
#68214=CARTESIAN_POINT('Ctrl Pts',(0.325091181782599,0.48291031658352,-1.48302389268244));
#68215=CARTESIAN_POINT('Ctrl Pts',(0.0541166904024802,0.579618869737247,
-1.46911426273668));
#68216=CARTESIAN_POINT('Ctrl Pts',(-0.23007686532507,0.534744131690842,
-1.45520463279092));
#68217=CARTESIAN_POINT('Ctrl Pts',(-0.458069628562033,0.359247638439899,
-1.44129500284516));
#68218=CARTESIAN_POINT('Ctrl Pts',(-0.574169889679393,0.0959978547737282,
-1.4273853728994));
#68219=CARTESIAN_POINT('Ctrl Pts',(-0.550017879980101,-0.190701290079009,
-1.41347574295365));
#68220=CARTESIAN_POINT('Ctrl Pts',(-0.391513202118355,-0.430817899932948,
-1.39956611300789));
#68221=CARTESIAN_POINT('Ctrl Pts',(-0.13737373629784,-0.565698777540818,
-1.38565648306213));
#68222=CARTESIAN_POINT('Ctrl Pts',(0.150321962290467,-0.562396619823365,
-1.37174685311637));
#68223=CARTESIAN_POINT('Ctrl Pts',(0.401298569641467,-0.42171804364921,
-1.35783722317061));
#68224=CARTESIAN_POINT('Ctrl Pts',(0.554250120856,-0.178026553824736,-1.34392759322485));
#68225=CARTESIAN_POINT('Ctrl Pts',(0.571815195963504,0.109151417768263,
-1.33001796327909));
#68226=CARTESIAN_POINT('Ctrl Pts',(0.449703180434771,0.369667012110162,
-1.31610833333333));
#68227=CARTESIAN_POINT('Ctrl Pts',(0.217742332037662,0.539884179407402,
-1.30219870338757));
#68228=CARTESIAN_POINT('Ctrl Pts',(-0.0674063568751685,0.578224033907638,
-1.28828907344181));
#68229=CARTESIAN_POINT('Ctrl Pts',(-0.336089719428759,0.475321313250208,
-1.27437944349606));
#68230=CARTESIAN_POINT('Ctrl Pts',(-0.522676568049277,0.256312027708089,
-1.2604698135503));
#68231=CARTESIAN_POINT('Ctrl Pts',(-0.581589400861518,-0.0253065039297315,
-1.24656018360454));
#68232=CARTESIAN_POINT('Ctrl Pts',(-0.498437601550204,-0.30074342502619,
-1.23265055365878));
#68233=CARTESIAN_POINT('Ctrl Pts',(-0.293532629990769,-0.502717858710337,
-1.21874092371302));
#68234=CARTESIAN_POINT('Ctrl Pts',(-0.0169265493084289,-0.581893583281438,
-1.20483129376726));
#68235=CARTESIAN_POINT('Ctrl Pts',(0.263814173437639,-0.518930373199543,
-1.1909216638215));
#68236=CARTESIAN_POINT('Ctrl Pts',(0.480113103670162,-0.329208228967331,
-1.17701203387574));
#68237=CARTESIAN_POINT('Ctrl Pts',(0.579134980109133,-0.0590705099825352,
-1.16310240392998));
#68238=CARTESIAN_POINT('Ctrl Pts',(0.536691764892018,0.225496341062766,
-1.14919277398422));
#68239=CARTESIAN_POINT('Ctrl Pts',(0.363151046814323,0.454981282618599,
-1.13528314403847));
#68240=CARTESIAN_POINT('Ctrl Pts',(0.100903554172759,0.573328111198909,
-1.1213735140927));
#68241=CARTESIAN_POINT('Ctrl Pts',(-0.185991613069268,0.551628289886855,
-1.10746388414695));
#68242=CARTESIAN_POINT('Ctrl Pts',(-0.427454676408419,0.395182426168191,
-1.09355425420119));
#68243=CARTESIAN_POINT('Ctrl Pts',(-0.564503540892674,0.142205494462193,
-1.07964462425543));
#68244=CARTESIAN_POINT('Ctrl Pts',(-0.56366133007438,-0.145507921826901,
-1.06573499430967));
#68245=CARTESIAN_POINT('Ctrl Pts',(-0.425133770484826,-0.397678170797639,
-1.05182536436391));
#68246=CARTESIAN_POINT('Ctrl Pts',(-0.182758938889015,-0.552707717145115,
-1.03791573441815));
#68247=CARTESIAN_POINT('Ctrl Pts',(0.104258352459501,-0.5727275497809,-1.02400610447239));
#68248=CARTESIAN_POINT('Ctrl Pts',(0.365808493846163,-0.452847431444196,
-1.01009647452664));
#68249=CARTESIAN_POINT('Ctrl Pts',(0.538002727045805,-0.222350435184824,
-0.996186844580877));
#68250=CARTESIAN_POINT('Ctrl Pts',(0.578779229134785,0.0624600212755955,
-0.982277214635117));
#68251=CARTESIAN_POINT('Ctrl Pts',(0.478177538729221,0.332013390980647,
-0.968367584689359));
#68252=CARTESIAN_POINT('Ctrl Pts',(0.260771594276588,0.520465970024985,
-0.954457954743599));
#68253=CARTESIAN_POINT('Ctrl Pts',(-0.0203329329808465,0.581784515239103,
-0.940548324797841));
#68254=CARTESIAN_POINT('Ctrl Pts',(-0.296470742069694,0.500990767811392,
-0.926638694852082));
#68255=CARTESIAN_POINT('Ctrl Pts',(-0.500189750463181,0.297820187138455,
-0.912729064906322));
#68256=CARTESIAN_POINT('Ctrl Pts',(-0.581727589828724,0.0219011773123757,
-0.898819434960564));
#68257=CARTESIAN_POINT('Ctrl Pts',(-0.521167041701788,-0.25936762515667,
-0.884909805014805));
#68258=CARTESIAN_POINT('Ctrl Pts',(-0.333301209220274,-0.477280791848893,
-0.871000175069045));
#68259=CARTESIAN_POINT('Ctrl Pts',(-0.0640200111834863,-0.578608752529436,
-0.857090545123287));
#68260=CARTESIAN_POINT('Ctrl Pts',(0.220899331777977,-0.538600162974025,
-0.843180915177526));
#68261=CARTESIAN_POINT('Ctrl Pts',(0.451859675041561,-0.367027906850336,
-0.82927128523177));
#68262=CARTESIAN_POINT('Ctrl Pts',(0.572444419280888,-0.105801876967134,
-0.815361655286009));
#68263=CARTESIAN_POINT('Ctrl Pts',(0.553198372732334,0.181268339049875,
-0.801452025340251));
#68264=CARTESIAN_POINT('Ctrl Pts',(0.398822760209661,0.424060203596552,
-0.787542395394492));
#68265=CARTESIAN_POINT('Ctrl Pts',(0.147026856622959,0.563267035931604,
-0.773632765448732));
#68266=CARTESIAN_POINT('Ctrl Pts',(-0.140683243934122,0.564884833582719,
-0.759723135502974));
#68267=CARTESIAN_POINT('Ctrl Pts',(-0.394028699492784,0.428518417704104,
-0.745813505557215));
#68268=CARTESIAN_POINT('Ctrl Pts',(-0.551124907460887,0.187477963269903,
-0.731903875611457));
#68269=CARTESIAN_POINT('Ctrl Pts',(-0.573598034065102,-0.0993576652918848,
-0.717994245665696));
#68270=CARTESIAN_POINT('Ctrl Pts',(-0.45595857681627,-0.361923232969764,
-0.704084615719939));
#68271=CARTESIAN_POINT('Ctrl Pts',(-0.226942283292515,-0.536081943726502,
-0.690174985774178));
#68272=CARTESIAN_POINT('Ctrl Pts',(0.0575091195050125,-0.579292112417698,
-0.67626535582842));
#68273=CARTESIAN_POINT('Ctrl Pts',(0.327912790527978,-0.480998806800763,
-0.66235572588266));
#68274=CARTESIAN_POINT('Ctrl Pts',(0.518217323076349,-0.265212097007629,
-0.648446095936903));
#68275=CARTESIAN_POINT('Ctrl Pts',(0.581937097969522,0.0153578755827512,
-0.634536465991143));
#68276=CARTESIAN_POINT('Ctrl Pts',(0.503507308892608,0.292176385471736,
-0.620626836045384));
#68277=CARTESIAN_POINT('Ctrl Pts',(0.302085971992796,0.497625075594841,
-0.606717206099625));
#68278=CARTESIAN_POINT('Ctrl Pts',(0.026874204219816,0.581519068890397,
-0.592807576153866));
#68279=CARTESIAN_POINT('Ctrl Pts',(-0.254902115676097,0.523365610027496,
-0.578897946208108));
#68280=CARTESIAN_POINT('Ctrl Pts',(-0.474413588177279,0.33736982332207,
-0.564988316262347));
#68281=CARTESIAN_POINT('Ctrl Pts',(-0.578040225468284,0.0689648321695848,
-0.551078686316589));
#68282=CARTESIAN_POINT('Ctrl Pts',(-0.540469186422474,-0.216286173537356,
-0.537169056370829));
#68283=CARTESIAN_POINT('Ctrl Pts',(-0.370877935128156,-0.448705034037593,
-0.523259426425072));
#68284=CARTESIAN_POINT('Ctrl Pts',(-0.110692465062534,-0.571518878528068,
-0.509349796479312));
#68285=CARTESIAN_POINT('Ctrl Pts',(0.176531813318142,-0.554728013734852,
-0.495440166533554));
#68286=CARTESIAN_POINT('Ctrl Pts',(0.420634729651996,-0.402433938114313,
-0.481530536587794));
#68287=CARTESIAN_POINT('Ctrl Pts',(0.561989353052933,-0.151837470312021,
-0.467620906642035));
#68288=CARTESIAN_POINT('Ctrl Pts',(0.566067040903533,0.135848281322644,
-0.453711276696276));
#68289=CARTESIAN_POINT('Ctrl Pts',(0.431871737870722,0.390350422523305,
-0.439801646750518));
#68290=CARTESIAN_POINT('Ctrl Pts',(0.192183281980758,0.549501807515437,
-0.425892016804758));
#68291=CARTESIAN_POINT('Ctrl Pts',(-0.0944497145325559,0.574426585178866,
-0.411982386859));
#68292=CARTESIAN_POINT('Ctrl Pts',(-0.358011513514948,0.459036389109272,
-0.398072756913241));
#68293=CARTESIAN_POINT('Ctrl Pts',(-0.534121969869188,0.231517540671202,
-0.384163126967482));
#68294=CARTESIAN_POINT('Ctrl Pts',(-0.579762646262023,-0.0525540135011436,
-0.370253497021723));
#68295=CARTESIAN_POINT('Ctrl Pts',(-0.48378491121418,-0.323788217847987,
-0.356343867075963));
#68296=CARTESIAN_POINT('Ctrl Pts',(-0.269633211276888,-0.515930791590299,
-0.342434237130205));
#68297=CARTESIAN_POINT('Ctrl Pts',(0.0103816954412071,-0.582047137901145,
-0.328524607184445));
#68298=CARTESIAN_POINT('Ctrl Pts',(0.287860669170086,-0.505987040814971,
-0.314614977238687));
#68299=CARTESIAN_POINT('Ctrl Pts',(0.495024021603582,-0.306329672713003,
-0.300705347292928));
#68300=CARTESIAN_POINT('Ctrl Pts',(0.581268035697884,-0.031845266452672,
-0.28679571734717));
#68301=CARTESIAN_POINT('Ctrl Pts',(0.525525917473871,0.250417971405241,
-0.272886087401411));
#68302=CARTESIAN_POINT('Ctrl Pts',(0.34141377378654,0.471511702349578,-0.258976457455652));
#68303=CARTESIAN_POINT('Ctrl Pts',(0.0739046115413053,0.577429440320225,
-0.245066827509892));
#68304=CARTESIAN_POINT('Ctrl Pts',(-0.211657203771934,0.542298698929604,
-0.231157197564133));
#68305=CARTESIAN_POINT('Ctrl Pts',(-0.445517589869098,0.37470084954831,
-0.217247567618374));
#68306=CARTESIAN_POINT('Ctrl Pts',(-0.570551557304549,0.115574962183174,
-0.203337937672615));
#68307=CARTESIAN_POINT('Ctrl Pts',(-0.556217099697408,-0.171782384589059,
-0.189428307726856));
#68308=CARTESIAN_POINT('Ctrl Pts',(-0.406015698566048,-0.417178500209998,
-0.175518677781097));
#68309=CARTESIAN_POINT('Ctrl Pts',(-0.156636978608061,-0.560670595014718,
-0.161609047835338));
#68310=CARTESIAN_POINT('Ctrl Pts',(0.131003377216481,-0.56720784733414,
-0.14769941788958));
#68311=CARTESIAN_POINT('Ctrl Pts',(0.386643628799531,-0.435193521555786,
-0.133789787943821));
#68312=CARTESIAN_POINT('Ctrl Pts',(0.547838496865826,-0.196874481237042,
-0.119880157998062));
#68313=CARTESIAN_POINT('Ctrl Pts',(0.575213218962054,0.0895347225743331,
-0.105970528052302));
#68314=CARTESIAN_POINT('Ctrl Pts',(0.462080493992123,0.354073888018237,
-0.0920608981065435));
#68315=CARTESIAN_POINT('Ctrl Pts',(0.236076164663117,0.532122427819931,
-0.0781512681607847));
#68316=CARTESIAN_POINT('Ctrl Pts',(-0.047595635797325,0.580191814324249,
-0.0642416382150254));
#68317=CARTESIAN_POINT('Ctrl Pts',(-0.319638859935216,0.486533658576269,
-0.0503320082692662));
#68318=CARTESIAN_POINT('Ctrl Pts',(-0.513608721405772,0.274038504320584,
-0.0364223783235072));
#68319=CARTESIAN_POINT('Ctrl Pts',(-0.582110362739213,-0.00541238131170235,
-0.0225127483777487));
#68320=CARTESIAN_POINT('Ctrl Pts',(-0.508438185945303,-0.283508771827898,
-0.00860311843199003));
#68321=CARTESIAN_POINT('Ctrl Pts',(-0.310533807033502,-0.492418870624804,
0.00530651151376876));
#68322=CARTESIAN_POINT('Ctrl Pts',(-0.128081630931447,-0.551395568835168,
0.0145795981442749));
#68323=CARTESIAN_POINT('Ctrl Pts',(-0.0353121949621431,-0.557273992116744,
0.0192161414595281));
#68324=CARTESIAN_POINT('Ctrl Pts',(0.305041111877683,-0.427420965560345,
-3.96754114145953));
#68325=CARTESIAN_POINT('Ctrl Pts',(0.376193906476754,-0.376640752780538,
-3.96290459814427));
#68326=CARTESIAN_POINT('Ctrl Pts',(0.49257674617948,-0.238910373259439,
-3.95363151151377));
#68327=CARTESIAN_POINT('Ctrl Pts',(0.546812900484255,0.0262129455514636,
-3.93972188156801));
#68328=CARTESIAN_POINT('Ctrl Pts',(0.467483302272917,0.28486232584599,-3.92581225162225));
#68329=CARTESIAN_POINT('Ctrl Pts',(0.27396005171883,0.473963347551388,-3.91190262167649));
#68330=CARTESIAN_POINT('Ctrl Pts',(0.0135174993871538,0.547271810816138,
-3.89799299173073));
#68331=CARTESIAN_POINT('Ctrl Pts',(-0.250227384164322,0.486907433624593,
-3.88408336178497));
#68332=CARTESIAN_POINT('Ctrl Pts',(-0.452849102465794,0.307601726185072,
-3.87017373183922));
#68333=CARTESIAN_POINT('Ctrl Pts',(-0.54485364354006,0.0531606246437338,
-3.85626410189345));
#68334=CARTESIAN_POINT('Ctrl Pts',(-0.503766926905405,-0.214267215150516,
-3.84235447194771));
#68335=CARTESIAN_POINT('Ctrl Pts',(-0.339625274156856,-0.429355459912895,
-3.82844484200193));
#68336=CARTESIAN_POINT('Ctrl Pts',(-0.0925234642162299,-0.539565519412296,
-3.81453521205618));
#68337=CARTESIAN_POINT('Ctrl Pts',(0.177179011324535,-0.517975942716222,
-3.80062558211042));
#68338=CARTESIAN_POINT('Ctrl Pts',(0.403602037815667,-0.369860653339095,
-3.78671595216466));
#68339=CARTESIAN_POINT('Ctrl Pts',(0.531437338879899,-0.131399593731153,
-3.7728063222189));
#68340=CARTESIAN_POINT('Ctrl Pts',(0.529458634820968,0.139158375250956,
-3.75889669227314));
#68341=CARTESIAN_POINT('Ctrl Pts',(0.398149261450136,0.375724189487086,
-3.74498706232739));
#68342=CARTESIAN_POINT('Ctrl Pts',(0.169584112575006,0.520511986460079,
-3.73107743238162));
#68343=CARTESIAN_POINT('Ctrl Pts',(-0.100405286138957,0.538154512099795,
-3.71716780243587));
#68344=CARTESIAN_POINT('Ctrl Pts',(-0.345868721935883,0.424342228657172,
-3.7032581724901));
#68345=CARTESIAN_POINT('Ctrl Pts',(-0.506846930437278,0.206876023606841,
-3.68934854254435));
#68346=CARTESIAN_POINT('Ctrl Pts',(-0.544017822953714,-0.0611237131283834,
-3.67543891259859));
#68347=CARTESIAN_POINT('Ctrl Pts',(-0.448301679071712,-0.314192782415098,
-3.66152928265283));
#68348=CARTESIAN_POINT('Ctrl Pts',(-0.243079046546545,-0.490514094737742,
-3.64761965270707));
#68349=CARTESIAN_POINT('Ctrl Pts',(0.0215204165605152,-0.547017706896761,
-3.63371002276131));
#68350=CARTESIAN_POINT('Ctrl Pts',(0.280863095316674,-0.469901502111615,
-3.61980039281555));
#68351=CARTESIAN_POINT('Ctrl Pts',(0.47159944759146,-0.278002627730234,
-3.6058907628698));
#68352=CARTESIAN_POINT('Ctrl Pts',(0.547138373757176,-0.0181961522555487,
-3.59198113292403));
#68353=CARTESIAN_POINT('Ctrl Pts',(0.489028007701532,0.246055090738122,
-3.57807150297828));
#68354=CARTESIAN_POINT('Ctrl Pts',(0.311462947476309,0.45020254590979,-3.56416187303252));
#68355=CARTESIAN_POINT('Ctrl Pts',(0.0578169459756449,0.544379188390458,
-3.55025224308676));
#68356=CARTESIAN_POINT('Ctrl Pts',(-0.209951979959951,0.505580523858779,
-3.536342613141));
#68357=CARTESIAN_POINT('Ctrl Pts',(-0.426436011857877,0.343283888036202,
-3.52243298319524));
#68358=CARTESIAN_POINT('Ctrl Pts',(-0.538754673721399,0.0971334213225582,
-3.50852335324948));
#68359=CARTESIAN_POINT('Ctrl Pts',(-0.519471926732396,-0.172743791006827,
-3.49461372330373));
#68360=CARTESIAN_POINT('Ctrl Pts',(-0.373297960507913,-0.400424940126257,
-3.48070409335796));
#68361=CARTESIAN_POINT('Ctrl Pts',(-0.135938636789861,-0.5302944342742,
-3.46679446341221));
#68362=CARTESIAN_POINT('Ctrl Pts',(0.134626368459391,-0.53062909919257,
-3.45288483346644));
#68363=CARTESIAN_POINT('Ctrl Pts',(0.372306239486833,-0.401347186403061,
-3.43897520352069));
#68364=CARTESIAN_POINT('Ctrl Pts',(0.519043000355028,-0.174028341878362,
-3.42506557357493));
#68365=CARTESIAN_POINT('Ctrl Pts',(0.538993315678459,0.0958003426320719,
-3.41115594362917));
#68366=CARTESIAN_POINT('Ctrl Pts',(0.427283929165017,0.342227912175184,
-3.39724631368341));
#68367=CARTESIAN_POINT('Ctrl Pts',(0.211202052163931,0.505059593668139,
-3.38333668373765));
#68368=CARTESIAN_POINT('Ctrl Pts',(-0.0564700735589543,0.544520551298779,
-3.36942705379189));
#68369=CARTESIAN_POINT('Ctrl Pts',(-0.310348274883871,0.450971671251184,
-3.35551742384613));
#68370=CARTESIAN_POINT('Ctrl Pts',(-0.48841781560348,0.247264104543312,
-3.34160779390037));
#68371=CARTESIAN_POINT('Ctrl Pts',(-0.547181713556024,-0.0168425753486551,
-3.32769816395462));
#68372=CARTESIAN_POINT('Ctrl Pts',(-0.472285732690417,-0.276835125465604,
-3.31378853400885));
#68373=CARTESIAN_POINT('Ctrl Pts',(-0.282024687103075,-0.469205259837199,
-3.2998789040631));
#68374=CARTESIAN_POINT('Ctrl Pts',(-0.0228735734304004,-0.546962795474249,
-3.28596927411734));
#68375=CARTESIAN_POINT('Ctrl Pts',(0.241864859732498,-0.491113927333628,
-3.27205964417158));
#68376=CARTESIAN_POINT('Ctrl Pts',(0.447523051284027,-0.315300838190951,
-3.25815001422582));
#68377=CARTESIAN_POINT('Ctrl Pts',(0.543864949324536,-0.0624693275992378,
-3.24424038428006));
#68378=CARTESIAN_POINT('Ctrl Pts',(0.507357153343402,0.205621543000143,
-3.2303307543343));
#68379=CARTESIAN_POINT('Ctrl Pts',(0.346917409430942,0.423485313828243,
-3.21642112438854));
#68380=CARTESIAN_POINT('Ctrl Pts',(0.10173627567359,0.537904480560023,-3.20251149444279));
#68381=CARTESIAN_POINT('Ctrl Pts',(-0.168295941263372,0.52092991481461,
-3.18860186449702));
#68382=CARTESIAN_POINT('Ctrl Pts',(-0.397218569634841,0.376707987613393,
-3.17469223455126));
#68383=CARTESIAN_POINT('Ctrl Pts',(-0.529112761992475,0.140467736833678,
-3.16078260460551));
#68384=CARTESIAN_POINT('Ctrl Pts',(-0.531760771780433,-0.130084517103148,
-3.14687297465975));
#68385=CARTESIAN_POINT('Ctrl Pts',(-0.404515770607708,-0.368861073202545,
-3.13296334471399));
#68386=CARTESIAN_POINT('Ctrl Pts',(-0.178459848784724,-0.517536068662093,
-3.11905371476823));
#68387=CARTESIAN_POINT('Ctrl Pts',(0.0911883956095983,-0.539792716235249,
-3.10514408482247));
#68388=CARTESIAN_POINT('Ctrl Pts',(0.338562083663956,-0.430194392687307,
-3.09123445487671));
#68389=CARTESIAN_POINT('Ctrl Pts',(0.50323533426974,-0.215512640782169,
-3.07732482493095));
#68390=CARTESIAN_POINT('Ctrl Pts',(0.544983472195168,0.051812305763967,
-3.0634151949852));
#68391=CARTESIAN_POINT('Ctrl Pts',(0.453608694922806,0.306481079162989,
-3.04950556503943));
#68392=CARTESIAN_POINT('Ctrl Pts',(0.251431086173814,0.486285830453589,
-3.03559593509368));
#68393=CARTESIAN_POINT('Ctrl Pts',(-0.0121635028516318,0.547305718216847,
-3.02168630514792));
#68394=CARTESIAN_POINT('Ctrl Pts',(-0.272786917444753,0.47463543658841,
-3.00777667520216));
#68395=CARTESIAN_POINT('Ctrl Pts',(-0.46677677059831,0.286026128918834,
-2.9938670452564));
#68396=CARTESIAN_POINT('Ctrl Pts',(-0.546747231203381,0.0275493224221043,
-2.97995741531064));
#68397=CARTESIAN_POINT('Ctrl Pts',(-0.493163943837085,-0.237656947076102,
-2.96604778536488));
#68398=CARTESIAN_POINT('Ctrl Pts',(-0.319115678680562,-0.444810840262156,
-2.95213815541912));
#68399=CARTESIAN_POINT('Ctrl Pts',(-0.0671171423714758,-0.543310950740336,
-2.93822852547336));
#68400=CARTESIAN_POINT('Ctrl Pts',(0.201276073974873,-0.509096692230211,
-2.9243188955276));
#68401=CARTESIAN_POINT('Ctrl Pts',(0.420503656693519,-0.350525569255455,
-2.91040926558185));
#68402=CARTESIAN_POINT('Ctrl Pts',(0.537014963623297,-0.106331692543425,
-2.89649963563608));
#68403=CARTESIAN_POINT('Ctrl Pts',(0.522349820055569,0.163835788161179,
-2.88259000569033));
#68404=CARTESIAN_POINT('Ctrl Pts',(0.380090475293543,0.393983160281768,
-2.86868037574457));
#68405=CARTESIAN_POINT('Ctrl Pts',(0.144986567913532,0.527892408658371,
-2.85477074579881));
#68406=CARTESIAN_POINT('Ctrl Pts',(-0.125533155853402,0.532853569731841,
-2.84086111585305));
#68407=CARTESIAN_POINT('Ctrl Pts',(-0.36538894114552,0.407654782485176,
-2.82695148590729));
#68408=CARTESIAN_POINT('Ctrl Pts',(-0.515991302236719,0.182878309294829,
-2.81304185596153));
#68409=CARTESIAN_POINT('Ctrl Pts',(-0.540552654976281,-0.0865697822139766,
-2.79913222601577));
#68410=CARTESIAN_POINT('Ctrl Pts',(-0.433073406633946,-0.334871504402733,
-2.78522259607001));
#68411=CARTESIAN_POINT('Ctrl Pts',(-0.219807474241307,-0.501374285601225,
-2.77131296612426));
#68412=CARTESIAN_POINT('Ctrl Pts',(0.0471507502045272,-0.545406551802993,
-2.7574033361785));
#68413=CARTESIAN_POINT('Ctrl Pts',(0.302591477989944,-0.456212557304533,
-2.74349370623274));
#68414=CARTESIAN_POINT('Ctrl Pts',(0.484118295135511,-0.255579686809354,
-2.72958407628698));
#68415=CARTESIAN_POINT('Ctrl Pts',(0.547389711820154,0.00748354113566584,
-2.71567444634122));
#68416=CARTESIAN_POINT('Ctrl Pts',(0.476950442026069,0.268718767200243,
-2.70176481639546));
#68417=CARTESIAN_POINT('Ctrl Pts',(0.290006660651773,0.464314157410786,
-2.6878551864497));
#68418=CARTESIAN_POINT('Ctrl Pts',(0.032223057406854,0.546491696703467,
-2.67394555650394));
#68419=CARTESIAN_POINT('Ctrl Pts',(-0.233431660390051,0.495177907344447,
-2.66003592655819));
#68420=CARTESIAN_POINT('Ctrl Pts',(-0.442066111121947,0.32290719005931,
-2.64612629661242));
#68421=CARTESIAN_POINT('Ctrl Pts',(-0.542717233138088,0.071760050511542,
-2.63221666666667));
#68422=CARTESIAN_POINT('Ctrl Pts',(-0.510799013349406,-0.196915890561819,
-2.61830703672091));
#68423=CARTESIAN_POINT('Ctrl Pts',(-0.354108103733396,-0.417491258429227,
-2.60439740677515));
#68424=CARTESIAN_POINT('Ctrl Pts',(-0.110919335981845,-0.536086187939802,
-2.59048777682939));
#68425=CARTESIAN_POINT('Ctrl Pts',(0.159363657761974,-0.523731538652395,
-2.57657814688363));
#68426=CARTESIAN_POINT('Ctrl Pts',(0.390718948593253,-0.383445176269912,
-2.56266851693787));
#68427=CARTESIAN_POINT('Ctrl Pts',(0.526633463486426,-0.14949479967802,
-2.54875888699211));
#68428=CARTESIAN_POINT('Ctrl Pts',(0.533907413157257,0.120972617439681,
-2.53484925704635));
#68429=CARTESIAN_POINT('Ctrl Pts',(0.41076399255644,0.361890097147703,-2.52093962710059));
#68430=CARTESIAN_POINT('Ctrl Pts',(0.187283400394916,0.514408814009829,
-2.50702999715484));
#68431=CARTESIAN_POINT('Ctrl Pts',(-0.0819448400912485,0.541273076345849,
-2.49312036720907));
#68432=CARTESIAN_POINT('Ctrl Pts',(-0.33115644419315,0.435920760533185,
-2.47921073726332));
#68433=CARTESIAN_POINT('Ctrl Pts',(-0.499476583715483,0.224086238565404,
-2.46530110731756));
#68434=CARTESIAN_POINT('Ctrl Pts',(-0.545789759192809,-0.0424857476659746,
-2.4513914773718));
#68435=CARTESIAN_POINT('Ctrl Pts',(-0.458783068039706,-0.298679755715977,
-2.43748184742604));
#68436=CARTESIAN_POINT('Ctrl Pts',(-0.259709603164407,-0.481915368107998,
-2.42357221748028));
#68437=CARTESIAN_POINT('Ctrl Pts',(0.00280303233169327,-0.54743368822555,
-2.40966258753452));
#68438=CARTESIAN_POINT('Ctrl Pts',(0.264630972136224,-0.479230579763768,
-2.39575295758876));
#68439=CARTESIAN_POINT('Ctrl Pts',(0.461817600305192,-0.293965991303136,
-2.381843327643));
#68440=CARTESIAN_POINT('Ctrl Pts',(0.546196210655486,-0.0368944367089179,
-2.36793369769724));
#68441=CARTESIAN_POINT('Ctrl Pts',(0.497155670623904,0.229189308566033,
-2.35402406775149));
#68442=CARTESIAN_POINT('Ctrl Pts',(0.326675095146872,0.439289064518186,
-2.34011443780572));
#68443=CARTESIAN_POINT('Ctrl Pts',(0.0763977125973221,0.542083839921813,
-2.32620480785997));
#68444=CARTESIAN_POINT('Ctrl Pts',(-0.192541311514372,0.51246399225195,
-2.31229517791421));
#68445=CARTESIAN_POINT('Ctrl Pts',(-0.414448339258253,0.357664750961786,
-2.29838554796845));
#68446=CARTESIAN_POINT('Ctrl Pts',(-0.535118221408144,0.115498870606881,
-2.28447591802269));
#68447=CARTESIAN_POINT('Ctrl Pts',(-0.52507496959386,-0.154879877003077,
-2.27056628807693));
#68448=CARTESIAN_POINT('Ctrl Pts',(-0.386771845295417,-0.387426173201114,
-2.25665665813117));
#68449=CARTESIAN_POINT('Ctrl Pts',(-0.153992102550614,-0.525336018512459,
-2.24274702818542));
#68450=CARTESIAN_POINT('Ctrl Pts',(0.116403235262424,-0.534922225014928,
-2.22883739823965));
#68451=CARTESIAN_POINT('Ctrl Pts',(0.358364796993828,-0.413843173521145,
-2.2149277682939));
#68452=CARTESIAN_POINT('Ctrl Pts',(0.512788719670011,-0.191674800048603,
-2.20101813834814));
#68453=CARTESIAN_POINT('Ctrl Pts',(0.541953927677195,0.0773139073501151,
-2.18710850840238));
#68454=CARTESIAN_POINT('Ctrl Pts',(0.43873624622779,0.327417174626545,-2.17319887845662));
#68455=CARTESIAN_POINT('Ctrl Pts',(0.228348620953256,0.49754236734496,-2.15928924851086));
#68456=CARTESIAN_POINT('Ctrl Pts',(-0.0378176391856524,0.546133066350047,
-2.1453796185651));
#68457=CARTESIAN_POINT('Ctrl Pts',(-0.294746198309491,0.461320039209855,
-2.13146998861934));
#68458=CARTESIAN_POINT('Ctrl Pts',(-0.479677210417124,0.263820533319387,
-2.11756035867358));
#68459=CARTESIAN_POINT('Ctrl Pts',(-0.547437644218116,0.00187768138936353,
-2.10365072872783));
#68460=CARTESIAN_POINT('Ctrl Pts',(-0.481475683110906,-0.260523831092987,
-2.08974109878207));
#68461=CARTESIAN_POINT('Ctrl Pts',(-0.297903831424081,-0.459287281793578,
-2.07583146883631));
#68462=CARTESIAN_POINT('Ctrl Pts',(-0.0415631188247858,-0.545860794661091,
-2.06192183889055));
#68463=CARTESIAN_POINT('Ctrl Pts',(0.2249302017433,-0.499097089090089,-2.04801220894479));
#68464=CARTESIAN_POINT('Ctrl Pts',(0.436479903468258,-0.330419118488657,
-2.03410257899903));
#68465=CARTESIAN_POINT('Ctrl Pts',(0.541410817396038,-0.0810297895902128,
-2.02019294905327));
#68466=CARTESIAN_POINT('Ctrl Pts',(0.514091507218732,0.188152656638311,
-2.00628331910751));
#68467=CARTESIAN_POINT('Ctrl Pts',(0.361195250930158,0.41137512163472,-1.99237368916175));
#68468=CARTESIAN_POINT('Ctrl Pts',(0.120069961629371,0.534111134792003,
-1.97846405921599));
#68469=CARTESIAN_POINT('Ctrl Pts',(-0.150384773673522,0.526380014667772,
-1.96455442927023));
#68470=CARTESIAN_POINT('Ctrl Pts',(-0.38410507482534,0.390070239172256,
-1.95064479932448));
#68471=CARTESIAN_POINT('Ctrl Pts',(-0.524000168586827,0.158478147753744,
-1.93673516937872));
#68472=CARTESIAN_POINT('Ctrl Pts',(-0.535897931116531,-0.111825343368592,
-1.92282553943296));
#68473=CARTESIAN_POINT('Ctrl Pts',(-0.416892100274231,-0.354813298402725,
-1.9089159094872));
#68474=CARTESIAN_POINT('Ctrl Pts',(-0.196052187220425,-0.511131137655072,
-1.89500627954144));
#68475=CARTESIAN_POINT('Ctrl Pts',(0.0726773225372251,-0.54259515919634,
-1.88109664959568));
#68476=CARTESIAN_POINT('Ctrl Pts',(0.323653969064078,-0.44151965789028,
-1.86718701964992));
#68477=CARTESIAN_POINT('Ctrl Pts',(0.495571777891505,-0.232594309801278,
-1.85327738970416));
#68478=CARTESIAN_POINT('Ctrl Pts',(0.546436448177067,0.0331467660279462,
-1.8393677597584));
#68479=CARTESIAN_POINT('Ctrl Pts',(0.463823285348445,0.290791093335156,
-1.82545812981264));
#68480=CARTESIAN_POINT('Ctrl Pts',(0.267912176742691,0.477403985684529,
-1.81154849986689));
#68481=CARTESIAN_POINT('Ctrl Pts',(0.00655825784157817,0.54740157950865,
-1.79763886992113));
#68482=CARTESIAN_POINT('Ctrl Pts',(-0.256397644325143,0.483685587938072,
-1.78372923997537));
#68483=CARTESIAN_POINT('Ctrl Pts',(-0.456723386856148,0.301819893136834,
-1.76981961002961));
#68484=CARTESIAN_POINT('Ctrl Pts',(-0.545485473241036,0.0462287624481154,
-1.75590998008385));
#68485=CARTESIAN_POINT('Ctrl Pts',(-0.501002020814631,-0.220654651285976,
-1.74200035013809));
#68486=CARTESIAN_POINT('Ctrl Pts',(-0.334138986375984,-0.433638833337272,
-1.72809072019233));
#68487=CARTESIAN_POINT('Ctrl Pts',(-0.085655942859932,-0.540698214762409,
-1.71418109024657));
#68488=CARTESIAN_POINT('Ctrl Pts',(0.183750246768424,-0.515681439269462,
-1.70027146030081));
#68489=CARTESIAN_POINT('Ctrl Pts',(0.408271830227724,-0.364699345539563,
-1.68636183035505));
#68490=CARTESIAN_POINT('Ctrl Pts',(0.533065001714948,-0.124632274877432,
-1.6724522004093));
#68491=CARTESIAN_POINT('Ctrl Pts',(0.527646578468163,0.145878676390081,
-1.65854257046354));
#68492=CARTESIAN_POINT('Ctrl Pts',(0.393340116769695,0.380755896256491,
-1.64463294051778));
#68493=CARTESIAN_POINT('Ctrl Pts',(0.16295260733283,0.522626011367511,-1.63072331057202));
#68494=CARTESIAN_POINT('Ctrl Pts',(-0.107239276427261,0.53683446013258,
-1.61681368062626));
#68495=CARTESIAN_POINT('Ctrl Pts',(-0.351235861008467,0.419910549922387,
-1.6029040506805));
#68496=CARTESIAN_POINT('Ctrl Pts',(-0.509436189143367,0.200415241899318,
-1.58899442073474));
#68497=CARTESIAN_POINT('Ctrl Pts',(-0.543196724025735,-0.0680354246124073,
-1.57508479078898));
#68498=CARTESIAN_POINT('Ctrl Pts',(-0.444270792037967,-0.319867102616756,
-1.56117516084323));
#68499=CARTESIAN_POINT('Ctrl Pts',(-0.236822994726279,-0.49356495941604,
-1.54726553089746));
#68500=CARTESIAN_POINT('Ctrl Pts',(0.0284734696593775,-0.546699882494992,
-1.53335590095171));
#68501=CARTESIAN_POINT('Ctrl Pts',(0.286814729932908,-0.466292623454408,
-1.51944627100595));
#68502=CARTESIAN_POINT('Ctrl Pts',(0.475095860095443,-0.271984234312676,
-1.50553664106019));
#68503=CARTESIAN_POINT('Ctrl Pts',(0.547325496733678,-0.0112383548490794,
-1.49162701111443));
#68504=CARTESIAN_POINT('Ctrl Pts',(0.485860132689079,0.252252713479623,
-1.47771738116867));
#68505=CARTESIAN_POINT('Ctrl Pts',(0.305713890155758,0.454126102927714,
-1.46380775122291));
#68506=CARTESIAN_POINT('Ctrl Pts',(0.0508910264947163,0.545070273833379,
-1.44989812127715));
#68507=CARTESIAN_POINT('Ctrl Pts',(-0.216362969760304,0.502870326536555,
-1.43598849133139));
#68508=CARTESIAN_POINT('Ctrl Pts',(-0.430766061823084,0.337834426866049,
-1.42207886138564));
#68509=CARTESIAN_POINT('Ctrl Pts',(-0.539946084116101,0.0902758342092153,
-1.40816923143988));
#68510=CARTESIAN_POINT('Ctrl Pts',(-0.517233672171357,-0.179334403745111,
-1.39425960149412));
#68511=CARTESIAN_POINT('Ctrl Pts',(-0.368176778621395,-0.405138691904949,
-1.38034997154836));
#68512=CARTESIAN_POINT('Ctrl Pts',(-0.129185476820866,-0.531979898655059,
-1.3664403416026));
#68513=CARTESIAN_POINT('Ctrl Pts',(0.141361914573243,-0.528874568402252,
-1.35253071165684));
#68514=CARTESIAN_POINT('Ctrl Pts',(0.377378882337932,-0.396581239041707,
-1.33862108171108));
#68515=CARTESIAN_POINT('Ctrl Pts',(0.521213647312955,-0.16741515418028,
-1.32471145176532));
#68516=CARTESIAN_POINT('Ctrl Pts',(0.537731743597658,0.102645369705129,
-1.31080182181956));
#68517=CARTESIAN_POINT('Ctrl Pts',(0.422898301800352,0.347632746341392,
-1.29689219187381));
#68518=CARTESIAN_POINT('Ctrl Pts',(0.204763645121989,0.50770399804496,-1.28298256192804));
#68519=CARTESIAN_POINT('Ctrl Pts',(-0.0633885529239486,0.543758578187681,
-1.26907293198229));
#68520=CARTESIAN_POINT('Ctrl Pts',(-0.316056852125366,0.446989447547798,
-1.25516330203653));
#68521=CARTESIAN_POINT('Ctrl Pts',(-0.491522058628041,0.241034366588115,
-1.24125367209077));
#68522=CARTESIAN_POINT('Ctrl Pts',(-0.54692335004532,-0.0237980917236146,
-1.22734404214501));
#68523=CARTESIAN_POINT('Ctrl Pts',(-0.468727873005551,-0.282817398796772,
-1.21343441219925));
#68524=CARTESIAN_POINT('Ctrl Pts',(-0.276036408339551,-0.472753002386535,
-1.19952478225349));
#68525=CARTESIAN_POINT('Ctrl Pts',(-0.0159176302710459,-0.547209401455269,
-1.18561515230773));
#68526=CARTESIAN_POINT('Ctrl Pts',(0.248089341573656,-0.487999158392747,
-1.17170552236197));
#68527=CARTESIAN_POINT('Ctrl Pts',(0.451495619884012,-0.309585537808265,
-1.15779589241622));
#68528=CARTESIAN_POINT('Ctrl Pts',(0.544615226791482,-0.0555495701274412,
-1.14388626247046));
#68529=CARTESIAN_POINT('Ctrl Pts',(0.504701869672432,0.212055470911817,
-1.1299766325247));
#68530=CARTESIAN_POINT('Ctrl Pts',(0.341505169801825,0.427861798941093,
-1.11606700257894));
#68531=CARTESIAN_POINT('Ctrl Pts',(0.0948891258986073,0.539154480441997,
-1.10215737263318));
#68532=CARTESIAN_POINT('Ctrl Pts',(-0.174905450390763,0.51874809244766,
-1.08824774268742));
#68533=CARTESIAN_POINT('Ctrl Pts',(-0.401975935716025,0.371627295956186,
-1.07433811274166));
#68534=CARTESIAN_POINT('Ctrl Pts',(-0.530855904939337,0.133729234595581,
-1.0604284827959));
#68535=CARTESIAN_POINT('Ctrl Pts',(-0.530063894697224,-0.136834818423128,
-1.04651885285014));
#68536=CARTESIAN_POINT('Ctrl Pts',(-0.399793369044433,-0.373974279947941,
-1.03260922290438));
#68537=CARTESIAN_POINT('Ctrl Pts',(-0.171865462059389,-0.519763179674737,
-1.01869959295862));
#68538=CARTESIAN_POINT('Ctrl Pts',(0.0980439590420491,-0.53858971591541,
-1.00478996301287));
#68539=CARTESIAN_POINT('Ctrl Pts',(0.344004217809009,-0.425855137487025,
-0.990880333067106));
#68540=CARTESIAN_POINT('Ctrl Pts',(0.505934690992543,-0.209097078996244,
-0.976970703121349));
#68541=CARTESIAN_POINT('Ctrl Pts',(0.544280680607551,0.058737047183714,
-0.963061073175588));
#68542=CARTESIAN_POINT('Ctrl Pts',(0.449675425671115,0.312223496140158,
-0.949151443229832));
#68543=CARTESIAN_POINT('Ctrl Pts',(0.245228117512358,0.48944322487478,-0.93524181328407));
#68544=CARTESIAN_POINT('Ctrl Pts',(-0.0191209740164775,0.547106834491346,
-0.921332183338313));
#68545=CARTESIAN_POINT('Ctrl Pts',(-0.278799392153621,0.471128855971752,
-0.907422553392553));
#68546=CARTESIAN_POINT('Ctrl Pts',(-0.470375583833576,0.280068402587124,
-0.893512923446795));
#68547=CARTESIAN_POINT('Ctrl Pts',(-0.54705330216063,0.0205957420267234,
-0.879603293501035));
#68548=CARTESIAN_POINT('Ctrl Pts',(-0.490102508674538,-0.243907832972633,
-0.865693663555277));
#68549=CARTESIAN_POINT('Ctrl Pts',(-0.313434553055607,-0.448832130027823,
-0.851784033609516));
#68550=CARTESIAN_POINT('Ctrl Pts',(-0.0602040527811273,-0.544120365381786,
-0.83787440366376));
#68551=CARTESIAN_POINT('Ctrl Pts',(0.207732469642362,-0.506496516326388,
-0.823964773717998));
#68552=CARTESIAN_POINT('Ctrl Pts',(0.424926257008878,-0.345150946831826,
-0.810055143772242));
#68553=CARTESIAN_POINT('Ctrl Pts',(0.538323461610678,-0.0994954806711237,
-0.79614551382648));
#68554=CARTESIAN_POINT('Ctrl Pts',(0.520224589385922,0.170463710486215,
-0.782235883880723));
#68555=CARTESIAN_POINT('Ctrl Pts',(0.375050645292154,0.398783792875813,
-0.768326253934963));
#68556=CARTESIAN_POINT('Ctrl Pts',(0.138263216027914,0.529693102737896,
-0.754416623989205));
#68557=CARTESIAN_POINT('Ctrl Pts',(-0.132297718895352,0.531214470406791,
-0.740506994043446));
#68558=CARTESIAN_POINT('Ctrl Pts',(-0.370542337981686,0.402976271953508,
-0.726597364097687));
#68559=CARTESIAN_POINT('Ctrl Pts',(-0.518274714490022,0.176303205628164,
-0.712687734151928));
#68560=CARTESIAN_POINT('Ctrl Pts',(-0.539408314363338,-0.0934353808264442,
-0.698778104206169));
#68561=CARTESIAN_POINT('Ctrl Pts',(-0.428780840821461,-0.340350540676703,
-0.68486847426041));
#68562=CARTESIAN_POINT('Ctrl Pts',(-0.213415226724241,-0.50412839733219,
-0.670958844314651));
#68563=CARTESIAN_POINT('Ctrl Pts',(0.0540812474423478,-0.544762993116785,
-0.657049214368891));
#68564=CARTESIAN_POINT('Ctrl Pts',(0.308367314900525,-0.45232853004815,
-0.643139584423134));
#68565=CARTESIAN_POINT('Ctrl Pts',(0.487328610130435,-0.249403940912765,
-0.629229954477374));
#68566=CARTESIAN_POINT('Ctrl Pts',(0.547250322419351,0.0144424584609956,
-0.615320324531616));
#68567=CARTESIAN_POINT('Ctrl Pts',(0.473495396827942,0.274761003741857,
-0.601410694585855));
#68568=CARTESIAN_POINT('Ctrl Pts',(0.284079922294417,0.467963778238956,
-0.587501064640098));
#68569=CARTESIAN_POINT('Ctrl Pts',(0.0252723481203937,0.546857210261474,
-0.573591434694337));
#68570=CARTESIAN_POINT('Ctrl Pts',(-0.239708493367827,0.492170029767972,
-0.55968180474858));
#68571=CARTESIAN_POINT('Ctrl Pts',(-0.446135828074901,0.317260654513612,
-0.545772174802819));
#68572=CARTESIAN_POINT('Ctrl Pts',(-0.543585725781381,0.0648541341875027,
-0.531862544857062));
#68573=CARTESIAN_POINT('Ctrl Pts',(-0.508254135299884,-0.203394281987098,
-0.517952914911301));
#68574=CARTESIAN_POINT('Ctrl Pts',(-0.348771491429709,-0.421959650630693,
-0.504043284965544));
#68575=CARTESIAN_POINT('Ctrl Pts',(-0.10409456177691,-0.537453088374187,
-0.490133655019784));
#68576=CARTESIAN_POINT('Ctrl Pts',(0.166009508747088,-0.521663055046103,
-0.476224025074026));
#68577=CARTESIAN_POINT('Ctrl Pts',(0.395562496747523,-0.378446576363621,
-0.462314395128266));
#68578=CARTESIAN_POINT('Ctrl Pts',(0.528491577057985,-0.142787089658862,
-0.448404765182507));
#68579=CARTESIAN_POINT('Ctrl Pts',(0.532326211417529,0.127750947676867,
-0.434495135236748));
#68580=CARTESIAN_POINT('Ctrl Pts',(0.406129715081226,0.367083307332981,
-0.42058550529099));
#68581=CARTESIAN_POINT('Ctrl Pts',(0.180728060463137,0.516748360573824,
-0.40667587534523));
#68582=CARTESIAN_POINT('Ctrl Pts',(-0.0888199719706895,0.540187479097346,
-0.392766245399471));
#68583=CARTESIAN_POINT('Ctrl Pts',(-0.336671982048404,0.431675197918763,
-0.378856615453713));
#68584=CARTESIAN_POINT('Ctrl Pts',(-0.502285249113782,0.217717772625464,
-0.364946985507953));
#68585=CARTESIAN_POINT('Ctrl Pts',(-0.545205480455905,-0.0494214940640173,
-0.351037355562195));
#68586=CARTESIAN_POINT('Ctrl Pts',(-0.454948566721971,-0.304488590315269,
-0.337127725616434));
#68587=CARTESIAN_POINT('Ctrl Pts',(-0.253561531514476,-0.485178368983532,
-0.323218095670677));
#68588=CARTESIAN_POINT('Ctrl Pts',(0.00976288708398863,-0.547353803342409,
-0.309308465724917));
#68589=CARTESIAN_POINT('Ctrl Pts',(0.270702528786763,-0.47582732256143,
-0.295398835779159));
#68590=CARTESIAN_POINT('Ctrl Pts',(0.465517761924972,-0.288070674208134,
-0.2814892058334));
#68591=CARTESIAN_POINT('Ctrl Pts',(0.546621140081346,-0.0299471066453085,
-0.267579575887642));
#68592=CARTESIAN_POINT('Ctrl Pts',(0.494201570549062,0.235491629712694,
-0.253669945941882));
#68593=CARTESIAN_POINT('Ctrl Pts',(0.321063562427973,0.443406911220529,
-0.239760315996123));
#68594=CARTESIAN_POINT('Ctrl Pts',(0.0694994744885192,0.543011346917461,
-0.225850686050364));
#68595=CARTESIAN_POINT('Ctrl Pts',(-0.199041225264239,0.509974598409885,
-0.211941056104605));
#68596=CARTESIAN_POINT('Ctrl Pts',(-0.418962196343987,0.352366538310738,
-0.198031426158846));
#68597=CARTESIAN_POINT('Ctrl Pts',(-0.536543425021737,0.108686034176255,
-0.184121796213087));
#68598=CARTESIAN_POINT('Ctrl Pts',(-0.523063382978388,-0.161543173102966,
-0.170212166267328));
#68599=CARTESIAN_POINT('Ctrl Pts',(-0.381814843430422,-0.392312278325139,
-0.156302536321569));
#68600=CARTESIAN_POINT('Ctrl Pts',(-0.147300519841655,-0.527251424532697,
-0.14239290637581));
#68601=CARTESIAN_POINT('Ctrl Pts',(0.123194827533574,-0.53339901926763,
-0.128483276430052));
#68602=CARTESIAN_POINT('Ctrl Pts',(0.363597459691447,-0.409253501481856,
-0.114573646484293));
#68603=CARTESIAN_POINT('Ctrl Pts',(0.515184192741152,-0.185139637443695,
-0.100664016538534));
#68604=CARTESIAN_POINT('Ctrl Pts',(0.540927225013145,0.0841979416117195,
-0.0867543865927742));
#68605=CARTESIAN_POINT('Ctrl Pts',(0.434537856760124,0.332969061526306,
-0.0728447566470156));
#68606=CARTESIAN_POINT('Ctrl Pts',(0.222004676584789,0.500404891193716,
-0.0589351267012565));
#68607=CARTESIAN_POINT('Ctrl Pts',(-0.0447586639977449,0.545609067649857,
-0.0450254967554974));
#68608=CARTESIAN_POINT('Ctrl Pts',(-0.3005865578387,0.457533473038136,-0.0311158668097381));
#68609=CARTESIAN_POINT('Ctrl Pts',(-0.48299470744761,0.257704243926052,
-0.0172062368639793));
#68610=CARTESIAN_POINT('Ctrl Pts',(-0.547413259618935,-0.00508977246547882,
-0.00329660691822061));
#68611=CARTESIAN_POINT('Ctrl Pts',(-0.478132365439005,-0.266610029387846,
0.010613023027538));
#68612=CARTESIAN_POINT('Ctrl Pts',(-0.292024218105601,-0.463067892827328,
0.0245226529732968));
#68613=CARTESIAN_POINT('Ctrl Pts',(-0.120447234018584,-0.518529242900151,
0.033795739603803));
#68614=CARTESIAN_POINT('Ctrl Pts',(-0.0332073864096211,-0.524057278571678,
0.0384322829190561));
#68615=CARTESIAN_POINT('Ctrl Pts',(0.285706463458477,-0.400329423553965,
-3.948325));
#68616=CARTESIAN_POINT('Ctrl Pts',(0.35234932738247,-0.352767850893538,
-3.94368845668475));
#68617=CARTESIAN_POINT('Ctrl Pts',(0.461355386710151,-0.223767338793563,
-3.93441537005424));
#68618=CARTESIAN_POINT('Ctrl Pts',(0.512153850375005,0.024551470863185,
-3.92050574010848));
#68619=CARTESIAN_POINT('Ctrl Pts',(0.437852459283724,0.266806684479465,
-3.90659611016272));
#68620=CARTESIAN_POINT('Ctrl Pts',(0.256595437328703,0.443921775016828,
-3.89268648021697));
#68621=CARTESIAN_POINT('Ctrl Pts',(0.0126607096365889,0.51258367325088,
-3.8787768502712));
#68622=CARTESIAN_POINT('Ctrl Pts',(-0.234367035151384,0.456045416423434,
-3.86486722032544));
#68623=CARTESIAN_POINT('Ctrl Pts',(-0.424145829883178,0.288104776438461,
-3.85095759037969));
#68624=CARTESIAN_POINT('Ctrl Pts',(-0.510318778475725,0.0497911051028911,
-3.83704796043392));
#68625=CARTESIAN_POINT('Ctrl Pts',(-0.471836291860887,-0.200686156364057,
-3.82313833048817));
#68626=CARTESIAN_POINT('Ctrl Pts',(-0.318098551972822,-0.402141302407426,
-3.80922870054241));
#68627=CARTESIAN_POINT('Ctrl Pts',(-0.086658980441776,-0.505365835465607,
-3.79531907059665));
#68628=CARTESIAN_POINT('Ctrl Pts',(0.165948741836808,-0.485144687019642,
-3.7814094406509));
#68629=CARTESIAN_POINT('Ctrl Pts',(0.378020228680476,-0.346417499554377,
-3.76749981070513));
#68630=CARTESIAN_POINT('Ctrl Pts',(0.497752849465234,-0.123070995229855,
-3.75359018075938));
#68631=CARTESIAN_POINT('Ctrl Pts',(0.495899563082201,0.130337996110901,
-3.73968055081361));
#68632=CARTESIAN_POINT('Ctrl Pts',(0.372913069708243,0.351909382815266,
-3.72577092086785));
#68633=CARTESIAN_POINT('Ctrl Pts',(0.158835236222117,0.487519986810459,
-3.7118612909221));
#68634=CARTESIAN_POINT('Ctrl Pts',(-0.0940412229640735,0.504044263082503,
-3.69795166097634));
#68635=CARTESIAN_POINT('Ctrl Pts',(-0.323946266642341,0.397445828529313,
-3.68404203103058));
#68636=CARTESIAN_POINT('Ctrl Pts',(-0.474721073230568,0.193763446229383,
-3.67013240108482));
#68637=CARTESIAN_POINT('Ctrl Pts',(-0.509535935329301,-0.0572494632079747,
-3.65622277113906));
#68638=CARTESIAN_POINT('Ctrl Pts',(-0.419886639219421,-0.294278066833141,
-3.6423131411933));
#68639=CARTESIAN_POINT('Ctrl Pts',(-0.227671785951002,-0.459423473843918,
-3.62840351124754));
#68640=CARTESIAN_POINT('Ctrl Pts',(0.0201563719388868,-0.512345675389839,
-3.61449388130178));
#68641=CARTESIAN_POINT('Ctrl Pts',(0.263060940163059,-0.440117384557558,
-3.60058425135602));
#68642=CARTESIAN_POINT('Ctrl Pts',(0.441707707892028,-0.260381779728162,
-3.58667462141027));
#68643=CARTESIAN_POINT('Ctrl Pts',(0.512458693932598,-0.0170428119589638,
-3.57276499146451));
#68644=CARTESIAN_POINT('Ctrl Pts',(0.458031580571258,0.230459197312829,
-3.55885536151875));
#68645=CARTESIAN_POINT('Ctrl Pts',(0.291721259059309,0.421667021996254,
-3.54494573157299));
#68646=CARTESIAN_POINT('Ctrl Pts',(0.0541522913452231,0.509874396070913,
-3.53103610162723));
#68647=CARTESIAN_POINT('Ctrl Pts',(-0.196644436945652,0.473534936245239,
-3.51712647168147));
#68648=CARTESIAN_POINT('Ctrl Pts',(-0.399406899907004,0.321525269198555,
-3.50321684173571));
#68649=CARTESIAN_POINT('Ctrl Pts',(-0.504606384212198,0.0909767411968328,
-3.48930721178995));
#68650=CARTESIAN_POINT('Ctrl Pts',(-0.486545849964599,-0.161794642398108,
-3.4753975818442));
#68651=CARTESIAN_POINT('Ctrl Pts',(-0.349636937317957,-0.3750445073447,
-3.46148795189843));
#68652=CARTESIAN_POINT('Ctrl Pts',(-0.127322336735289,-0.496682386435005,
-3.44757832195268));
#68653=CARTESIAN_POINT('Ctrl Pts',(0.12609324488764,-0.496995839037123,
-3.43366869200692));
#68654=CARTESIAN_POINT('Ctrl Pts',(0.348708075290391,-0.375908298197551,
-3.41975906206116));
#68655=CARTESIAN_POINT('Ctrl Pts',(0.486144110547877,-0.162997773623204,
-3.4058494321154));
#68656=CARTESIAN_POINT('Ctrl Pts',(0.504829900148016,0.0897281580277445,
-3.39193980216964));
#68657=CARTESIAN_POINT('Ctrl Pts',(0.40020107303874,0.320536225043519,-3.37803017222388));
#68658=CARTESIAN_POINT('Ctrl Pts',(0.197815274890308,0.473047024561597,
-3.36412054227812));
#68659=CARTESIAN_POINT('Ctrl Pts',(-0.0528907887479718,0.51000679886853,
-3.35021091233236));
#68660=CARTESIAN_POINT('Ctrl Pts',(-0.29067723859158,0.422387397292203,
-3.3363012823866));
#68661=CARTESIAN_POINT('Ctrl Pts',(-0.457460064734289,0.231591579293824,
-3.32239165244084));
#68662=CARTESIAN_POINT('Ctrl Pts',(-0.512499286692634,-0.0157750298272154,
-3.30848202249509));
#68663=CARTESIAN_POINT('Ctrl Pts',(-0.442350493670444,-0.259288278130775,
-3.29457239254933));
#68664=CARTESIAN_POINT('Ctrl Pts',(-0.264148905910468,-0.439465272726765,
-3.28066276260357));
#68665=CARTESIAN_POINT('Ctrl Pts',(-0.0214237606571462,-0.512294244458996,
-3.26675313265781));
#68666=CARTESIAN_POINT('Ctrl Pts',(0.226534558845831,-0.459985286802776,
-3.25284350271205));
#68667=CARTESIAN_POINT('Ctrl Pts',(0.419157363777824,-0.295315889882908,
-3.2389338727663));
#68668=CARTESIAN_POINT('Ctrl Pts',(0.509392751403437,-0.0585097875927088,
-3.22502424282053));
#68669=CARTESIAN_POINT('Ctrl Pts',(0.475198956297498,0.192588479303088,
-3.21111461287478));
#68670=CARTESIAN_POINT('Ctrl Pts',(0.324928484395358,0.396643228172426,
-3.19720498292901));
#68671=CARTESIAN_POINT('Ctrl Pts',(0.0952878493958325,0.503810079478394,
-3.18329535298326));
#68672=CARTESIAN_POINT('Ctrl Pts',(-0.157628714033977,0.487911425300231,
-3.1693857230375));
#68673=CARTESIAN_POINT('Ctrl Pts',(-0.372041368626771,0.35283082413081,
-3.15547609309174));
#68674=CARTESIAN_POINT('Ctrl Pts',(-0.49557561296929,0.131564365451365,
-3.14156646314598));
#68675=CARTESIAN_POINT('Ctrl Pts',(-0.498055781976883,-0.12183927308509,
-3.12765683320022));
#68676=CARTESIAN_POINT('Ctrl Pts',(-0.378876045665121,-0.345481276551521,
-3.11374720325446));
#68677=CARTESIAN_POINT('Ctrl Pts',(-0.167148395020481,-0.484732693830926,
-3.0998375733087));
#68678=CARTESIAN_POINT('Ctrl Pts',(0.0854085334848828,-0.505578631702793,
-3.08592794336294));
#68679=CARTESIAN_POINT('Ctrl Pts',(0.317102750476299,-0.402927060479777,
-3.07201831341718));
#68680=CARTESIAN_POINT('Ctrl Pts',(0.47133839355793,-0.201852642253547,
-3.05810868347143));
#68681=CARTESIAN_POINT('Ctrl Pts',(0.510440378104306,0.0485282477248127,
-3.04419905352566));
#68682=CARTESIAN_POINT('Ctrl Pts',(0.424857276524671,0.287055160222818,
-3.03028942357991));
#68683=CARTESIAN_POINT('Ctrl Pts',(0.235494442018191,0.455463212790065,
-3.01637979363415));
#68684=CARTESIAN_POINT('Ctrl Pts',(-0.0113925344738468,0.512615431473507,
-3.00247016368839));
#68685=CARTESIAN_POINT('Ctrl Pts',(-0.255496660699727,0.444551264532895,
-2.98856053374263));
#68686=CARTESIAN_POINT('Ctrl Pts',(-0.437190710233471,0.267896721353699,
-2.97465090379687));
#68687=CARTESIAN_POINT('Ctrl Pts',(-0.512092343459165,0.0258031431614133,
-2.96074127385111));
#68688=CARTESIAN_POINT('Ctrl Pts',(-0.46190536558045,-0.222593359457327,
-2.94683164390536));
#68689=CARTESIAN_POINT('Ctrl Pts',(-0.29888893149109,-0.416617062851034,
-2.93292201395959));
#68690=CARTESIAN_POINT('Ctrl Pts',(-0.0628630064529875,-0.5088738673249,
-2.91901238401384));
#68691=CARTESIAN_POINT('Ctrl Pts',(0.188518442383684,-0.476828236692982,
-2.90510275406808));
#68692=CARTESIAN_POINT('Ctrl Pts',(0.393850559636817,-0.328307945533265,
-2.89119312412232));
#68693=CARTESIAN_POINT('Ctrl Pts',(0.502976943457436,-0.0995919915290553,
-2.87728349417656));
#68694=CARTESIAN_POINT('Ctrl Pts',(0.489241331627754,0.153451262144076,
-2.8633738642308));
#68695=CARTESIAN_POINT('Ctrl Pts',(0.35599891707028,0.369011031639022,-2.84946423428504));
#68696=CARTESIAN_POINT('Ctrl Pts',(0.135796776088882,0.494432610201203,
-2.83555460433928));
#68697=CARTESIAN_POINT('Ctrl Pts',(-0.117576394161712,0.499079314300279,
-2.82164497439352));
#68698=CARTESIAN_POINT('Ctrl Pts',(-0.342229221231611,0.381816095210394,
-2.80773534444777));
#68699=CARTESIAN_POINT('Ctrl Pts',(-0.483285840488613,0.17128679695097,
-2.793825714502));
#68700=CARTESIAN_POINT('Ctrl Pts',(-0.506290402679528,-0.0810826651085765,
-2.77991608455625));
#68701=CARTESIAN_POINT('Ctrl Pts',(-0.405623591737084,-0.313646093954341,
-2.76600645461048));
#68702=CARTESIAN_POINT('Ctrl Pts',(-0.205875253078692,-0.469595305125906,
-2.75209682466473));
#68703=CARTESIAN_POINT('Ctrl Pts',(0.0441621590199009,-0.510836641341642,
-2.73818719471897));
#68704=CARTESIAN_POINT('Ctrl Pts',(0.283412096543389,-0.427296096354025,
-2.72427756477321));
#68705=CARTESIAN_POINT('Ctrl Pts',(0.453433063980492,-0.239380088803917,
-2.71036793482745));
#68706=CARTESIAN_POINT('Ctrl Pts',(0.512694101247579,0.00700920626356338,
-2.69645830488169));
#68707=CARTESIAN_POINT('Ctrl Pts',(0.446719536253416,0.251686365057864,
-2.68254867493593));
#68708=CARTESIAN_POINT('Ctrl Pts',(0.271624952073492,0.434884186695241,
-2.66863904499017));
#68709=CARTESIAN_POINT('Ctrl Pts',(0.0301806393140316,0.511853005693142,
-2.65472941504441));
#68710=CARTESIAN_POINT('Ctrl Pts',(-0.218635887270253,0.463791676535983,
-2.64081978509866));
#68711=CARTESIAN_POINT('Ctrl Pts',(-0.414046304926066,0.302440122674851,
-2.6269101551529));
#68712=CARTESIAN_POINT('Ctrl Pts',(-0.508317781768474,0.0672116296818217,
-2.61300052520714));
#68713=CARTESIAN_POINT('Ctrl Pts',(-0.478422658322387,-0.184434623729516,
-2.59909089526138));
#68714=CARTESIAN_POINT('Ctrl Pts',(-0.331663405555064,-0.391029098459597,
-2.58518126531562));
#68715=CARTESIAN_POINT('Ctrl Pts',(-0.103888852940067,-0.502107037056149,
-2.57127163536986));
#68716=CARTESIAN_POINT('Ctrl Pts',(0.149262592123117,-0.490535471723703,
-2.5573620054241));
#68717=CARTESIAN_POINT('Ctrl Pts',(0.365953717915752,-0.359140984531349,
-2.54345237547834));
#68718=CARTESIAN_POINT('Ctrl Pts',(0.49325346169053,-0.140019259235349,
-2.52954274553259));
#68719=CARTESIAN_POINT('Ctrl Pts',(0.500066361181473,0.113304919757393,
-2.51563311558682));
#68720=CARTESIAN_POINT('Ctrl Pts',(0.384728231899584,0.338952147073784,
-2.50172348564107));
#68721=CARTESIAN_POINT('Ctrl Pts',(0.175412676874732,0.481803656293877,
-2.48781385569531));
#68722=CARTESIAN_POINT('Ctrl Pts',(-0.0767508691435963,0.506965161043843,
-2.47390422574955));
#68723=CARTESIAN_POINT('Ctrl Pts',(-0.310166508178242,0.4082904696794,-2.45999459580379));
#68724=CARTESIAN_POINT('Ctrl Pts',(-0.467817886694874,0.209882813290774,
-2.44608496585803));
#68725=CARTESIAN_POINT('Ctrl Pts',(-0.511195559611515,-0.0397928418183265,
-2.43217533591227));
#68726=CARTESIAN_POINT('Ctrl Pts',(-0.429703678489127,-0.279748313881283,
-2.41826570596651));
#68727=CARTESIAN_POINT('Ctrl Pts',(-0.243248235588849,-0.451369766720613,
-2.40435607602075));
#68728=CARTESIAN_POINT('Ctrl Pts',(0.00262536564176082,-0.512735290263655,
-2.39044644607499));
#68729=CARTESIAN_POINT('Ctrl Pts',(0.247857669758745,-0.448855150319423,
-2.37653681612923));
#68730=CARTESIAN_POINT('Ctrl Pts',(0.432545870731629,-0.275333325515683,
-2.36262718618348));
#68731=CARTESIAN_POINT('Ctrl Pts',(0.511576248657834,-0.0345559290959576,
-2.34871755623772));
#68732=CARTESIAN_POINT('Ctrl Pts',(0.46564408176967,0.214662431597587,-2.33480792629196));
#68733=CARTESIAN_POINT('Ctrl Pts',(0.305969203822596,0.411445277939455,
-2.3208982963462));
#68734=CARTESIAN_POINT('Ctrl Pts',(0.0715553393709438,0.507724535387071,
-2.30698866640044));
#68735=CARTESIAN_POINT('Ctrl Pts',(-0.180337321890193,0.479982104624726,
-2.29307903645468));
#68736=CARTESIAN_POINT('Ctrl Pts',(-0.388179050905097,0.334994619158167,
-2.27916940650892));
#68737=CARTESIAN_POINT('Ctrl Pts',(-0.501200423869475,0.108178119504665,
-2.26525977656316));
#68738=CARTESIAN_POINT('Ctrl Pts',(-0.491793750979322,-0.145063010185908,
-2.2513501466174));
#68739=CARTESIAN_POINT('Ctrl Pts',(-0.362256796811613,-0.362869650963398,
-2.23744051667165));
#68740=CARTESIAN_POINT('Ctrl Pts',(-0.144231506204031,-0.492038253639516,
-2.22353088672589));
#68741=CARTESIAN_POINT('Ctrl Pts',(0.1090251621404,-0.501016850461905,-2.20962125678013));
#68742=CARTESIAN_POINT('Ctrl Pts',(0.33565029365018,-0.387612242839485,
-2.19571162683437));
#68743=CARTESIAN_POINT('Ctrl Pts',(0.480286249602533,-0.179525733167259,
-2.18180199688861));
#68744=CARTESIAN_POINT('Ctrl Pts',(0.507602857467195,0.0724134622680479,
-2.16789236694285));
#68745=CARTESIAN_POINT('Ctrl Pts',(0.410927499343277,0.306664247524861,
-2.15398273699709));
#68746=CARTESIAN_POINT('Ctrl Pts',(0.213875029915099,0.466006268203898,
-2.14007310705133));
#68747=CARTESIAN_POINT('Ctrl Pts',(-0.0354206155412066,0.511517106675026,
-2.12616347710558));
#68748=CARTESIAN_POINT('Ctrl Pts',(-0.276064080079156,0.432079846922483,
-2.11225384715981));
#68749=CARTESIAN_POINT('Ctrl Pts',(-0.449273471848797,0.247098599590194,
-2.09834421721406));
#68750=CARTESIAN_POINT('Ctrl Pts',(-0.512738995510593,0.00175866690871404,
-2.0844345872683));
#68751=CARTESIAN_POINT('Ctrl Pts',(-0.450957950605788,-0.244010854701047,
-2.07052495732254));
#68752=CARTESIAN_POINT('Ctrl Pts',(-0.279021570577783,-0.430175933286389,
-2.05661532737678));
#68753=CARTESIAN_POINT('Ctrl Pts',(-0.0389286926494526,-0.511262092585704,
-2.04270569743102));
#68754=CARTESIAN_POINT('Ctrl Pts',(0.210673282920791,-0.467462445860503,
-2.02879606748526));
#68755=CARTESIAN_POINT('Ctrl Pts',(0.408814172040582,-0.309475916939077,
-2.0148864375395));
#68756=CARTESIAN_POINT('Ctrl Pts',(0.507094171550263,-0.0758938179712873,
-2.00097680759374));
#68757=CARTESIAN_POINT('Ctrl Pts',(0.481506461595899,0.176226836401005,
-1.98706717764799));
#68758=CARTESIAN_POINT('Ctrl Pts',(0.338301342812545,0.385300625327465,
-1.97315754770222));
#68759=CARTESIAN_POINT('Ctrl Pts',(0.112459477653878,0.500257170175825,
-1.95924791775647));
#68760=CARTESIAN_POINT('Ctrl Pts',(-0.140852823344986,0.493016077407475,
-1.94533828781071));
#68761=CARTESIAN_POINT('Ctrl Pts',(-0.359759056244216,0.365346126128058,
-1.93142865786495));
#68762=CARTESIAN_POINT('Ctrl Pts',(-0.490787074886546,0.148433209056515,
-1.91751902791919));
#68763=CARTESIAN_POINT('Ctrl Pts',(-0.501930712655587,-0.104737434184549,
-1.90360939797343));
#68764=CARTESIAN_POINT('Ctrl Pts',(-0.390467917193037,-0.332323902344444,
-1.88969976802767));
#68765=CARTESIAN_POINT('Ctrl Pts',(-0.183625665141514,-0.478733731345353,
-1.87579013808191));
#68766=CARTESIAN_POINT('Ctrl Pts',(0.0680707615702241,-0.508203445330468,
-1.86188050813615));
#68767=CARTESIAN_POINT('Ctrl Pts',(0.303139568028706,-0.413534487947351,
-1.8479708781904));
#68768=CARTESIAN_POINT('Ctrl Pts',(0.464160582092247,-0.217851611098688,
-1.83406124824463));
#68769=CARTESIAN_POINT('Ctrl Pts',(0.511801259025317,0.0310457998223131,
-1.82015161829888));
#68770=CARTESIAN_POINT('Ctrl Pts',(0.43442442794312,0.272359664474753,-1.80624198835312));
#68771=CARTESIAN_POINT('Ctrl Pts',(0.250930899325168,0.447144332615734,
-1.79233235840736));
#68772=CARTESIAN_POINT('Ctrl Pts',(0.00614257089095992,0.512705216717518,
-1.7784227284616));
#68773=CARTESIAN_POINT('Ctrl Pts',(-0.240146201108115,0.453027783386239,
-1.76451309851584));
#68774=CARTESIAN_POINT('Ctrl Pts',(-0.427774547614985,0.282689417628787,
-1.75060346857008));
#68775=CARTESIAN_POINT('Ctrl Pts',(-0.510910560443286,0.0432986103014504,
-1.73669383862433));
#68776=CARTESIAN_POINT('Ctrl Pts',(-0.469246635876068,-0.206668732868568,
-1.72278420867856));
#68777=CARTESIAN_POINT('Ctrl Pts',(-0.312960005664294,-0.406153179577745,
-1.70887457873281));
#68778=CARTESIAN_POINT('Ctrl Pts',(-0.0802267483162252,-0.506426736341114,
-1.69496494878705));
#68779=CARTESIAN_POINT('Ctrl Pts',(0.172103467761028,-0.482995617797032,
-1.68105531884129));
#68780=CARTESIAN_POINT('Ctrl Pts',(0.38239403215543,-0.341583334778529,
-1.66714568889553));
#68781=CARTESIAN_POINT('Ctrl Pts',(0.499277344932229,-0.116732614396888,
-1.65323605894977));
#68782=CARTESIAN_POINT('Ctrl Pts',(0.494202361649382,0.136632339388161,
-1.63932642900401));
#68783=CARTESIAN_POINT('Ctrl Pts',(0.36840874663372,0.35662216115979,-1.62541679905825));
#68784=CARTESIAN_POINT('Ctrl Pts',(0.152624060625208,0.489500016899674,
-1.61150716911249));
#68785=CARTESIAN_POINT('Ctrl Pts',(-0.100442049346334,0.502807880954164,
-1.59759753916673));
#68786=CARTESIAN_POINT('Ctrl Pts',(-0.328973216334069,0.393295046194743,
-1.58368790922097));
#68787=CARTESIAN_POINT('Ctrl Pts',(-0.477146215019956,0.187712173069935,
-1.56977827927521));
#68788=CARTESIAN_POINT('Ctrl Pts',(-0.508766880727387,-0.0637230845254107,
-1.55586864932946));
#68789=CARTESIAN_POINT('Ctrl Pts',(-0.416111244906428,-0.299592727363217,
-1.5419590193837));
#68790=CARTESIAN_POINT('Ctrl Pts',(-0.221812266131596,-0.462280963289723,
-1.52804938943794));
#68791=CARTESIAN_POINT('Ctrl Pts',(0.0266687144847388,-0.512047995889291,
-1.51413975949218));
#68792=CARTESIAN_POINT('Ctrl Pts',(0.268635337881236,-0.436737250149265,
-1.50023012954642));
#68793=CARTESIAN_POINT('Ctrl Pts',(0.44498250467321,-0.254744854631581,
-1.48632049960066));
#68794=CARTESIAN_POINT('Ctrl Pts',(0.512633956353846,-0.0105260258174941,
-1.4724108696549));
#68795=CARTESIAN_POINT('Ctrl Pts',(0.455064497344623,0.23626399150737,-1.45850123970914));
#68796=CARTESIAN_POINT('Ctrl Pts',(0.286336598528917,0.425341889271909,
-1.44459160976338));
#68797=CARTESIAN_POINT('Ctrl Pts',(0.047665362586952,0.510521677929509,
-1.43068197981763));
#68798=CARTESIAN_POINT('Ctrl Pts',(-0.202649074195538,0.47099652138227,
-1.41677234987187));
#68799=CARTESIAN_POINT('Ctrl Pts',(-0.403462495084136,0.316421215292198,
-1.40286271992611));
#68800=CARTESIAN_POINT('Ctrl Pts',(-0.505722278552809,0.0845538136447024,
-1.38895308998035));
#68801=CARTESIAN_POINT('Ctrl Pts',(-0.484449464362613,-0.167967517411213,
-1.37504346003459));
#68802=CARTESIAN_POINT('Ctrl Pts',(-0.344840355124436,-0.379459483876949,
-1.36113383008883));
#68803=CARTESIAN_POINT('Ctrl Pts',(-0.120997217343892,-0.498261019769301,
-1.34722420014307));
#68804=CARTESIAN_POINT('Ctrl Pts',(0.132401866856018,-0.495352516981138,
-1.33331457019731));
#68805=CARTESIAN_POINT('Ctrl Pts',(0.353459195034396,-0.371444434434203,
-1.31940494025155));
#68806=CARTESIAN_POINT('Ctrl Pts',(0.488177173769909,-0.156803754535824,
-1.30549531030579));
#68807=CARTESIAN_POINT('Ctrl Pts',(0.503648291231812,0.0961393216419958,
-1.29158568036004));
#68808=CARTESIAN_POINT('Ctrl Pts',(0.396093423165933,0.325598480572622,
-1.27767605041428));
#68809=CARTESIAN_POINT('Ctrl Pts',(0.191784958206317,0.475523816682518,
-1.26376642046852));
#68810=CARTESIAN_POINT('Ctrl Pts',(-0.0593707489727289,0.509293122467725,
-1.24985679052276));
#68811=CARTESIAN_POINT('Ctrl Pts',(-0.296023984821974,0.418657581845388,
-1.235947160577));
#68812=CARTESIAN_POINT('Ctrl Pts',(-0.460367549206804,0.22575670546814,
-1.22203753063124));
#68813=CARTESIAN_POINT('Ctrl Pts',(-0.512257299229123,-0.0222896795174969,
-1.20812790068548));
#68814=CARTESIAN_POINT('Ctrl Pts',(-0.439018144460899,-0.264891372567355,
-1.19421827073972));
#68815=CARTESIAN_POINT('Ctrl Pts',(-0.258540186688332,-0.442788146062732,
-1.18030864079396));
#68816=CARTESIAN_POINT('Ctrl Pts',(-0.0149087112336633,-0.512525219629101,
-1.1663990108482));
#68817=CARTESIAN_POINT('Ctrl Pts',(0.232364509709674,-0.45706794358595,
-1.15248938090245));
#68818=CARTESIAN_POINT('Ctrl Pts',(0.422878136097861,-0.289962846649199,
-1.13857975095669));
#68819=CARTESIAN_POINT('Ctrl Pts',(0.51009547347383,-0.052028630272347,
-1.12467012101093));
#68820=CARTESIAN_POINT('Ctrl Pts',(0.472711974452847,0.198614600760868,
-1.11076049106517));
#68821=CARTESIAN_POINT('Ctrl Pts',(0.319859292789327,0.400742315263586,
-1.09685086111941));
#68822=CARTESIAN_POINT('Ctrl Pts',(0.0888746976244564,0.504980849685084,
-1.08294123117365));
#68823=CARTESIAN_POINT('Ctrl Pts',(-0.163819287712257,0.485867895008465,
-1.06903160122789));
#68824=CARTESIAN_POINT('Ctrl Pts',(-0.376497195023632,0.348072165744182,
-1.05512197128213));
#68825=CARTESIAN_POINT('Ctrl Pts',(-0.497208268985998,0.125252974728969,
-1.04121234133637));
#68826=CARTESIAN_POINT('Ctrl Pts',(-0.496466459320068,-0.128161715019355,
-1.02730271139061));
#68827=CARTESIAN_POINT('Ctrl Pts',(-0.37445296760404,-0.350270389098243,
-1.01339308144486));
#68828=CARTESIAN_POINT('Ctrl Pts',(-0.160971985229762,-0.48681864220436,
-0.999483451499097));
#68829=CARTESIAN_POINT('Ctrl Pts',(0.091829565624597,-0.50445188204992,
-0.985573821553339));
#68830=CARTESIAN_POINT('Ctrl Pts',(0.322199941771856,-0.398862843529854,
-0.971664191607578));
#68831=CARTESIAN_POINT('Ctrl Pts',(0.473866654939281,-0.195843722807663,
-0.957754561661822));
#68832=CARTESIAN_POINT('Ctrl Pts',(0.509782132080318,0.0550140730918329,
-0.94384493171606));
#68833=CARTESIAN_POINT('Ctrl Pts',(0.421173312613008,0.292433601299668,
-0.929935301770304));
#68834=CARTESIAN_POINT('Ctrl Pts',(0.229684640748129,0.458420479724576,
-0.916025671824541));
#68835=CARTESIAN_POINT('Ctrl Pts',(-0.017909015052109,0.512429153743588,
-0.902116041878785));
#68836=CARTESIAN_POINT('Ctrl Pts',(-0.261128042237548,0.441266944132112,
-0.888206411933025));
#68837=CARTESIAN_POINT('Ctrl Pts',(-0.440561417203972,0.262316618035793,
-0.874296781987266));
#68838=CARTESIAN_POINT('Ctrl Pts',(-0.512379014492537,0.0192903067410717,
-0.860387152041508));
#68839=CARTESIAN_POINT('Ctrl Pts',(-0.459037975647287,-0.228448040788597,
-0.846477522095749));
#68840=CARTESIAN_POINT('Ctrl Pts',(-0.293567896890941,-0.420383468206752,
-0.832567892149989));
#68841=CARTESIAN_POINT('Ctrl Pts',(-0.0563880943787678,-0.509631978234137,
-0.818658262204231));
#68842=CARTESIAN_POINT('Ctrl Pts',(0.194565607506746,-0.474392869678749,
-0.804748632258471));
#68843=CARTESIAN_POINT('Ctrl Pts',(0.397992838976195,-0.323273986813317,
-0.790839002312714));
#68844=CARTESIAN_POINT('Ctrl Pts',(0.504202503940466,-0.0931890843751128,
-0.776929372366952));
#68845=CARTESIAN_POINT('Ctrl Pts',(0.487250806039511,0.159659081922555,
-0.763019742421195));
#68846=CARTESIAN_POINT('Ctrl Pts',(0.351278530374647,0.373507382155073,
-0.749110112475436));
#68847=CARTESIAN_POINT('Ctrl Pts',(0.12949957543287,0.496119169544188,-0.735200482529676));
#68848=CARTESIAN_POINT('Ctrl Pts',(-0.123912193856582,0.497544107230863,
-0.721290852583919));
#68849=CARTESIAN_POINT('Ctrl Pts',(-0.347055976470588,0.377434126202911,
-0.707381222638158));
#68850=CARTESIAN_POINT('Ctrl Pts',(-0.485424521519157,0.165128447986424,
-0.6934715926924));
#68851=CARTESIAN_POINT('Ctrl Pts',(-0.505218594661576,-0.0875130963610043,
-0.67956196274664));
#68852=CARTESIAN_POINT('Ctrl Pts',(-0.401603104826651,-0.318777848383641,
-0.665652332800882));
#68853=CARTESIAN_POINT('Ctrl Pts',(-0.199888170155967,-0.472174850937878,
-0.651742702855122));
#68854=CARTESIAN_POINT('Ctrl Pts',(0.0506533753796834,-0.510233873815872,
-0.637833072909363));
#68855=CARTESIAN_POINT('Ctrl Pts',(0.288821839273072,-0.423658253295539,
-0.623923442963605));
#68856=CARTESIAN_POINT('Ctrl Pts',(0.45643989718452,-0.233595784817902,
-0.610013813017846));
#68857=CARTESIAN_POINT('Ctrl Pts',(0.512563546869181,0.0135270413392405,
-0.596104183072087));
#68858=CARTESIAN_POINT('Ctrl Pts',(0.443483484763275,0.257345622011976,
-0.582194553126329));
#68859=CARTESIAN_POINT('Ctrl Pts',(0.266073872596039,0.438302480883072,
-0.568284923180568));
#68860=CARTESIAN_POINT('Ctrl Pts',(0.0236704920209714,0.51219535163255,
-0.55437529323481));
#68861=CARTESIAN_POINT('Ctrl Pts',(-0.224514871059556,0.460974449508451,
-0.540465663289051));
#68862=CARTESIAN_POINT('Ctrl Pts',(-0.417858067972524,0.297151485705153,
-0.526556033343292));
#68863=CARTESIAN_POINT('Ctrl Pts',(-0.509131226094477,0.0607434362054208,
-0.512646403397532));
#68864=CARTESIAN_POINT('Ctrl Pts',(-0.476039084177294,-0.19050239043684,
-0.498736773451774));
#68865=CARTESIAN_POINT('Ctrl Pts',(-0.326665047731261,-0.395214267223794,
-0.484827143506015));
#68866=CARTESIAN_POINT('Ctrl Pts',(-0.0974966584912855,-0.503387298220306,
-0.470917513560256));
#68867=CARTESIAN_POINT('Ctrl Pts',(0.155487204176033,-0.488598096357353,
-0.457007883614497));
#68868=CARTESIAN_POINT('Ctrl Pts',(0.37049026384305,-0.354459214612929,
-0.443098253668739));
#68869=CARTESIAN_POINT('Ctrl Pts',(0.494993801063038,-0.133736709005703,
-0.429188623722979));
#68870=CARTESIAN_POINT('Ctrl Pts',(0.498585381931524,0.11965361403109,-0.41527899377722));
#68871=CARTESIAN_POINT('Ctrl Pts',(0.380387692291731,0.343816192142657,
-0.401369363831462));
#68872=CARTESIAN_POINT('Ctrl Pts',(0.169272838945517,0.483994913632211,
-0.387459733885702));
#68873=CARTESIAN_POINT('Ctrl Pts',(-0.0831902294088231,0.505948373015826,
-0.373550103939943));
#68874=CARTESIAN_POINT('Ctrl Pts',(-0.315332450581861,0.404314006728254,
-0.359640473994185));
#68875=CARTESIAN_POINT('Ctrl Pts',(-0.470448528358375,0.203918004579725,
-0.345730844048426));
#68876=CARTESIAN_POINT('Ctrl Pts',(-0.510648314649788,-0.0462889746268909,
-0.331821214102667));
#68877=CARTESIAN_POINT('Ctrl Pts',(-0.426112222229761,-0.285188962782551,
-0.317911584156906));
#68878=CARTESIAN_POINT('Ctrl Pts',(-0.237489851752064,-0.454425946376765,
-0.304001954211149));
#68879=CARTESIAN_POINT('Ctrl Pts',(0.00914407872677023,-0.512660468783674,
-0.290092324265389));
#68880=CARTESIAN_POINT('Ctrl Pts',(0.253544388403441,-0.445667604307889,
-0.27618269431963));
#68881=CARTESIAN_POINT('Ctrl Pts',(0.436011502246361,-0.269811675703265,
-0.262273064373872));
#68882=CARTESIAN_POINT('Ctrl Pts',(0.511974244464808,-0.0280489468379449,
-0.248363434428113));
#68883=CARTESIAN_POINT('Ctrl Pts',(0.462877223624254,0.220565288020147,
-0.234453804482355));
#68884=CARTESIAN_POINT('Ctrl Pts',(0.300713351069406,0.41530212009148,-0.220544174536595));
#68885=CARTESIAN_POINT('Ctrl Pts',(0.0650943374357338,0.508593253514698,
-0.206634544590836));
#68886=CARTESIAN_POINT('Ctrl Pts',(-0.186425246756546,0.477650497890165,
-0.192724914645077));
#68887=CARTESIAN_POINT('Ctrl Pts',(-0.392406802818875,0.330032227073166,
-0.178815284699318));
#68888=CARTESIAN_POINT('Ctrl Pts',(-0.502535292738926,0.101797106169335,
-0.164905654753559));
#68889=CARTESIAN_POINT('Ctrl Pts',(-0.489909666259365,-0.151303961616872,
-0.1509960248078));
#68890=CARTESIAN_POINT('Ctrl Pts',(-0.357613988294798,-0.367446056440282,
-0.137086394862041));
#68891=CARTESIAN_POINT('Ctrl Pts',(-0.137964061075247,-0.493832254050675,
-0.123176764916282));
#68892=CARTESIAN_POINT('Ctrl Pts',(0.115386277850666,-0.499590191201122,
-0.109267134970524));
#68893=CARTESIAN_POINT('Ctrl Pts',(0.340551290583365,-0.383313481407925,
-0.0953575050247649));
#68894=CARTESIAN_POINT('Ctrl Pts',(0.482529888616476,-0.173404793650348,
-0.0814478750790055));
#68895=CARTESIAN_POINT('Ctrl Pts',(0.506641231064238,0.0788611606491063,
-0.0675382451332463));
#68896=CARTESIAN_POINT('Ctrl Pts',(0.406995219528124,0.311864235034375,
-0.0536286151874873));
#68897=CARTESIAN_POINT('Ctrl Pts',(0.207933188506461,0.468687354567501,
-0.0397189852417286));
#68898=CARTESIAN_POINT('Ctrl Pts',(-0.0419216921981646,0.511026320975463,
-0.0258093552959692));
#68899=CARTESIAN_POINT('Ctrl Pts',(-0.281534255742185,0.428533287500004,
-0.01189972535021));
#68900=CARTESIAN_POINT('Ctrl Pts',(-0.452380693489446,0.241369983531519,
0.00200990459554883));
#68901=CARTESIAN_POINT('Ctrl Pts',(-0.512716156498659,-0.00476716361925517,
0.0159195345413075));
#68902=CARTESIAN_POINT('Ctrl Pts',(-0.447826544932705,-0.249711286947794,
0.0298291644870661));
#68903=CARTESIAN_POINT('Ctrl Pts',(-0.273514629177701,-0.433716915029852,
0.0437387944328249));
#68904=CARTESIAN_POINT('Ctrl Pts',(-0.112812837105721,-0.485662916965135,
0.053011881063331));
#68905=CARTESIAN_POINT('Ctrl Pts',(-0.0311025778570991,-0.490840565026611,
0.0576484243785842));
#68906=CARTESIAN_POINT('',(-0.0374170035146652,-0.590490705661811,0.));
#68907=CARTESIAN_POINT('Ctrl Pts',(-0.416126897194384,0.262207742448202,
-3.46944695195361E-16));
#68908=CARTESIAN_POINT('Ctrl Pts',(-0.423456757845617,0.252783076367721,
-2.81103177996561E-16));
#68909=CARTESIAN_POINT('Ctrl Pts',(-0.430430889999018,0.243100779102031,
-6.06387724157159E-16));
#68910=CARTESIAN_POINT('Ctrl Pts',(-0.437033887600588,0.23317991320548,
-4.92661467177413E-16));
#68911=CARTESIAN_POINT('Ctrl Pts',(-0.448776940256658,0.215536222014478,
-2.9040583955556E-16));
#68912=CARTESIAN_POINT('Ctrl Pts',(-0.459347224703845,0.197138928554313,
-2.70434607762433E-17));
#68913=CARTESIAN_POINT('Ctrl Pts',(-0.468722856687143,0.178121194347624,
-2.15105711021124E-16));
#68914=CARTESIAN_POINT('Ctrl Pts',(-0.472737812302806,0.169977171748789,
-2.9564018475687E-16));
#68915=CARTESIAN_POINT('Ctrl Pts',(-0.476533480487776,0.161719154066443,
5.04918675384624E-16));
#68916=CARTESIAN_POINT('Ctrl Pts',(-0.480107142500344,0.153356755948507,
4.9960036108132E-16));
#68917=CARTESIAN_POINT('Ctrl Pts',(-0.482712193460394,0.147260915555978,
4.95723531170447E-16));
#68918=CARTESIAN_POINT('Ctrl Pts',(-0.485198246772411,0.141111675674135,
1.86231101641602E-15));
#68919=CARTESIAN_POINT('Ctrl Pts',(-0.487561379590333,0.134921318921676,
1.80411241501588E-15));
#68920=CARTESIAN_POINT('Ctrl Pts',(-0.496114159650689,0.112516839834682,
1.59347684099283E-15));
#68921=CARTESIAN_POINT('Ctrl Pts',(-0.503072184875732,0.0895449453933402,
1.51969670221732E-15));
#68922=CARTESIAN_POINT('Ctrl Pts',(-0.508399533149054,0.0661879148866036,
8.32667268468867E-16));
#68923=CARTESIAN_POINT('Ctrl Pts',(-0.510644266283795,0.0563461892066425,
5.43180331374654E-16));
#68924=CARTESIAN_POINT('Ctrl Pts',(-0.512599142677303,0.046435830069688,
1.58032048240269E-15));
#68925=CARTESIAN_POINT('Ctrl Pts',(-0.514259891977282,0.0364695744349397,
1.59594559789866E-15));
#68926=CARTESIAN_POINT('Ctrl Pts',(-0.515360081604947,0.0298672708385183,
1.60629670266802E-15));
#68927=CARTESIAN_POINT('Ctrl Pts',(-0.516331496812872,0.0232377441031986,
9.27056533275263E-16));
#68928=CARTESIAN_POINT('Ctrl Pts',(-0.517171545692938,0.0165936208095082,
8.95117313604032E-16));
#68929=CARTESIAN_POINT('Ctrl Pts',(-0.518072885339055,0.00946473595482552,
8.60847778058109E-16));
#68930=CARTESIAN_POINT('Ctrl Pts',(-0.518822529669948,0.00232377075164661,
9.51323429436439E-16));
#68931=CARTESIAN_POINT('Ctrl Pts',(-0.519419892085964,-0.00482444278728938,
9.99200722162641E-16));
#68932=CARTESIAN_POINT('Ctrl Pts',(-0.521658993972392,-0.0316181914237927,
1.17847232452288E-15));
#68933=CARTESIAN_POINT('Ctrl Pts',(-0.521762558905488,-0.0585122034193784,
7.45081943606969E-16));
#68934=CARTESIAN_POINT('Ctrl Pts',(-0.51982826242077,-0.0852697613657021,
6.80011602582908E-16));
#68935=CARTESIAN_POINT('Ctrl Pts',(-0.518558307423402,-0.102837334227329,
6.37289917765324E-16));
#68936=CARTESIAN_POINT('Ctrl Pts',(-0.516408879605909,-0.120346639156886,
9.3813456749543E-16));
#68937=CARTESIAN_POINT('Ctrl Pts',(-0.51339580078198,-0.137733394192191,
9.99200722162641E-16));
#68938=CARTESIAN_POINT('Ctrl Pts',(-0.510987430814588,-0.151630720184754,
1.04801122514605E-15));
#68939=CARTESIAN_POINT('Ctrl Pts',(-0.508027102869678,-0.165449816645127,
8.85342351292076E-16));
#68940=CARTESIAN_POINT('Ctrl Pts',(-0.504518647045066,-0.179157643895939,
9.99200722162641E-16));
#68941=CARTESIAN_POINT('Ctrl Pts',(-0.502965597266262,-0.185225537905152,
1.04960116228077E-15));
#68942=CARTESIAN_POINT('Ctrl Pts',(-0.501306004368436,-0.191267606929154,
1.52465683996833E-15));
#68943=CARTESIAN_POINT('Ctrl Pts',(-0.499543447133405,-0.197271810403005,
1.46410661372443E-15));
#68944=CARTESIAN_POINT('Ctrl Pts',(-0.492776236939559,-0.220324512548841,
1.23162842797623E-15));
#68945=CARTESIAN_POINT('Ctrl Pts',(-0.484483280990387,-0.242859221574429,
8.43887503199872E-16));
#68946=CARTESIAN_POINT('Ctrl Pts',(-0.47471735717438,-0.26471982397249,
4.92661467177413E-16));
#68947=CARTESIAN_POINT('Ctrl Pts',(-0.465268640557773,-0.285870371633841,
1.53167248280808E-16));
#68948=CARTESIAN_POINT('Ctrl Pts',(-0.454440972414739,-0.306390519760755,
1.13612733355049E-15));
#68949=CARTESIAN_POINT('Ctrl Pts',(-0.442338530304677,-0.32618075080411,
1.13450915328883E-15));
#68950=CARTESIAN_POINT('Ctrl Pts',(-0.434728174109778,-0.338625405035842,
1.13349159600024E-15));
#68951=CARTESIAN_POINT('Ctrl Pts',(-0.426613216462773,-0.350781336469998,
3.00879890662803E-16));
#68952=CARTESIAN_POINT('Ctrl Pts',(-0.418014837814341,-0.362621829072243,
4.30211422042248E-16));
#68953=CARTESIAN_POINT('Ctrl Pts',(-0.413274602275642,-0.36914942295055,
5.01511134044471E-16));
#68954=CARTESIAN_POINT('Ctrl Pts',(-0.408385147719558,-0.375583552328859,
6.51549061365782E-16));
#68955=CARTESIAN_POINT('Ctrl Pts',(-0.403366333700444,-0.381899519271175,
7.11236625150491E-16));
#68956=CARTESIAN_POINT('Ctrl Pts',(-0.385533464976329,-0.404341436608463,
9.23318699796284E-16));
#68957=CARTESIAN_POINT('Ctrl Pts',(-0.366035043915957,-0.425345967666594,
-5.57238779820851E-16));
#68958=CARTESIAN_POINT('Ctrl Pts',(-0.345069333505709,-0.444737671558352,
-3.64291929955129E-16));
#68959=CARTESIAN_POINT('Ctrl Pts',(-0.331576851910909,-0.457217201358757,
-2.40120997053403E-16));
#68960=CARTESIAN_POINT('Ctrl Pts',(-0.317475581157184,-0.469028537099824,
9.23032294553399E-16));
#68961=CARTESIAN_POINT('Ctrl Pts',(-0.302808350652492,-0.480119506590464,
9.03790930983916E-16));
#68962=CARTESIAN_POINT('Ctrl Pts',(-0.291140523150296,-0.488942407328781,
8.87259861740289E-16));
#68963=CARTESIAN_POINT('Ctrl Pts',(-0.279114374699222,-0.497309373181222,
1.62196618340084E-15));
#68964=CARTESIAN_POINT('Ctrl Pts',(-0.266759816115952,-0.505209972003307,
1.64451785522601E-15));
#68965=CARTESIAN_POINT('Ctrl Pts',(-0.261397323725431,-0.508639224515927,
1.65430640151368E-15));
#68966=CARTESIAN_POINT('Ctrl Pts',(-0.255972929899824,-0.51198057793193,
5.15295006550516E-16));
#68967=CARTESIAN_POINT('Ctrl Pts',(-0.250488958758761,-0.515233006220709,
4.82253126321552E-16));
#68968=CARTESIAN_POINT('Ctrl Pts',(-0.244806899749902,-0.518602916270116,
4.48017732225684E-16));
#68969=CARTESIAN_POINT('Ctrl Pts',(-0.239068043186357,-0.521873056054226,
8.87214571818307E-16));
#68970=CARTESIAN_POINT('Ctrl Pts',(-0.233279325439751,-0.525040899581259,
8.62157567560473E-16));
#68971=CARTESIAN_POINT('Ctrl Pts',(-0.207742211930793,-0.539015942633911,
7.51617791752285E-16));
#68972=CARTESIAN_POINT('Ctrl Pts',(-0.181214866084196,-0.551016628517353,
1.89496927408592E-15));
#68973=CARTESIAN_POINT('Ctrl Pts',(-0.15395161752934,-0.560992522191175,
1.26027660529715E-15));
#68974=CARTESIAN_POINT('Ctrl Pts',(-0.126481843682384,-0.571043985522471,
6.20775995570898E-16));
#68975=CARTESIAN_POINT('Ctrl Pts',(-0.0982638372323879,-0.5790405373196,
-4.73556415712161E-16));
#68976=CARTESIAN_POINT('Ctrl Pts',(-0.0695277070223783,-0.584888355781468,
-1.35763796038635E-15));
#68977=CARTESIAN_POINT('Ctrl Pts',(-0.0588916184022295,-0.587052805724463,
-1.68486259320477E-15));
#68978=CARTESIAN_POINT('Ctrl Pts',(-0.04818434176478,-0.58892242285403,
2.76336445804202E-17));
#68979=CARTESIAN_POINT('Ctrl Pts',(-0.0374170035146651,-0.590490705661811,
0.));
#68980=CARTESIAN_POINT('Ctrl Pts',(-0.0374170035146651,-0.590490705661811,
0.));
#68981=CARTESIAN_POINT('Ctrl Pts',(-0.135716027844311,-0.584261894770184,
-0.00463654331525316));
#68982=CARTESIAN_POINT('Ctrl Pts',(-0.23237971190286,-0.553015871596231,
-0.00927308663050638));
#68983=CARTESIAN_POINT('Ctrl Pts',(-0.315661655680501,-0.500499137650197,
-0.0139096299457595));
#68984=CARTESIAN_POINT('Ctrl Pts',(-0.398943599458139,-0.447982403704166,
-0.0185461732610124));
#68985=CARTESIAN_POINT('Ctrl Pts',(-0.468843802954871,-0.374194958986059,
-0.0231827165762653));
#68986=CARTESIAN_POINT('Ctrl Pts',(-0.516804481271218,-0.288189149275334,
-0.0278192598915181));
#68987=CARTESIAN_POINT('Ctrl Pts',(-0.564765159587562,-0.202183339564614,
-0.0324558032067708));
#68988=CARTESIAN_POINT('Ctrl Pts',(-0.590786312723525,-0.103959164861278,
-0.0370923465220234));
#68989=CARTESIAN_POINT('Ctrl Pts',(-0.591699434208916,-0.00549578503077282,
-0.041728889837276));
#68990=CARTESIAN_POINT('Ctrl Pts',(-0.591716409854293,-0.00366527348840485,
-0.0418150868180202));
#68991=CARTESIAN_POINT('Ctrl Pts',(-0.591724707729724,-0.0018346792726083,
-0.0419012837987644));
#68992=CARTESIAN_POINT('Ctrl Pts',(-0.591724346791278,-4.07989592221547E-6,
-0.0419874807795086));
#68993=CARTESIAN_POINT('Origin',(0.,0.,0.682383483348824));
#68994=CARTESIAN_POINT('',(0.9,-0.519615242270664,0.64363448015713));
#68995=CARTESIAN_POINT('',(-1.90903542970483E-16,-1.03923048454133,0.64363448015713));
#68996=CARTESIAN_POINT('Ctrl Pts',(0.9,-0.519615242270664,0.64363448015713));
#68997=CARTESIAN_POINT('Ctrl Pts',(0.45,-0.779422863405995,0.79363448015713));
#68998=CARTESIAN_POINT('Ctrl Pts',(-1.90903542970483E-16,-1.03923048454133,
0.64363448015713));
#68999=CARTESIAN_POINT('',(0.9,0.519615242270663,0.64363448015713));
#69000=CARTESIAN_POINT('Ctrl Pts',(0.9,0.519615242270663,0.64363448015713));
#69001=CARTESIAN_POINT('Ctrl Pts',(0.9,-2.22044604925031E-16,0.79363448015713));
#69002=CARTESIAN_POINT('Ctrl Pts',(0.9,-0.519615242270664,0.64363448015713));
#69003=CARTESIAN_POINT('',(6.36345143234944E-17,1.03923048454133,0.64363448015713));
#69004=CARTESIAN_POINT('Ctrl Pts',(6.36345143234944E-17,1.03923048454133,
0.64363448015713));
#69005=CARTESIAN_POINT('Ctrl Pts',(0.45,0.779422863405995,0.79363448015713));
#69006=CARTESIAN_POINT('Ctrl Pts',(0.9,0.519615242270663,0.64363448015713));
#69007=CARTESIAN_POINT('',(-0.9,0.519615242270663,0.64363448015713));
#69008=CARTESIAN_POINT('Ctrl Pts',(-0.9,0.519615242270663,0.64363448015713));
#69009=CARTESIAN_POINT('Ctrl Pts',(-0.45,0.779422863405995,0.79363448015713));
#69010=CARTESIAN_POINT('Ctrl Pts',(6.36345143234944E-17,1.03923048454133,
0.64363448015713));
#69011=CARTESIAN_POINT('',(-0.9,-8.02243635933536E-17,0.724019237886466));
#69012=CARTESIAN_POINT('Ctrl Pts',(-0.9,-5.02305152634454E-17,0.724019237886467));
#69013=CARTESIAN_POINT('Ctrl Pts',(-0.9,0.24115427318801,0.724019237886467));
#69014=CARTESIAN_POINT('Ctrl Pts',(-0.9,0.519615242270663,0.64363448015713));
#69015=CARTESIAN_POINT('',(-0.855,-1.04707301327099E-16,0.75));
#69016=CARTESIAN_POINT('',(-0.972115242270663,-1.19049781984912E-16,0.682383483348824));
#69017=CARTESIAN_POINT('Origin',(0.,0.,0.75));
#69018=CARTESIAN_POINT('',(-0.9,-0.519615242270663,0.64363448015713));
#69019=CARTESIAN_POINT('Ctrl Pts',(-0.9,-0.519615242270663,0.64363448015713));
#69020=CARTESIAN_POINT('Ctrl Pts',(-0.9,-0.24115427318801,0.724019237886466));
#69021=CARTESIAN_POINT('Ctrl Pts',(-0.9,-5.02305152634454E-17,0.724019237886467));
#69022=CARTESIAN_POINT('Ctrl Pts',(-1.90903542970483E-16,-1.03923048454133,
0.64363448015713));
#69023=CARTESIAN_POINT('Ctrl Pts',(-0.45,-0.779422863405995,0.79363448015713));
#69024=CARTESIAN_POINT('Ctrl Pts',(-0.9,-0.519615242270663,0.64363448015713));
#69025=CARTESIAN_POINT('Origin',(6.36345143234944E-17,1.03923048454133,
0.05));
#69026=CARTESIAN_POINT('',(6.36345143234944E-17,1.03923048454133,0.05));
#69027=CARTESIAN_POINT('',(6.36345143234944E-17,1.03923048454133,0.05));
#69028=CARTESIAN_POINT('',(-0.9,0.519615242270663,0.05));
#69029=CARTESIAN_POINT('',(6.36345143234944E-17,1.03923048454133,0.05));
#69030=CARTESIAN_POINT('',(-0.9,0.519615242270663,0.05));
#69031=CARTESIAN_POINT('Origin',(0.9,0.519615242270663,0.05));
#69032=CARTESIAN_POINT('',(0.9,0.519615242270663,0.05));
#69033=CARTESIAN_POINT('',(0.9,0.519615242270663,0.05));
#69034=CARTESIAN_POINT('',(0.9,0.519615242270663,0.05));
#69035=CARTESIAN_POINT('Origin',(0.9,-0.519615242270664,0.05));
#69036=CARTESIAN_POINT('',(0.9,-0.519615242270664,0.05));
#69037=CARTESIAN_POINT('',(0.9,-0.519615242270664,0.05));
#69038=CARTESIAN_POINT('',(0.9,-0.519615242270664,0.05));
#69039=CARTESIAN_POINT('Origin',(0.,0.,0.05));
#69040=CARTESIAN_POINT('',(-1.90903542970483E-16,-1.03923048454133,0.05));
#69041=CARTESIAN_POINT('',(-1.90903542970483E-16,-1.03923048454133,0.05));
#69042=CARTESIAN_POINT('',(-0.9,-0.519615242270663,0.05));
#69043=CARTESIAN_POINT('',(-0.9,-0.519615242270663,0.05));
#69044=CARTESIAN_POINT('',(-0.9,0.519615242270663,0.05));
#69045=CARTESIAN_POINT('',(-0.83,-1.0164568432923E-16,0.05));
#69046=CARTESIAN_POINT('Origin',(0.,0.,0.05));
#69047=CARTESIAN_POINT('Origin',(-1.90903542970483E-16,-1.03923048454133,
0.05));
#69048=CARTESIAN_POINT('',(-1.90903542970483E-16,-1.03923048454133,0.05));
#69049=CARTESIAN_POINT('Origin',(-0.9,-0.519615242270663,0.05));
#69050=CARTESIAN_POINT('',(-0.9,-0.519615242270663,0.05));
#69051=CARTESIAN_POINT('Origin',(-0.9,0.519615242270663,0.05));
#69052=CARTESIAN_POINT('Origin',(0.,0.,0.75));
#69053=CARTESIAN_POINT('Origin',(0.54,0.,-4.));
#69054=CARTESIAN_POINT('',(-0.54,-6.61309271539571E-17,-4.));
#69055=CARTESIAN_POINT('Origin',(0.,0.,-4.));
#69056=CARTESIAN_POINT('Origin',(0.,0.,-3.97));
#69057=CARTESIAN_POINT('',(-0.57,-6.98048675513991E-17,-3.97));
#69058=CARTESIAN_POINT('Origin',(0.,0.,-1.97));
#69059=CARTESIAN_POINT('Origin',(0.,0.,0.));
#69060=CARTESIAN_POINT('Origin',(0.83,0.,0.));
#69061=CARTESIAN_POINT('',(-0.83,-1.0164568432923E-16,0.));
#69062=CARTESIAN_POINT('Origin',(0.,0.,0.));
#69063=CARTESIAN_POINT('Origin',(0.,0.,0.025));
#69064=CARTESIAN_POINT('',(-0.83,-1.0164568432923E-16,0.025));
#76635=UNCERTAINTY_MEASURE_WITH_UNIT(LENGTH_MEASURE(0.001),#76661,
'DISTANCE_ACCURACY_VALUE',
'Maximum model space distance between geometric entities at asserted c
onnectivities');
#76638=UNCERTAINTY_MEASURE_WITH_UNIT(LENGTH_MEASURE(0.001),#76661,
'DISTANCE_ACCURACY_VALUE',
'Maximum model space distance between geometric entities at asserted c
onnectivities');
#76657=(
GEOMETRIC_REPRESENTATION_CONTEXT(3)
GLOBAL_UNCERTAINTY_ASSIGNED_CONTEXT((#76635))
GLOBAL_UNIT_ASSIGNED_CONTEXT((#76661,#76663,#76664))
REPRESENTATION_CONTEXT('','3D')
);
#76660=(
GEOMETRIC_REPRESENTATION_CONTEXT(3)
GLOBAL_UNCERTAINTY_ASSIGNED_CONTEXT((#76638))
GLOBAL_UNIT_ASSIGNED_CONTEXT((#76661,#76663,#76664))
REPRESENTATION_CONTEXT('','3D')
);
#76661=(
LENGTH_UNIT()
NAMED_UNIT(*)
SI_UNIT(.CENTI.,.METRE.)
);
#76663=(
NAMED_UNIT(*)
PLANE_ANGLE_UNIT()
SI_UNIT($,.RADIAN.)
);
#76664=(
NAMED_UNIT(*)
SI_UNIT($,.STERADIAN.)
SOLID_ANGLE_UNIT()
);
#76683=SHAPE_DEFINITION_REPRESENTATION(#76704,#76753);
#76704=PRODUCT_DEFINITION_SHAPE('',$,#76775);
#76753=SHAPE_REPRESENTATION('',(#28560),#76657);
#76756=PRODUCT_DEFINITION_CONTEXT('part definition',#76821,'design');
#76775=PRODUCT_DEFINITION('2026-10-26-11-13-29-864',
'15_Offset_Adjusting_Screw_ISO_4017_M12x40',#76796,#76756);
#76796=PRODUCT_DEFINITION_FORMATION('',$,#76841);
#76821=APPLICATION_CONTEXT(
'Core Data for Automotive Mechanical Design Process');
#76822=PRODUCT_CONTEXT('part definition',#76821,'mechanical');
#76841=PRODUCT('2026-10-26-11-13-29-864',
'15_Offset_Adjusting_Screw_ISO_4017_M12x40',$,(#76822));
#76907=COLOUR_RGB('Black',0.12,0.14,0.17);
#76908=FILL_AREA_STYLE_COLOUR('',#76907);
#76909=FILL_AREA_STYLE('',(#76908));
#76910=SURFACE_STYLE_FILL_AREA(#76909);
#76911=SURFACE_SIDE_STYLE('',(#76910));
#76912=SURFACE_STYLE_USAGE(.BOTH.,#76911);
#76913=PRESENTATION_STYLE_ASSIGNMENT((#76912));
ENDSEC;
END-ISO-10303-21;
